ISO-10303-21;
HEADER;
/* Generated by software containing ST-Developer
 * from STEP Tools, Inc. (www.steptools.com) 
 */

FILE_DESCRIPTION(
/* description */ ('Independent two-stage fixed-ring planetary gearbox,24/24/72 teeth,mod
ule2,20deg involutes,three planets per stage,4:1 x4:1=16:1. Native cut
-space/fillet/pattern tooth profiles derived from reusable gear blanks
; shared sun/planet/ring/carrier parts across both stages. Captured br
onze-journal input/carriers, headed retained planet pins, keyed inters
tage drive and modular keyed output interface. Native ideal gear links
; no torque, precision grade, production backlash/fits, lubrication, s
peed or life rating.'),
/* implementation_level */ '2;1');

FILE_NAME(
/* name */ 'Socket head cap screw M6x20.step',
/* time_stamp */ '2026-11-08T19:10:00-08:00',
/* author */ (''),
/* organization */ (''),
/* preprocessor_version */ 'ST-DEVELOPER v20.2',
/* originating_system */ 'Autodesk Translation Framework v15.17.0.0',
/* authorisation */ '');

FILE_SCHEMA (('AUTOMOTIVE_DESIGN { 1 0 10303 214 3 1 1 }'));
ENDSEC;

DATA;
#10=MECHANICAL_DESIGN_GEOMETRIC_PRESENTATION_REPRESENTATION('',(#1182),#259224);
#1142=SHAPE_REPRESENTATION_RELATIONSHIP('SRR','None',#259389,#1162);
#1162=ADVANCED_BREP_SHAPE_REPRESENTATION('',(#1202),#259223);
#1182=STYLED_ITEM('',(#259492),#1202);
#1202=MANIFOLD_SOLID_BREP('Socket head cap screw M6x20',#25169);
#1316=FACE_BOUND('',#4500,.T.);
#1317=FACE_BOUND('',#4503,.T.);
#1478=B_SPLINE_SURFACE_WITH_KNOTS('',3,3,((#257559,#257560,#257561,#257562,
#257563,#257564,#257565,#257566,#257567,#257568,#257569,#257570,#257571,
#257572,#257573,#257574,#257575,#257576,#257577,#257578,#257579,#257580,
#257581,#257582,#257583,#257584,#257585,#257586,#257587,#257588,#257589,
#257590,#257591,#257592,#257593,#257594,#257595,#257596,#257597,#257598,
#257599,#257600,#257601,#257602,#257603,#257604,#257605,#257606,#257607,
#257608,#257609,#257610,#257611,#257612,#257613,#257614,#257615,#257616,
#257617,#257618,#257619,#257620,#257621,#257622,#257623,#257624,#257625,
#257626,#257627,#257628,#257629,#257630,#257631,#257632,#257633,#257634,
#257635,#257636,#257637,#257638,#257639,#257640,#257641,#257642,#257643,
#257644,#257645,#257646,#257647,#257648,#257649,#257650,#257651,#257652,
#257653,#257654,#257655,#257656,#257657,#257658,#257659,#257660,#257661,
#257662,#257663,#257664,#257665,#257666,#257667,#257668,#257669,#257670,
#257671,#257672,#257673,#257674,#257675,#257676,#257677,#257678,#257679,
#257680,#257681,#257682,#257683,#257684,#257685,#257686,#257687,#257688,
#257689),(#257690,#257691,#257692,#257693,#257694,#257695,#257696,#257697,
#257698,#257699,#257700,#257701,#257702,#257703,#257704,#257705,#257706,
#257707,#257708,#257709,#257710,#257711,#257712,#257713,#257714,#257715,
#257716,#257717,#257718,#257719,#257720,#257721,#257722,#257723,#257724,
#257725,#257726,#257727,#257728,#257729,#257730,#257731,#257732,#257733,
#257734,#257735,#257736,#257737,#257738,#257739,#257740,#257741,#257742,
#257743,#257744,#257745,#257746,#257747,#257748,#257749,#257750,#257751,
#257752,#257753,#257754,#257755,#257756,#257757,#257758,#257759,#257760,
#257761,#257762,#257763,#257764,#257765,#257766,#257767,#257768,#257769,
#257770,#257771,#257772,#257773,#257774,#257775,#257776,#257777,#257778,
#257779,#257780,#257781,#257782,#257783,#257784,#257785,#257786,#257787,
#257788,#257789,#257790,#257791,#257792,#257793,#257794,#257795,#257796,
#257797,#257798,#257799,#257800,#257801,#257802,#257803,#257804,#257805,
#257806,#257807,#257808,#257809,#257810,#257811,#257812,#257813,#257814,
#257815,#257816,#257817,#257818,#257819,#257820),(#257821,#257822,#257823,
#257824,#257825,#257826,#257827,#257828,#257829,#257830,#257831,#257832,
#257833,#257834,#257835,#257836,#257837,#257838,#257839,#257840,#257841,
#257842,#257843,#257844,#257845,#257846,#257847,#257848,#257849,#257850,
#257851,#257852,#257853,#257854,#257855,#257856,#257857,#257858,#257859,
#257860,#257861,#257862,#257863,#257864,#257865,#257866,#257867,#257868,
#257869,#257870,#257871,#257872,#257873,#257874,#257875,#257876,#257877,
#257878,#257879,#257880,#257881,#257882,#257883,#257884,#257885,#257886,
#257887,#257888,#257889,#257890,#257891,#257892,#257893,#257894,#257895,
#257896,#257897,#257898,#257899,#257900,#257901,#257902,#257903,#257904,
#257905,#257906,#257907,#257908,#257909,#257910,#257911,#257912,#257913,
#257914,#257915,#257916,#257917,#257918,#257919,#257920,#257921,#257922,
#257923,#257924,#257925,#257926,#257927,#257928,#257929,#257930,#257931,
#257932,#257933,#257934,#257935,#257936,#257937,#257938,#257939,#257940,
#257941,#257942,#257943,#257944,#257945,#257946,#257947,#257948,#257949,
#257950,#257951),(#257952,#257953,#257954,#257955,#257956,#257957,#257958,
#257959,#257960,#257961,#257962,#257963,#257964,#257965,#257966,#257967,
#257968,#257969,#257970,#257971,#257972,#257973,#257974,#257975,#257976,
#257977,#257978,#257979,#257980,#257981,#257982,#257983,#257984,#257985,
#257986,#257987,#257988,#257989,#257990,#257991,#257992,#257993,#257994,
#257995,#257996,#257997,#257998,#257999,#258000,#258001,#258002,#258003,
#258004,#258005,#258006,#258007,#258008,#258009,#258010,#258011,#258012,
#258013,#258014,#258015,#258016,#258017,#258018,#258019,#258020,#258021,
#258022,#258023,#258024,#258025,#258026,#258027,#258028,#258029,#258030,
#258031,#258032,#258033,#258034,#258035,#258036,#258037,#258038,#258039,
#258040,#258041,#258042,#258043,#258044,#258045,#258046,#258047,#258048,
#258049,#258050,#258051,#258052,#258053,#258054,#258055,#258056,#258057,
#258058,#258059,#258060,#258061,#258062,#258063,#258064,#258065,#258066,
#258067,#258068,#258069,#258070,#258071,#258072,#258073,#258074,#258075,
#258076,#258077,#258078,#258079,#258080,#258081,#258082)),.UNSPECIFIED.,
 .F.,.F.,.F.,(4,4),(4,1,1,1,1,1,1,1,1,1,1,1,1,1,1,1,1,1,1,1,1,1,1,1,1,1,
1,1,1,1,1,1,1,1,1,1,1,1,1,1,1,1,1,1,1,1,1,1,1,1,1,1,1,1,1,1,1,1,1,1,1,1,
1,1,1,1,1,1,1,1,1,1,1,1,1,1,1,1,1,1,1,1,1,1,1,1,1,1,1,1,1,1,1,1,1,1,1,1,
1,1,1,1,1,1,1,1,1,1,1,1,1,1,1,1,1,1,1,1,1,1,1,1,1,1,1,1,1,1,4),(0.,0.0658467982010768),
(8.30747755240104,9.30538649238933,10.3032954323776,11.3012043723659,12.2991133123542,
13.2970222523425,14.2949311923308,15.2928401323191,16.2907490723073,17.2886580122956,
18.2865669522839,19.2844758922722,20.2823848322605,21.2802937722488,22.2782027122371,
23.2761116522254,24.2740205922137,25.2719295322019,26.2698384721902,27.2677474121785,
28.2656563521668,29.2635652921551,30.2614742321434,31.2593831721317,32.25729211212,
33.2552010521082,34.2531099920965,35.2510189320848,36.2489278720731,37.2468368120614,
38.2447457520497,39.242654692038,40.2405636320263,41.2384725720146,42.2363815120028,
43.2342904519911,44.2321993919794,45.2301083319677,46.228017271956,47.2259262119443,
48.2238351519326,49.2217440919209,50.2196530319092,51.2175619718974,52.2154709118857,
53.213379851874,54.2112887918623,55.2091977318506,56.2071066718389,57.2050156118272,
58.2029245518155,59.2008334918037,60.198742431792,61.1966513717803,62.1945603117686,
63.1924692517569,64.1903781917452,65.1882871317335,66.1861960717218,67.1841050117101,
68.1820139516983,69.1799228916866,70.1778318316749,71.1757407716632,72.1736497116515,
73.1715586516398,74.1694675916281,75.1673765316164,76.1652854716046,77.1631944115929,
78.1611033515812,79.1590122915695,80.1569212315578,81.1548301715461,82.1527391115344,
83.1506480515227,84.148556991511,85.1464659314993,86.1443748714875,87.1422838114758,
88.1401927514641,89.1381016914524,90.1360106314407,91.133919571429,92.1318285114173,
93.1297374514056,94.1276463913938,95.1255553313821,96.1234642713704,97.1213732113587,
98.119282151347,99.1171910913353,100.115100031324,101.113008971312,102.1109179113,
103.108826851288,104.106735791277,105.104644731265,106.102553671253,107.100462611242,
108.09837155123,109.096280491218,110.094189431206,111.092098371195,112.090007311183,
113.087916251171,114.08582519116,115.083734131148,116.081643071136,117.079552011124,
118.077460951113,119.075369891101,120.073278831089,121.071187771078,122.069096711066,
123.067005651054,124.064914591042,125.062823531031,126.060732471019,127.058641411007,
128.056550350996,129.054459290984,130.052368230972,131.05027717096,132.048186110949,
133.046095050937,134.044003990925,135.041912930914,136.039821870902),
 .UNSPECIFIED.);
#1479=B_SPLINE_SURFACE_WITH_KNOTS('',3,3,((#258309,#258310,#258311,#258312,
#258313,#258314,#258315,#258316,#258317,#258318,#258319,#258320,#258321,
#258322,#258323,#258324,#258325,#258326,#258327,#258328,#258329,#258330,
#258331,#258332,#258333,#258334,#258335,#258336,#258337,#258338,#258339,
#258340,#258341,#258342,#258343,#258344,#258345,#258346,#258347,#258348,
#258349,#258350,#258351,#258352,#258353,#258354,#258355,#258356,#258357,
#258358,#258359,#258360,#258361,#258362,#258363,#258364,#258365,#258366,
#258367,#258368,#258369,#258370,#258371,#258372,#258373,#258374,#258375,
#258376,#258377,#258378,#258379,#258380,#258381,#258382,#258383,#258384,
#258385,#258386,#258387,#258388,#258389,#258390,#258391,#258392,#258393,
#258394,#258395,#258396,#258397,#258398,#258399,#258400,#258401,#258402,
#258403,#258404,#258405,#258406,#258407,#258408,#258409,#258410,#258411,
#258412,#258413,#258414,#258415,#258416,#258417,#258418,#258419,#258420,
#258421,#258422,#258423,#258424,#258425,#258426,#258427,#258428,#258429,
#258430,#258431,#258432,#258433,#258434,#258435,#258436,#258437,#258438,
#258439),(#258440,#258441,#258442,#258443,#258444,#258445,#258446,#258447,
#258448,#258449,#258450,#258451,#258452,#258453,#258454,#258455,#258456,
#258457,#258458,#258459,#258460,#258461,#258462,#258463,#258464,#258465,
#258466,#258467,#258468,#258469,#258470,#258471,#258472,#258473,#258474,
#258475,#258476,#258477,#258478,#258479,#258480,#258481,#258482,#258483,
#258484,#258485,#258486,#258487,#258488,#258489,#258490,#258491,#258492,
#258493,#258494,#258495,#258496,#258497,#258498,#258499,#258500,#258501,
#258502,#258503,#258504,#258505,#258506,#258507,#258508,#258509,#258510,
#258511,#258512,#258513,#258514,#258515,#258516,#258517,#258518,#258519,
#258520,#258521,#258522,#258523,#258524,#258525,#258526,#258527,#258528,
#258529,#258530,#258531,#258532,#258533,#258534,#258535,#258536,#258537,
#258538,#258539,#258540,#258541,#258542,#258543,#258544,#258545,#258546,
#258547,#258548,#258549,#258550,#258551,#258552,#258553,#258554,#258555,
#258556,#258557,#258558,#258559,#258560,#258561,#258562,#258563,#258564,
#258565,#258566,#258567,#258568,#258569,#258570),(#258571,#258572,#258573,
#258574,#258575,#258576,#258577,#258578,#258579,#258580,#258581,#258582,
#258583,#258584,#258585,#258586,#258587,#258588,#258589,#258590,#258591,
#258592,#258593,#258594,#258595,#258596,#258597,#258598,#258599,#258600,
#258601,#258602,#258603,#258604,#258605,#258606,#258607,#258608,#258609,
#258610,#258611,#258612,#258613,#258614,#258615,#258616,#258617,#258618,
#258619,#258620,#258621,#258622,#258623,#258624,#258625,#258626,#258627,
#258628,#258629,#258630,#258631,#258632,#258633,#258634,#258635,#258636,
#258637,#258638,#258639,#258640,#258641,#258642,#258643,#258644,#258645,
#258646,#258647,#258648,#258649,#258650,#258651,#258652,#258653,#258654,
#258655,#258656,#258657,#258658,#258659,#258660,#258661,#258662,#258663,
#258664,#258665,#258666,#258667,#258668,#258669,#258670,#258671,#258672,
#258673,#258674,#258675,#258676,#258677,#258678,#258679,#258680,#258681,
#258682,#258683,#258684,#258685,#258686,#258687,#258688,#258689,#258690,
#258691,#258692,#258693,#258694,#258695,#258696,#258697,#258698,#258699,
#258700,#258701),(#258702,#258703,#258704,#258705,#258706,#258707,#258708,
#258709,#258710,#258711,#258712,#258713,#258714,#258715,#258716,#258717,
#258718,#258719,#258720,#258721,#258722,#258723,#258724,#258725,#258726,
#258727,#258728,#258729,#258730,#258731,#258732,#258733,#258734,#258735,
#258736,#258737,#258738,#258739,#258740,#258741,#258742,#258743,#258744,
#258745,#258746,#258747,#258748,#258749,#258750,#258751,#258752,#258753,
#258754,#258755,#258756,#258757,#258758,#258759,#258760,#258761,#258762,
#258763,#258764,#258765,#258766,#258767,#258768,#258769,#258770,#258771,
#258772,#258773,#258774,#258775,#258776,#258777,#258778,#258779,#258780,
#258781,#258782,#258783,#258784,#258785,#258786,#258787,#258788,#258789,
#258790,#258791,#258792,#258793,#258794,#258795,#258796,#258797,#258798,
#258799,#258800,#258801,#258802,#258803,#258804,#258805,#258806,#258807,
#258808,#258809,#258810,#258811,#258812,#258813,#258814,#258815,#258816,
#258817,#258818,#258819,#258820,#258821,#258822,#258823,#258824,#258825,
#258826,#258827,#258828,#258829,#258830,#258831,#258832)),.UNSPECIFIED.,
 .F.,.F.,.F.,(4,4),(4,1,1,1,1,1,1,1,1,1,1,1,1,1,1,1,1,1,1,1,1,1,1,1,1,1,
1,1,1,1,1,1,1,1,1,1,1,1,1,1,1,1,1,1,1,1,1,1,1,1,1,1,1,1,1,1,1,1,1,1,1,1,
1,1,1,1,1,1,1,1,1,1,1,1,1,1,1,1,1,1,1,1,1,1,1,1,1,1,1,1,1,1,1,1,1,1,1,1,
1,1,1,1,1,1,1,1,1,1,1,1,1,1,1,1,1,1,1,1,1,1,1,1,1,1,1,1,1,1,4),(0.,0.0658467982010768),
(11.6150328478182,12.6129417878065,13.6108507277948,14.6087596677831,15.6066686077714,
16.6045775477597,17.602486487748,18.6003954277363,19.5983043677246,20.5962133077128,
21.5941222477011,22.5920311876894,23.5899401276777,24.587849067666,25.5857580076543,
26.5836669476426,27.5815758876309,28.5794848276191,29.5773937676074,30.5753027075957,
31.573211647584,32.5711205875723,33.5690295275606,34.5669384675489,35.5648474075372,
36.5627563475255,37.5606652875137,38.558574227502,39.5564831674903,40.5543921074786,
41.5523010474669,42.5502099874552,43.5481189274435,44.5460278674318,45.54393680742,
46.5418457474083,47.5397546873966,48.5376636273849,49.5355725673732,50.5334815073615,
51.5313904473498,52.5292993873381,53.5272083273263,54.5251172673146,55.5230262073029,
56.5209351472912,57.5188440872795,58.5167530272678,59.5146619672561,60.5125709072444,
61.5104798472327,62.5083887872209,63.5062977272092,64.5042066671975,65.5021156071858,
66.5000245471741,67.4979334871624,68.4958424271507,69.493751367139,70.4916603071272,
71.4895692471155,72.4874781871038,73.4853871270921,74.4832960670804,75.4812050070687,
76.479113947057,77.4770228870453,78.4749318270335,79.4728407670218,80.4707497070101,
81.4686586469984,82.4665675869867,83.464476526975,84.4623854669633,85.4602944069516,
86.4582033469399,87.4561122869281,88.4540212269164,89.4519301669047,90.449839106893,
91.4477480468813,92.4456569868696,93.4435659268579,94.4414748668462,95.4393838068345,
96.4372927468227,97.435201686811,98.4331106267993,99.4310195667876,100.428928506776,
101.426837446764,102.424746386752,103.422655326741,104.420564266729,105.418473206717,
106.416382146706,107.414291086694,108.412200026682,109.41010896667,110.408017906659,
111.405926846647,112.403835786635,113.401744726624,114.399653666612,115.3975626066,
116.395471546589,117.393380486577,118.391289426565,119.389198366553,120.387107306542,
121.38501624653,122.382925186518,123.380834126507,124.378743066495,125.376652006483,
126.374560946471,127.37246988646,128.370378826448,129.368287766436,130.366196706425,
131.364105646413,132.362014586401,133.359923526389,134.357832466378,135.355741406366,
136.353650346354,137.351559286343,138.349468226331,139.347377166319),
 .UNSPECIFIED.);
#1688=PLANE('',#27223);
#1689=PLANE('',#27224);
#1690=PLANE('',#27225);
#1691=PLANE('',#27226);
#1692=PLANE('',#27227);
#1693=PLANE('',#27228);
#1694=PLANE('',#27229);
#1695=PLANE('',#27230);
#1696=PLANE('',#27234);
#1697=PLANE('',#27235);
#2989=FACE_OUTER_BOUND('',#4448,.T.);
#2990=FACE_OUTER_BOUND('',#4449,.T.);
#2991=FACE_OUTER_BOUND('',#4450,.T.);
#2992=FACE_OUTER_BOUND('',#4451,.T.);
#2993=FACE_OUTER_BOUND('',#4452,.T.);
#2994=FACE_OUTER_BOUND('',#4453,.T.);
#2995=FACE_OUTER_BOUND('',#4454,.T.);
#2996=FACE_OUTER_BOUND('',#4455,.T.);
#2997=FACE_OUTER_BOUND('',#4456,.T.);
#2998=FACE_OUTER_BOUND('',#4457,.T.);
#2999=FACE_OUTER_BOUND('',#4458,.T.);
#3000=FACE_OUTER_BOUND('',#4459,.T.);
#3001=FACE_OUTER_BOUND('',#4460,.T.);
#3002=FACE_OUTER_BOUND('',#4461,.T.);
#3003=FACE_OUTER_BOUND('',#4462,.T.);
#3004=FACE_OUTER_BOUND('',#4463,.T.);
#3005=FACE_OUTER_BOUND('',#4464,.T.);
#3006=FACE_OUTER_BOUND('',#4465,.T.);
#3007=FACE_OUTER_BOUND('',#4466,.T.);
#3008=FACE_OUTER_BOUND('',#4467,.T.);
#3009=FACE_OUTER_BOUND('',#4468,.T.);
#3010=FACE_OUTER_BOUND('',#4469,.T.);
#3011=FACE_OUTER_BOUND('',#4470,.T.);
#3012=FACE_OUTER_BOUND('',#4471,.T.);
#3013=FACE_OUTER_BOUND('',#4472,.T.);
#3014=FACE_OUTER_BOUND('',#4473,.T.);
#3015=FACE_OUTER_BOUND('',#4474,.T.);
#3016=FACE_OUTER_BOUND('',#4475,.T.);
#3017=FACE_OUTER_BOUND('',#4476,.T.);
#3018=FACE_OUTER_BOUND('',#4477,.T.);
#3019=FACE_OUTER_BOUND('',#4478,.T.);
#3020=FACE_OUTER_BOUND('',#4479,.T.);
#3021=FACE_OUTER_BOUND('',#4480,.T.);
#3022=FACE_OUTER_BOUND('',#4481,.T.);
#3023=FACE_OUTER_BOUND('',#4482,.T.);
#3024=FACE_OUTER_BOUND('',#4483,.T.);
#3025=FACE_OUTER_BOUND('',#4484,.T.);
#3026=FACE_OUTER_BOUND('',#4485,.T.);
#3027=FACE_OUTER_BOUND('',#4486,.T.);
#3028=FACE_OUTER_BOUND('',#4487,.T.);
#3029=FACE_OUTER_BOUND('',#4488,.T.);
#3030=FACE_OUTER_BOUND('',#4489,.T.);
#3031=FACE_OUTER_BOUND('',#4490,.T.);
#3032=FACE_OUTER_BOUND('',#4491,.T.);
#3033=FACE_OUTER_BOUND('',#4492,.T.);
#3034=FACE_OUTER_BOUND('',#4493,.T.);
#3035=FACE_OUTER_BOUND('',#4494,.T.);
#3036=FACE_OUTER_BOUND('',#4495,.T.);
#3037=FACE_OUTER_BOUND('',#4496,.T.);
#3038=FACE_OUTER_BOUND('',#4497,.T.);
#3039=FACE_OUTER_BOUND('',#4498,.T.);
#3040=FACE_OUTER_BOUND('',#4499,.T.);
#3041=FACE_OUTER_BOUND('',#4501,.T.);
#3042=FACE_OUTER_BOUND('',#4502,.T.);
#3043=FACE_OUTER_BOUND('',#4504,.T.);
#4448=EDGE_LOOP('',(#22772,#22773,#22774,#22775));
#4449=EDGE_LOOP('',(#22776,#22777,#22778,#22779));
#4450=EDGE_LOOP('',(#22780,#22781,#22782,#22783));
#4451=EDGE_LOOP('',(#22784,#22785,#22786,#22787));
#4452=EDGE_LOOP('',(#22788,#22789,#22790,#22791));
#4453=EDGE_LOOP('',(#22792,#22793,#22794,#22795));
#4454=EDGE_LOOP('',(#22796,#22797,#22798,#22799));
#4455=EDGE_LOOP('',(#22800,#22801,#22802,#22803));
#4456=EDGE_LOOP('',(#22804,#22805,#22806,#22807));
#4457=EDGE_LOOP('',(#22808,#22809,#22810,#22811));
#4458=EDGE_LOOP('',(#22812,#22813,#22814,#22815));
#4459=EDGE_LOOP('',(#22816,#22817,#22818,#22819));
#4460=EDGE_LOOP('',(#22820,#22821,#22822,#22823));
#4461=EDGE_LOOP('',(#22824,#22825,#22826,#22827));
#4462=EDGE_LOOP('',(#22828,#22829,#22830,#22831));
#4463=EDGE_LOOP('',(#22832,#22833,#22834,#22835));
#4464=EDGE_LOOP('',(#22836,#22837,#22838,#22839));
#4465=EDGE_LOOP('',(#22840,#22841,#22842,#22843));
#4466=EDGE_LOOP('',(#22844,#22845,#22846,#22847));
#4467=EDGE_LOOP('',(#22848,#22849,#22850,#22851));
#4468=EDGE_LOOP('',(#22852,#22853,#22854,#22855));
#4469=EDGE_LOOP('',(#22856,#22857,#22858,#22859));
#4470=EDGE_LOOP('',(#22860,#22861,#22862,#22863));
#4471=EDGE_LOOP('',(#22864,#22865,#22866,#22867));
#4472=EDGE_LOOP('',(#22868,#22869,#22870,#22871));
#4473=EDGE_LOOP('',(#22872,#22873,#22874,#22875));
#4474=EDGE_LOOP('',(#22876,#22877,#22878,#22879));
#4475=EDGE_LOOP('',(#22880,#22881,#22882,#22883));
#4476=EDGE_LOOP('',(#22884,#22885,#22886,#22887));
#4477=EDGE_LOOP('',(#22888,#22889,#22890,#22891));
#4478=EDGE_LOOP('',(#22892,#22893,#22894,#22895));
#4479=EDGE_LOOP('',(#22896,#22897,#22898,#22899));
#4480=EDGE_LOOP('',(#22900,#22901,#22902,#22903));
#4481=EDGE_LOOP('',(#22904,#22905,#22906,#22907));
#4482=EDGE_LOOP('',(#22908,#22909,#22910,#22911));
#4483=EDGE_LOOP('',(#22912,#22913,#22914,#22915));
#4484=EDGE_LOOP('',(#22916,#22917,#22918,#22919));
#4485=EDGE_LOOP('',(#22920,#22921,#22922,#22923));
#4486=EDGE_LOOP('',(#22924,#22925,#22926,#22927));
#4487=EDGE_LOOP('',(#22928,#22929,#22930,#22931));
#4488=EDGE_LOOP('',(#22932,#22933,#22934,#22935,#22936,#22937,#22938,#22939,
#22940,#22941,#22942,#22943,#22944,#22945,#22946,#22947,#22948,#22949,#22950,
#22951,#22952,#22953,#22954,#22955,#22956,#22957,#22958,#22959,#22960,#22961,
#22962,#22963,#22964,#22965,#22966,#22967,#22968,#22969,#22970,#22971,#22972,
#22973,#22974,#22975));
#4489=EDGE_LOOP('',(#22976,#22977,#22978,#22979));
#4490=EDGE_LOOP('',(#22980,#22981,#22982,#22983,#22984,#22985,#22986,#22987,
#22988,#22989,#22990,#22991,#22992,#22993,#22994,#22995,#22996,#22997,#22998,
#22999,#23000,#23001,#23002,#23003,#23004,#23005,#23006,#23007,#23008,#23009,
#23010,#23011,#23012,#23013,#23014,#23015,#23016,#23017,#23018,#23019,#23020,
#23021,#23022,#23023));
#4491=EDGE_LOOP('',(#23024,#23025,#23026,#23027));
#4492=EDGE_LOOP('',(#23028,#23029,#23030,#23031));
#4493=EDGE_LOOP('',(#23032,#23033,#23034,#23035));
#4494=EDGE_LOOP('',(#23036,#23037,#23038,#23039));
#4495=EDGE_LOOP('',(#23040,#23041,#23042,#23043));
#4496=EDGE_LOOP('',(#23044,#23045,#23046,#23047));
#4497=EDGE_LOOP('',(#23048,#23049,#23050,#23051));
#4498=EDGE_LOOP('',(#23052,#23053,#23054,#23055,#23056,#23057));
#4499=EDGE_LOOP('',(#23058));
#4500=EDGE_LOOP('',(#23059,#23060,#23061,#23062));
#4501=EDGE_LOOP('',(#23063,#23064,#23065,#23066));
#4502=EDGE_LOOP('',(#23067));
#4503=EDGE_LOOP('',(#23068,#23069,#23070,#23071,#23072,#23073));
#4504=EDGE_LOOP('',(#23074,#23075,#23076,#23077));
#5379=CIRCLE('',#27178,2.942);
#5380=CIRCLE('',#27199,2.37175);
#5381=CIRCLE('',#27220,2.37175);
#5382=CIRCLE('',#27222,2.942);
#5383=CIRCLE('',#27231,5.);
#5384=CIRCLE('',#27233,5.);
#6579=B_SPLINE_CURVE_WITH_KNOTS('',3,(#256114,#256115,#256116,#256117,#256118,
#256119,#256120,#256121,#256122,#256123),.UNSPECIFIED.,.F.,.F.,(4,3,3,4),
(-4.09293042013066,-3.99163575995315,-2.99372681996486,-2.06863817490914),
 .UNSPECIFIED.);
#6580=B_SPLINE_CURVE_WITH_KNOTS('',3,(#256126,#256127,#256128,#256129,#256130,
#256131,#256132),.UNSPECIFIED.,.F.,.F.,(4,3,4),(0.,0.997908939988297,1.11730040836816),
 .UNSPECIFIED.);
#6581=B_SPLINE_CURVE_WITH_KNOTS('',3,(#256137,#256138,#256139,#256140,#256141,
#256142,#256143,#256144,#256145,#256146,#256147,#256148,#256149,#256150,
#256151,#256152,#256153,#256154,#256155,#256156,#256157,#256158),
 .UNSPECIFIED.,.F.,.F.,(4,3,3,3,3,3,3,4),(-10.3761157273102,-9.97908939988288,
-8.9811804598946,-7.9832715199063,-6.98536257991802,-5.98745363992973,-4.98954469994144,
-4.09293042013066),.UNSPECIFIED.);
#6582=B_SPLINE_CURVE_WITH_KNOTS('',3,(#256159,#256160,#256161,#256162,#256163,
#256164,#256165,#256166,#256167,#256168,#256169,#256170,#256171,#256172,
#256173,#256174,#256175,#256176,#256177,#256178,#256179,#256180),
 .UNSPECIFIED.,.F.,.F.,(4,3,3,3,3,3,3,4),(1.11730040836816,1.99581787997659,
2.99372681996487,3.99163575995315,4.98954469994144,5.98745363992972,6.98536257991801,
7.40048571554774),.UNSPECIFIED.);
#6583=B_SPLINE_CURVE_WITH_KNOTS('',3,(#256185,#256186,#256187,#256188,#256189,
#256190,#256191,#256192,#256193,#256194,#256195,#256196,#256197,#256198,
#256199,#256200,#256201,#256202,#256203,#256204,#256205,#256206),
 .UNSPECIFIED.,.F.,.F.,(4,3,3,3,3,3,3,4),(-16.6593010344898,-15.9665430398126,
-14.9686340998243,-13.970725159836,-12.9728162198477,-11.9749072798595,
-10.9769983398712,-10.3761157273102),.UNSPECIFIED.);
#6584=B_SPLINE_CURVE_WITH_KNOTS('',3,(#256207,#256208,#256209,#256210,#256211,
#256212,#256213,#256214,#256215,#256216,#256217,#256218,#256219,#256220,
#256221,#256222,#256223,#256224,#256225,#256226,#256227,#256228),
 .UNSPECIFIED.,.F.,.F.,(4,3,3,3,3,3,3,4),(7.40048571554774,7.9832715199063,
8.98118045989459,9.97908939988288,10.9769983398712,11.9749072798595,12.9728162198478,
13.6836710227273),.UNSPECIFIED.);
#6585=B_SPLINE_CURVE_WITH_KNOTS('',3,(#256233,#256234,#256235,#256236,#256237,
#256238,#256239,#256240,#256241,#256242,#256243,#256244,#256245,#256246,
#256247,#256248,#256249,#256250,#256251,#256252,#256253,#256254),
 .UNSPECIFIED.,.F.,.F.,(4,3,3,3,3,3,3,4),(-22.9424863416694,-21.9539966797423,
-20.956087739754,-19.9581787997658,-18.9602698597775,-17.9623609197892,
-16.9644519798009,-16.6593010344898),.UNSPECIFIED.);
#6586=B_SPLINE_CURVE_WITH_KNOTS('',3,(#256255,#256256,#256257,#256258,#256259,
#256260,#256261,#256262,#256263,#256264,#256265,#256266,#256267,#256268,
#256269,#256270,#256271,#256272,#256273,#256274,#256275,#256276,#256277,
#256278,#256279),.UNSPECIFIED.,.F.,.F.,(4,3,3,3,3,3,3,3,4),(13.6836710227273,
13.970725159836,14.9686340998243,15.9665430398126,16.9644519798009,17.9623609197892,
18.9602698597775,19.9581787997658,19.9668563299069),.UNSPECIFIED.);
#6587=B_SPLINE_CURVE_WITH_KNOTS('',3,(#256284,#256285,#256286,#256287,#256288,
#256289,#256290,#256291,#256292,#256293,#256294,#256295,#256296,#256297,
#256298,#256299,#256300,#256301,#256302,#256303,#256304,#256305,#256306,
#256307,#256308),.UNSPECIFIED.,.F.,.F.,(4,3,3,3,3,3,3,3,4),(-29.225671648849,
-28.9393592596604,-27.9414503196721,-26.9435413796838,-25.9456324396955,
-24.9477234997072,-23.9498145597189,-22.9519056197306,-22.9424863416694),
 .UNSPECIFIED.);
#6588=B_SPLINE_CURVE_WITH_KNOTS('',3,(#256309,#256310,#256311,#256312,#256313,
#256314,#256315,#256316,#256317,#256318,#256319,#256320,#256321,#256322,
#256323,#256324,#256325,#256326,#256327,#256328,#256329,#256330),
 .UNSPECIFIED.,.F.,.F.,(4,3,3,3,3,3,3,4),(19.9668563299069,20.9560877397541,
21.9539966797423,22.9519056197306,23.9498145597189,24.9477234997072,25.9456324396955,
26.2500416370865),.UNSPECIFIED.);
#6589=B_SPLINE_CURVE_WITH_KNOTS('',3,(#256335,#256336,#256337,#256338,#256339,
#256340,#256341,#256342,#256343,#256344,#256345,#256346,#256347,#256348,
#256349,#256350,#256351,#256352,#256353,#256354,#256355,#256356),
 .UNSPECIFIED.,.F.,.F.,(4,3,3,3,3,3,3,4),(-35.5088569560286,-34.9268128995901,
-33.9289039596018,-32.9309950196135,-31.9330860796252,-30.9351771396369,
-29.9372681996486,-29.225671648849),.UNSPECIFIED.);
#6590=B_SPLINE_CURVE_WITH_KNOTS('',3,(#256357,#256358,#256359,#256360,#256361,
#256362,#256363,#256364,#256365,#256366,#256367,#256368,#256369,#256370,
#256371,#256372,#256373,#256374,#256375,#256376,#256377,#256378),
 .UNSPECIFIED.,.F.,.F.,(4,3,3,3,3,3,3,4),(26.2500416370865,26.9435413796838,
27.9414503196721,28.9393592596604,29.9372681996487,30.9351771396369,31.9330860796252,
32.5332269442661),.UNSPECIFIED.);
#6591=B_SPLINE_CURVE_WITH_KNOTS('',3,(#256383,#256384,#256385,#256386,#256387,
#256388,#256389,#256390,#256391,#256392,#256393,#256394,#256395,#256396,
#256397,#256398,#256399,#256400,#256401,#256402,#256403,#256404),
 .UNSPECIFIED.,.F.,.F.,(4,3,3,3,3,3,3,4),(-41.7920422632082,-40.9142665395198,
-39.9163575995315,-38.9184486595432,-37.9205397195549,-36.9226307795667,
-35.9247218395784,-35.5088569560286),.UNSPECIFIED.);
#6592=B_SPLINE_CURVE_WITH_KNOTS('',3,(#256405,#256406,#256407,#256408,#256409,
#256410,#256411,#256412,#256413,#256414,#256415,#256416,#256417,#256418,
#256419,#256420,#256421,#256422,#256423,#256424,#256425,#256426),
 .UNSPECIFIED.,.F.,.F.,(4,3,3,3,3,3,3,4),(32.5332269442661,32.9309950196135,
33.9289039596018,34.9268128995901,35.9247218395784,36.9226307795667,37.9205397195549,
38.8164122514457),.UNSPECIFIED.);
#6593=B_SPLINE_CURVE_WITH_KNOTS('',3,(#256431,#256432,#256433,#256434,#256435,
#256436,#256437,#256438,#256439,#256440,#256441,#256442,#256443,#256444,
#256445,#256446,#256447,#256448,#256449,#256450,#256451,#256452,#256453,
#256454,#256455),.UNSPECIFIED.,.F.,.F.,(4,3,3,3,3,3,3,3,4),(-48.0752275703878,
-47.8996291194378,-46.9017201794495,-45.9038112394613,-44.905902299473,
-43.9079933594847,-42.9100844194964,-41.9121754795081,-41.7920422632082),
 .UNSPECIFIED.);
#6594=B_SPLINE_CURVE_WITH_KNOTS('',3,(#256456,#256457,#256458,#256459,#256460,
#256461,#256462,#256463,#256464,#256465,#256466,#256467,#256468,#256469,
#256470,#256471,#256472,#256473,#256474,#256475,#256476,#256477,#256478,
#256479,#256480),.UNSPECIFIED.,.F.,.F.,(4,3,3,3,3,3,3,3,4),(38.8164122514457,
38.9184486595432,39.9163575995315,40.9142665395198,41.9121754795081,42.9100844194964,
43.9079933594847,44.905902299473,45.0995975586253),.UNSPECIFIED.);
#6595=B_SPLINE_CURVE_WITH_KNOTS('',3,(#256485,#256486,#256487,#256488,#256489,
#256490,#256491,#256492,#256493,#256494,#256495,#256496,#256497,#256498,
#256499,#256500,#256501,#256502,#256503,#256504,#256505,#256506),
 .UNSPECIFIED.,.F.,.F.,(4,3,3,3,3,3,3,4),(-54.3584128775674,-53.8870827593676,
-52.8891738193793,-51.891264879391,-50.8933559394027,-49.8954469994144,
-48.8975380594261,-48.0752275703878),.UNSPECIFIED.);
#6596=B_SPLINE_CURVE_WITH_KNOTS('',3,(#256507,#256508,#256509,#256510,#256511,
#256512,#256513,#256514,#256515,#256516,#256517,#256518,#256519,#256520,
#256521,#256522,#256523,#256524,#256525,#256526,#256527,#256528),
 .UNSPECIFIED.,.F.,.F.,(4,3,3,3,3,3,3,4),(45.0995975586253,45.9038112394613,
46.9017201794496,47.8996291194378,48.8975380594261,49.8954469994144,50.8933559394027,
51.3827828658049),.UNSPECIFIED.);
#6597=B_SPLINE_CURVE_WITH_KNOTS('',3,(#256533,#256534,#256535,#256536,#256537,
#256538,#256539,#256540,#256541,#256542,#256543,#256544,#256545,#256546,
#256547,#256548,#256549,#256550,#256551,#256552,#256553,#256554),
 .UNSPECIFIED.,.F.,.F.,(4,3,3,3,3,3,3,4),(-60.641598184747,-59.8745363992973,
-58.876627459309,-57.8787185193207,-56.8808095793324,-55.8829006393441,
-54.8849916993559,-54.3584128775674),.UNSPECIFIED.);
#6598=B_SPLINE_CURVE_WITH_KNOTS('',3,(#256555,#256556,#256557,#256558,#256559,
#256560,#256561,#256562,#256563,#256564,#256565,#256566,#256567,#256568,
#256569,#256570,#256571,#256572,#256573,#256574,#256575,#256576),
 .UNSPECIFIED.,.F.,.F.,(4,3,3,3,3,3,3,4),(51.3827828658049,51.891264879391,
52.8891738193793,53.8870827593676,54.8849916993559,55.8829006393442,56.8808095793325,
57.6659681729845),.UNSPECIFIED.);
#6599=B_SPLINE_CURVE_WITH_KNOTS('',3,(#256581,#256582,#256583,#256584,#256585,
#256586,#256587,#256588,#256589,#256590,#256591,#256592,#256593,#256594,
#256595,#256596,#256597,#256598,#256599,#256600,#256601,#256602,#256603,
#256604,#256605),.UNSPECIFIED.,.F.,.F.,(4,3,3,3,3,3,3,3,4),(-66.9247834919266,
-66.8598989792153,-65.861990039227,-64.8640810992387,-63.8661721592505,
-62.8682632192622,-61.8703542792739,-60.8724453392856,-60.641598184747),
 .UNSPECIFIED.);
#6600=B_SPLINE_CURVE_WITH_KNOTS('',3,(#256606,#256607,#256608,#256609,#256610,
#256611,#256612,#256613,#256614,#256615,#256616,#256617,#256618,#256619,
#256620,#256621,#256622,#256623,#256624,#256625,#256626,#256627,#256628,
#256629,#256630),.UNSPECIFIED.,.F.,.F.,(4,3,3,3,3,3,3,3,4),(57.6659681729845,
57.8787185193207,58.876627459309,59.8745363992973,60.8724453392856,61.8703542792739,
62.8682632192622,63.8661721592505,63.949153480164),.UNSPECIFIED.);
#6601=B_SPLINE_CURVE_WITH_KNOTS('',3,(#256635,#256636,#256637,#256638,#256639,
#256640,#256641,#256642,#256643,#256644,#256645,#256646,#256647,#256648,
#256649,#256650,#256651,#256652,#256653,#256654,#256655,#256656),
 .UNSPECIFIED.,.F.,.F.,(4,3,3,3,3,3,3,4),(-73.2079687991062,-72.847352619145,
-71.8494436791567,-70.8515347391685,-69.8536257991802,-68.8557168591919,
-67.8578079192036,-66.9247834919266),.UNSPECIFIED.);
#6602=B_SPLINE_CURVE_WITH_KNOTS('',3,(#256657,#256658,#256659,#256660,#256661,
#256662,#256663,#256664,#256665,#256666,#256667,#256668,#256669,#256670,
#256671,#256672,#256673,#256674,#256675,#256676,#256677,#256678),
 .UNSPECIFIED.,.F.,.F.,(4,3,3,3,3,3,3,4),(63.949153480164,64.8640810992388,
65.8619900392271,66.8598989792153,67.8578079192036,68.8557168591919,69.8536257991802,
70.2323387873436),.UNSPECIFIED.);
#6603=B_SPLINE_CURVE_WITH_KNOTS('',3,(#256683,#256684,#256685,#256686,#256687,
#256688,#256689,#256690,#256691,#256692,#256693,#256694,#256695,#256696,
#256697,#256698,#256699,#256700,#256701,#256702,#256703,#256704),
 .UNSPECIFIED.,.F.,.F.,(4,3,3,3,3,3,3,4),(-79.4911541062857,-78.8348062590748,
-77.8368973190865,-76.8389883790982,-75.8410794391099,-74.8431704991216,
-73.8452615591333,-73.2079687991062),.UNSPECIFIED.);
#6604=B_SPLINE_CURVE_WITH_KNOTS('',3,(#256705,#256706,#256707,#256708,#256709,
#256710,#256711,#256712,#256713,#256714,#256715,#256716,#256717,#256718,
#256719,#256720,#256721,#256722,#256723,#256724,#256725,#256726),
 .UNSPECIFIED.,.F.,.F.,(4,3,3,3,3,3,3,4),(70.2323387873436,70.8515347391685,
71.8494436791568,72.8473526191451,73.8452615591333,74.8431704991216,75.8410794391099,
76.5155240945232),.UNSPECIFIED.);
#6605=B_SPLINE_CURVE_WITH_KNOTS('',3,(#256731,#256732,#256733,#256734,#256735,
#256736,#256737,#256738,#256739,#256740,#256741,#256742,#256743,#256744,
#256745,#256746,#256747,#256748,#256749,#256750,#256751,#256752),
 .UNSPECIFIED.,.F.,.F.,(4,3,3,3,3,3,3,4),(-85.7743394134653,-84.8222598990045,
-83.8243509590162,-82.8264420190279,-81.8285330790396,-80.8306241390513,
-79.832715199063,-79.4911541062857),.UNSPECIFIED.);
#6606=B_SPLINE_CURVE_WITH_KNOTS('',3,(#256753,#256754,#256755,#256756,#256757,
#256758,#256759,#256760,#256761,#256762,#256763,#256764,#256765,#256766,
#256767,#256768,#256769,#256770,#256771,#256772,#256773,#256774),
 .UNSPECIFIED.,.F.,.F.,(4,3,3,3,3,3,3,4),(76.5155240945232,76.8389883790982,
77.8368973190865,78.8348062590748,79.8327151990631,80.8306241390514,81.8285330790397,
82.7987094017028),.UNSPECIFIED.);
#6607=B_SPLINE_CURVE_WITH_KNOTS('',3,(#256779,#256780,#256781,#256782,#256783,
#256784,#256785,#256786,#256787,#256788,#256789,#256790,#256791,#256792,
#256793,#256794,#256795,#256796,#256797,#256798,#256799,#256800,#256801,
#256802,#256803),.UNSPECIFIED.,.F.,.F.,(4,3,3,3,3,3,3,3,4),(-92.0575247206449,
-91.8076224789225,-90.8097135389342,-89.8118045989459,-88.8138956589576,
-87.8159867189694,-86.8180777789811,-85.8201688389928,-85.7743394134653),
 .UNSPECIFIED.);
#6608=B_SPLINE_CURVE_WITH_KNOTS('',3,(#256804,#256805,#256806,#256807,#256808,
#256809,#256810,#256811,#256812,#256813,#256814,#256815,#256816,#256817,
#256818,#256819,#256820,#256821,#256822,#256823,#256824,#256825,#256826,
#256827,#256828),.UNSPECIFIED.,.F.,.F.,(4,3,3,3,3,3,3,3,4),(82.7987094017028,
82.8264420190279,83.8243509590162,84.8222598990045,85.8201688389928,86.8180777789811,
87.8159867189694,88.8138956589577,89.0818947088824),.UNSPECIFIED.);
#6609=B_SPLINE_CURVE_WITH_KNOTS('',3,(#256833,#256834,#256835,#256836,#256837,
#256838,#256839,#256840,#256841,#256842,#256843,#256844,#256845,#256846,
#256847,#256848,#256849,#256850,#256851,#256852,#256853,#256854),
 .UNSPECIFIED.,.F.,.F.,(4,3,3,3,3,3,3,4),(-98.3407100278245,-97.7950761188523,
-96.7971671788639,-95.7992582388757,-94.8013492988874,-93.8034403588991,
-92.8055314189108,-92.0575247206449),.UNSPECIFIED.);
#6610=B_SPLINE_CURVE_WITH_KNOTS('',3,(#256855,#256856,#256857,#256858,#256859,
#256860,#256861,#256862,#256863,#256864,#256865,#256866,#256867,#256868,
#256869,#256870,#256871,#256872,#256873,#256874,#256875,#256876),
 .UNSPECIFIED.,.F.,.F.,(4,3,3,3,3,3,3,4),(89.0818947088824,89.811804598946,
90.8097135389343,91.8076224789226,92.8055314189108,93.8034403588991,94.8013492988874,
95.365080016062),.UNSPECIFIED.);
#6611=B_SPLINE_CURVE_WITH_KNOTS('',3,(#256881,#256882,#256883,#256884,#256885,
#256886,#256887,#256888,#256889,#256890,#256891,#256892,#256893,#256894,
#256895,#256896,#256897,#256898,#256899,#256900,#256901,#256902),
 .UNSPECIFIED.,.F.,.F.,(4,3,3,3,3,3,3,4),(-104.623895335004,-103.782529758782,
-102.784620818794,-101.786711878805,-100.788802938817,-99.7908939988288,
-98.7929850588405,-98.3407100278245),.UNSPECIFIED.);
#6612=B_SPLINE_CURVE_WITH_KNOTS('',3,(#256903,#256904,#256905,#256906,#256907,
#256908,#256909,#256910,#256911,#256912,#256913,#256914,#256915,#256916,
#256917,#256918,#256919,#256920,#256921,#256922,#256923,#256924),
 .UNSPECIFIED.,.F.,.F.,(4,3,3,3,3,3,3,4),(95.365080016062,95.7992582388757,
96.797167178864,97.7950761188523,98.7929850588406,99.7908939988288,100.788802938817,
101.648265323242),.UNSPECIFIED.);
#6613=B_SPLINE_CURVE_WITH_KNOTS('',3,(#256929,#256930,#256931,#256932,#256933,
#256934,#256935,#256936,#256937,#256938,#256939,#256940,#256941,#256942,
#256943,#256944,#256945,#256946,#256947,#256948,#256949,#256950,#256951,
#256952,#256953),.UNSPECIFIED.,.F.,.F.,(4,3,3,3,3,3,3,3,4),(-110.907080642184,
-110.7678923387,-109.769983398712,-108.772074458723,-107.774165518735,-106.776256578747,
-105.778347638759,-104.78043869877,-104.623895335004),.UNSPECIFIED.);
#6614=B_SPLINE_CURVE_WITH_KNOTS('',3,(#256954,#256955,#256956,#256957,#256958,
#256959,#256960,#256961,#256962,#256963,#256964,#256965,#256966,#256967,
#256968,#256969,#256970,#256971,#256972,#256973,#256974,#256975,#256976,
#256977,#256978),.UNSPECIFIED.,.F.,.F.,(4,3,3,3,3,3,3,3,4),(101.648265323242,
101.786711878805,102.784620818794,103.782529758782,104.78043869877,105.778347638759,
106.776256578747,107.774165518735,107.931450630421),.UNSPECIFIED.);
#6615=B_SPLINE_CURVE_WITH_KNOTS('',3,(#256983,#256984,#256985,#256986,#256987,
#256988,#256989,#256990,#256991,#256992,#256993,#256994,#256995,#256996,
#256997,#256998,#256999,#257000,#257001,#257002,#257003,#257004),
 .UNSPECIFIED.,.F.,.F.,(4,3,3,3,3,3,3,4),(-117.190265949363,-116.75534597863,
-115.757437038641,-114.759528098653,-113.761619158665,-112.763710218677,
-111.765801278688,-110.907080642184),.UNSPECIFIED.);
#6616=B_SPLINE_CURVE_WITH_KNOTS('',3,(#257005,#257006,#257007,#257008,#257009,
#257010,#257011,#257012,#257013,#257014,#257015,#257016,#257017,#257018,
#257019,#257020,#257021,#257022,#257023,#257024,#257025,#257026),
 .UNSPECIFIED.,.F.,.F.,(4,3,3,3,3,3,3,4),(107.931450630421,108.772074458723,
109.769983398712,110.7678923387,111.765801278688,112.763710218677,113.761619158665,
114.214635937601),.UNSPECIFIED.);
#6617=B_SPLINE_CURVE_WITH_KNOTS('',3,(#257031,#257032,#257033,#257034,#257035,
#257036,#257037,#257038,#257039,#257040,#257041,#257042,#257043,#257044,
#257045,#257046,#257047,#257048,#257049,#257050,#257051,#257052),
 .UNSPECIFIED.,.F.,.F.,(4,3,3,3,3,3,3,4),(-123.473451256543,-122.742799618559,
-121.744890678571,-120.746981738583,-119.749072798595,-118.751163858606,
-117.753254918618,-117.190265949363),.UNSPECIFIED.);
#6618=B_SPLINE_CURVE_WITH_KNOTS('',3,(#257053,#257054,#257055,#257056,#257057,
#257058,#257059,#257060,#257061,#257062,#257063,#257064,#257065,#257066,
#257067,#257068,#257069,#257070,#257071,#257072,#257073,#257074),
 .UNSPECIFIED.,.F.,.F.,(4,3,3,3,3,3,3,4),(114.214635937601,114.759528098653,
115.757437038641,116.75534597863,117.753254918618,118.751163858606,119.749072798595,
120.49782124478),.UNSPECIFIED.);
#6619=B_SPLINE_CURVE_WITH_KNOTS('',3,(#257080,#257081,#257082,#257083,#257084,
#257085),.UNSPECIFIED.,.F.,.F.,(4,1,1,4),(135.088484104361,135.355741406366,
136.353650346354,137.27873899141),.UNSPECIFIED.);
#6620=B_SPLINE_CURVE_WITH_KNOTS('',3,(#257088,#257089,#257090,#257091),
 .UNSPECIFIED.,.F.,.F.,(4,4),(135.088484104361,136.039821870902),
 .UNSPECIFIED.);
#6621=B_SPLINE_CURVE_WITH_KNOTS('',3,(#257096,#257097,#257098,#257099,#257100,
#257101,#257102,#257103,#257104,#257105),.UNSPECIFIED.,.F.,.F.,(4,1,1,1,
1,1,1,4),(128.805298797182,129.368287766436,130.366196706425,131.364105646413,
132.362014586401,133.359923526389,134.357832466378,135.088484104361),
 .UNSPECIFIED.);
#6622=B_SPLINE_CURVE_WITH_KNOTS('',3,(#257106,#257107,#257108,#257109,#257110,
#257111,#257112,#257113,#257114,#257115,#257116),.UNSPECIFIED.,.F.,.F.,
(4,1,1,1,1,1,1,1,4),(128.805298797182,129.054459290984,130.052368230972,
131.05027717096,132.048186110949,133.046095050937,134.044003990925,135.041912930914,
135.088484104361),.UNSPECIFIED.);
#6623=B_SPLINE_CURVE_WITH_KNOTS('',3,(#257121,#257122,#257123,#257124,#257125,
#257126,#257127,#257128,#257129,#257130),.UNSPECIFIED.,.F.,.F.,(4,1,1,1,
1,1,1,4),(122.522113490002,123.380834126507,124.378743066495,125.376652006483,
126.374560946471,127.37246988646,128.370378826448,128.805298797182),
 .UNSPECIFIED.);
#6624=B_SPLINE_CURVE_WITH_KNOTS('',3,(#257131,#257132,#257133,#257134,#257135,
#257136,#257137,#257138,#257139,#257140),.UNSPECIFIED.,.F.,.F.,(4,1,1,1,
1,1,1,4),(122.522113490002,123.067005651054,124.064914591042,125.062823531031,
126.060732471019,127.058641411007,128.056550350996,128.805298797182),
 .UNSPECIFIED.);
#6625=B_SPLINE_CURVE_WITH_KNOTS('',3,(#257145,#257146,#257147,#257148,#257149,
#257150,#257151,#257152,#257153,#257154,#257155),.UNSPECIFIED.,.F.,.F.,
(4,1,1,1,1,1,1,1,4),(116.238928182822,116.395471546589,117.393380486577,
118.391289426565,119.389198366553,120.387107306542,121.38501624653,122.382925186518,
122.522113490002),.UNSPECIFIED.);
#6626=B_SPLINE_CURVE_WITH_KNOTS('',3,(#257156,#257157,#257158,#257159,#257160,
#257161,#257162,#257163,#257164,#257165),.UNSPECIFIED.,.F.,.F.,(4,1,1,1,
1,1,1,4),(116.238928182822,117.079552011124,118.077460951113,119.075369891101,
120.073278831089,121.071187771078,122.069096711066,122.522113490002),
 .UNSPECIFIED.);
#6627=B_SPLINE_CURVE_WITH_KNOTS('',3,(#257170,#257171,#257172,#257173,#257174,
#257175,#257176,#257177,#257178,#257179),.UNSPECIFIED.,.F.,.F.,(4,1,1,1,
1,1,1,4),(109.955742875643,110.408017906659,111.405926846647,112.403835786635,
113.401744726624,114.399653666612,115.3975626066,116.238928182822),
 .UNSPECIFIED.);
#6628=B_SPLINE_CURVE_WITH_KNOTS('',3,(#257180,#257181,#257182,#257183,#257184,
#257185,#257186,#257187,#257188,#257189,#257190),.UNSPECIFIED.,.F.,.F.,
(4,1,1,1,1,1,1,1,4),(109.955742875643,110.094189431206,111.092098371195,
112.090007311183,113.087916251171,114.08582519116,115.083734131148,116.081643071136,
116.238928182822),.UNSPECIFIED.);
#6629=B_SPLINE_CURVE_WITH_KNOTS('',3,(#257195,#257196,#257197,#257198,#257199,
#257200,#257201,#257202,#257203,#257204),.UNSPECIFIED.,.F.,.F.,(4,1,1,1,
1,1,1,4),(103.672557568463,104.420564266729,105.418473206717,106.416382146706,
107.414291086694,108.412200026682,109.41010896667,109.955742875643),
 .UNSPECIFIED.);
#6630=B_SPLINE_CURVE_WITH_KNOTS('',3,(#257205,#257206,#257207,#257208,#257209,
#257210,#257211,#257212,#257213,#257214),.UNSPECIFIED.,.F.,.F.,(4,1,1,1,
1,1,1,4),(103.672557568463,104.106735791277,105.104644731265,106.102553671253,
107.100462611242,108.09837155123,109.096280491218,109.955742875643),
 .UNSPECIFIED.);
#6631=B_SPLINE_CURVE_WITH_KNOTS('',3,(#257219,#257220,#257221,#257222,#257223,
#257224,#257225,#257226,#257227,#257228,#257229),.UNSPECIFIED.,.F.,.F.,
(4,1,1,1,1,1,1,1,4),(97.3893722612836,97.435201686811,98.4331106267993,
99.4310195667876,100.428928506776,101.426837446764,102.424746386752,103.422655326741,
103.672557568463),.UNSPECIFIED.);
#6632=B_SPLINE_CURVE_WITH_KNOTS('',3,(#257230,#257231,#257232,#257233,#257234,
#257235,#257236,#257237,#257238,#257239),.UNSPECIFIED.,.F.,.F.,(4,1,1,1,
1,1,1,4),(97.3893722612836,98.119282151347,99.1171910913353,100.115100031324,
101.113008971312,102.1109179113,103.108826851288,103.672557568463),
 .UNSPECIFIED.);
#6633=B_SPLINE_CURVE_WITH_KNOTS('',3,(#257244,#257245,#257246,#257247,#257248,
#257249,#257250,#257251,#257252,#257253),.UNSPECIFIED.,.F.,.F.,(4,1,1,1,
1,1,1,4),(91.106186954104,91.4477480468813,92.4456569868696,93.4435659268579,
94.4414748668462,95.4393838068345,96.4372927468227,97.3893722612836),
 .UNSPECIFIED.);
#6634=B_SPLINE_CURVE_WITH_KNOTS('',3,(#257254,#257255,#257256,#257257,#257258,
#257259,#257260,#257261,#257262,#257263,#257264),.UNSPECIFIED.,.F.,.F.,
(4,1,1,1,1,1,1,1,4),(91.106186954104,91.133919571429,92.1318285114173,93.1297374514056,
94.1276463913938,95.1255553313821,96.1234642713704,97.1213732113587,97.3893722612836),
 .UNSPECIFIED.);
#6635=B_SPLINE_CURVE_WITH_KNOTS('',3,(#257269,#257270,#257271,#257272,#257273,
#257274,#257275,#257276,#257277,#257278),.UNSPECIFIED.,.F.,.F.,(4,1,1,1,
1,1,1,4),(84.8230016469244,85.4602944069516,86.4582033469399,87.4561122869281,
88.4540212269164,89.4519301669047,90.449839106893,91.106186954104),
 .UNSPECIFIED.);
#6636=B_SPLINE_CURVE_WITH_KNOTS('',3,(#257279,#257280,#257281,#257282,#257283,
#257284,#257285,#257286,#257287,#257288),.UNSPECIFIED.,.F.,.F.,(4,1,1,1,
1,1,1,4),(84.8230016469244,85.1464659314993,86.1443748714875,87.1422838114758,
88.1401927514641,89.1381016914524,90.1360106314407,91.106186954104),
 .UNSPECIFIED.);
#6637=B_SPLINE_CURVE_WITH_KNOTS('',3,(#257293,#257294,#257295,#257296,#257297,
#257298,#257299,#257300,#257301,#257302),.UNSPECIFIED.,.F.,.F.,(4,1,1,1,
1,1,1,4),(78.5398163397448,79.4728407670218,80.4707497070101,81.4686586469984,
82.4665675869867,83.464476526975,84.4623854669633,84.8230016469244),
 .UNSPECIFIED.);
#6638=B_SPLINE_CURVE_WITH_KNOTS('',3,(#257303,#257304,#257305,#257306,#257307,
#257308,#257309,#257310,#257311,#257312),.UNSPECIFIED.,.F.,.F.,(4,1,1,1,
1,1,1,4),(78.5398163397448,79.1590122915695,80.1569212315578,81.1548301715461,
82.1527391115344,83.1506480515227,84.148556991511,84.8230016469244),
 .UNSPECIFIED.);
#6639=B_SPLINE_CURVE_WITH_KNOTS('',3,(#257317,#257318,#257319,#257320,#257321,
#257322,#257323,#257324,#257325,#257326,#257327),.UNSPECIFIED.,.F.,.F.,
(4,1,1,1,1,1,1,1,4),(72.2566310325652,72.4874781871038,73.4853871270921,
74.4832960670804,75.4812050070687,76.479113947057,77.4770228870453,78.4749318270335,
78.5398163397448),.UNSPECIFIED.);
#6640=B_SPLINE_CURVE_WITH_KNOTS('',3,(#257328,#257329,#257330,#257331,#257332,
#257333,#257334,#257335,#257336,#257337),.UNSPECIFIED.,.F.,.F.,(4,1,1,1,
1,1,1,4),(72.2566310325652,73.1715586516398,74.1694675916281,75.1673765316164,
76.1652854716046,77.1631944115929,78.1611033515812,78.5398163397448),
 .UNSPECIFIED.);
#6641=B_SPLINE_CURVE_WITH_KNOTS('',3,(#257342,#257343,#257344,#257345,#257346,
#257347,#257348,#257349,#257350,#257351),.UNSPECIFIED.,.F.,.F.,(4,1,1,1,
1,1,1,4),(65.9734457253856,66.5000245471741,67.4979334871624,68.4958424271507,
69.493751367139,70.4916603071272,71.4895692471155,72.2566310325652),
 .UNSPECIFIED.);
#6642=B_SPLINE_CURVE_WITH_KNOTS('',3,(#257352,#257353,#257354,#257355,#257356,
#257357,#257358,#257359,#257360,#257361,#257362),.UNSPECIFIED.,.F.,.F.,
(4,1,1,1,1,1,1,1,4),(65.9734457253856,66.1861960717218,67.1841050117101,
68.1820139516983,69.1799228916866,70.1778318316749,71.1757407716632,72.1736497116515,
72.2566310325652),.UNSPECIFIED.);
#6643=B_SPLINE_CURVE_WITH_KNOTS('',3,(#257367,#257368,#257369,#257370,#257371,
#257372,#257373,#257374,#257375,#257376),.UNSPECIFIED.,.F.,.F.,(4,1,1,1,
1,1,1,4),(59.690260418206,60.5125709072444,61.5104798472327,62.5083887872209,
63.5062977272092,64.5042066671975,65.5021156071858,65.9734457253856),
 .UNSPECIFIED.);
#6644=B_SPLINE_CURVE_WITH_KNOTS('',3,(#257377,#257378,#257379,#257380,#257381,
#257382,#257383,#257384,#257385,#257386),.UNSPECIFIED.,.F.,.F.,(4,1,1,1,
1,1,1,4),(59.690260418206,60.198742431792,61.1966513717803,62.1945603117686,
63.1924692517569,64.1903781917452,65.1882871317335,65.9734457253856),
 .UNSPECIFIED.);
#6645=B_SPLINE_CURVE_WITH_KNOTS('',3,(#257391,#257392,#257393,#257394,#257395,
#257396,#257397,#257398,#257399,#257400,#257401),.UNSPECIFIED.,.F.,.F.,
(4,1,1,1,1,1,1,1,4),(53.4070751110264,53.5272083273263,54.5251172673146,
55.5230262073029,56.5209351472912,57.5188440872795,58.5167530272678,59.5146619672561,
59.690260418206),.UNSPECIFIED.);
#6646=B_SPLINE_CURVE_WITH_KNOTS('',3,(#257402,#257403,#257404,#257405,#257406,
#257407,#257408,#257409,#257410,#257411),.UNSPECIFIED.,.F.,.F.,(4,1,1,1,
1,1,1,4),(53.4070751110264,54.2112887918623,55.2091977318506,56.2071066718389,
57.2050156118272,58.2029245518155,59.2008334918037,59.690260418206),
 .UNSPECIFIED.);
#6647=B_SPLINE_CURVE_WITH_KNOTS('',3,(#257416,#257417,#257418,#257419,#257420,
#257421,#257422,#257423,#257424,#257425),.UNSPECIFIED.,.F.,.F.,(4,1,1,1,
1,1,1,4),(47.1238898038468,47.5397546873966,48.5376636273849,49.5355725673732,
50.5334815073615,51.5313904473498,52.5292993873381,53.4070751110264),
 .UNSPECIFIED.);
#6648=B_SPLINE_CURVE_WITH_KNOTS('',3,(#257426,#257427,#257428,#257429,#257430,
#257431,#257432,#257433,#257434,#257435,#257436),.UNSPECIFIED.,.F.,.F.,
(4,1,1,1,1,1,1,1,4),(47.1238898038468,47.2259262119443,48.2238351519326,
49.2217440919209,50.2196530319092,51.2175619718974,52.2154709118857,53.213379851874,
53.4070751110264),.UNSPECIFIED.);
#6649=B_SPLINE_CURVE_WITH_KNOTS('',3,(#257441,#257442,#257443,#257444,#257445,
#257446,#257447,#257448,#257449,#257450),.UNSPECIFIED.,.F.,.F.,(4,1,1,1,
1,1,1,4),(40.8407044966673,41.5523010474669,42.5502099874552,43.5481189274435,
44.5460278674318,45.54393680742,46.5418457474083,47.1238898038468),
 .UNSPECIFIED.);
#6650=B_SPLINE_CURVE_WITH_KNOTS('',3,(#257451,#257452,#257453,#257454,#257455,
#257456,#257457,#257458,#257459,#257460),.UNSPECIFIED.,.F.,.F.,(4,1,1,1,
1,1,1,4),(40.8407044966672,41.2384725720146,42.2363815120028,43.2342904519911,
44.2321993919794,45.2301083319677,46.228017271956,47.1238898038468),
 .UNSPECIFIED.);
#6651=B_SPLINE_CURVE_WITH_KNOTS('',3,(#257465,#257466,#257467,#257468,#257469,
#257470,#257471,#257472,#257473,#257474,#257475),.UNSPECIFIED.,.F.,.F.,
(4,1,1,1,1,1,1,1,4),(34.5575191894877,34.5669384675489,35.5648474075372,
36.5627563475255,37.5606652875137,38.558574227502,39.5564831674903,40.5543921074786,
40.8407044966673),.UNSPECIFIED.);
#6652=B_SPLINE_CURVE_WITH_KNOTS('',3,(#257476,#257477,#257478,#257479,#257480,
#257481,#257482,#257483,#257484,#257485),.UNSPECIFIED.,.F.,.F.,(4,1,1,1,
1,1,1,4),(34.5575191894876,35.2510189320848,36.2489278720731,37.2468368120614,
38.2447457520497,39.242654692038,40.2405636320263,40.8407044966672),
 .UNSPECIFIED.);
#6653=B_SPLINE_CURVE_WITH_KNOTS('',3,(#257490,#257491,#257492,#257493,#257494,
#257495,#257496,#257497,#257498,#257499),.UNSPECIFIED.,.F.,.F.,(4,1,1,1,
1,1,1,4),(28.2743338823081,28.5794848276191,29.5773937676074,30.5753027075957,
31.573211647584,32.5711205875723,33.5690295275606,34.5575191894877),
 .UNSPECIFIED.);
#6654=B_SPLINE_CURVE_WITH_KNOTS('',3,(#257500,#257501,#257502,#257503,#257504,
#257505,#257506,#257507,#257508,#257509),.UNSPECIFIED.,.F.,.F.,(4,1,1,1,
1,1,1,4),(28.274333882308,29.2635652921551,30.2614742321434,31.2593831721317,
32.25729211212,33.2552010521082,34.2531099920965,34.5575191894876),
 .UNSPECIFIED.);
#6655=B_SPLINE_CURVE_WITH_KNOTS('',3,(#257514,#257515,#257516,#257517,#257518,
#257519,#257520,#257521,#257522,#257523),.UNSPECIFIED.,.F.,.F.,(4,1,1,1,
1,1,1,4),(21.9911485751285,22.5920311876894,23.5899401276777,24.587849067666,
25.5857580076543,26.5836669476426,27.5815758876309,28.2743338823081),
 .UNSPECIFIED.);
#6656=B_SPLINE_CURVE_WITH_KNOTS('',3,(#257524,#257525,#257526,#257527,#257528,
#257529,#257530,#257531,#257532,#257533,#257534),.UNSPECIFIED.,.F.,.F.,
(4,1,1,1,1,1,1,1,4),(21.9911485751285,22.2782027122371,23.2761116522254,
24.2740205922137,25.2719295322019,26.2698384721902,27.2677474121785,28.2656563521668,
28.274333882308),.UNSPECIFIED.);
#6657=B_SPLINE_CURVE_WITH_KNOTS('',3,(#257539,#257540,#257541,#257542,#257543,
#257544,#257545,#257546,#257547,#257548),.UNSPECIFIED.,.F.,.F.,(4,1,1,1,
1,1,1,4),(15.7079632679489,16.6045775477597,17.602486487748,18.6003954277363,
19.5983043677246,20.5962133077128,21.5941222477011,21.9911485751285),
 .UNSPECIFIED.);
#6658=B_SPLINE_CURVE_WITH_KNOTS('',3,(#257549,#257550,#257551,#257552,#257553,
#257554,#257555,#257556,#257557,#257558),.UNSPECIFIED.,.F.,.F.,(4,1,1,1,
1,1,1,4),(15.7079632679489,16.2907490723073,17.2886580122956,18.2865669522839,
19.2844758922722,20.2823848322605,21.2802937722488,21.9911485751285),
 .UNSPECIFIED.);
#6659=B_SPLINE_CURVE_WITH_KNOTS('',3,(#258084,#258085,#258086,#258087,#258088,
#258089,#258090,#258091,#258092,#258093,#258094,#258095,#258096,#258097,
#258098,#258099,#258100,#258101,#258102,#258103,#258104,#258105,#258106,
#258107,#258108,#258109,#258110,#258111,#258112,#258113,#258114,#258115,
#258116,#258117,#258118,#258119,#258120,#258121,#258122,#258123,#258124,
#258125,#258126,#258127,#258128,#258129,#258130,#258131,#258132,#258133,
#258134,#258135,#258136,#258137,#258138,#258139,#258140,#258141,#258142,
#258143,#258144,#258145,#258146,#258147,#258148,#258149,#258150,#258151,
#258152,#258153,#258154,#258155,#258156,#258157,#258158,#258159,#258160,
#258161,#258162,#258163,#258164,#258165,#258166,#258167,#258168,#258169,
#258170,#258171,#258172,#258173,#258174,#258175,#258176,#258177),
 .UNSPECIFIED.,.F.,.F.,(4,3,3,3,3,3,3,3,3,3,3,3,3,3,3,3,3,3,3,3,3,3,3,3,
3,3,3,3,3,3,3,4),(0.,0.0214813781660272,0.0505838925157975,0.0801385137508181,
0.107869705803836,0.112249638361506,0.116543512167008,0.145302650472993,
0.173939300969273,0.202061984063935,0.214552742327813,0.219720566839256,
0.223842900337521,0.251414063494629,0.278198363192956,0.301988050174959,
0.317818346313982,0.324029978565244,0.32770651927853,0.354360364834322,
0.381465816558906,0.408283310310737,0.418960437375512,0.42405923749684,
0.428492269676655,0.454806508102233,0.479923078176503,0.488621420709103,
0.494617238321095,0.519888501204842,0.544444359268273,0.555272788399315),
 .UNSPECIFIED.);
#6660=B_SPLINE_CURVE_WITH_KNOTS('',3,(#258178,#258179,#258180,#258181,#258182,
#258183,#258184,#258185,#258186,#258187,#258188,#258189,#258190,#258191,
#258192,#258193,#258194,#258195,#258196),.UNSPECIFIED.,.F.,.F.,(4,3,3,3,
3,3,4),(120.49782124478,120.746981738583,121.744890678571,122.742799618559,
123.740708558548,124.738617498536,125.663706143592),.UNSPECIFIED.);
#6661=B_SPLINE_CURVE_WITH_KNOTS('',3,(#258198,#258199,#258200,#258201,#258202,
#258203,#258204,#258205,#258206,#258207,#258208,#258209,#258210,#258211,
#258212,#258213,#258214,#258215,#258216,#258217,#258218,#258219,#258220,
#258221,#258222,#258223,#258224,#258225,#258226,#258227,#258228,#258229,
#258230,#258231,#258232,#258233,#258234,#258235,#258236,#258237,#258238,
#258239,#258240,#258241,#258242,#258243,#258244,#258245,#258246,#258247,
#258248,#258249,#258250,#258251,#258252,#258253,#258254,#258255,#258256,
#258257,#258258,#258259,#258260,#258261,#258262,#258263,#258264,#258265,
#258266,#258267,#258268,#258269,#258270,#258271,#258272,#258273,#258274,
#258275,#258276,#258277,#258278,#258279,#258280,#258281,#258282,#258283,
#258284,#258285,#258286,#258287,#258288),.UNSPECIFIED.,.F.,.F.,(4,3,3,3,
3,3,3,3,3,3,3,3,3,3,3,3,3,3,3,3,3,3,3,3,3,3,3,3,3,3,4),(-0.555272788399385,
-0.537726899847036,-0.513026435229613,-0.498613221691405,-0.492625231873332,
-0.487809143577052,-0.462024881019996,-0.439573648219782,-0.428798046855543,
-0.422005334072263,-0.395415250860688,-0.367165192800086,-0.345977649254635,
-0.330086991595546,-0.325505463211475,-0.320909481568035,-0.29299338650926,
-0.282415018618281,-0.255477639534726,-0.227997281807658,-0.221175758878058,
-0.216725875147774,-0.188767948011568,-0.160274771921768,-0.131545233209308,
-0.114320663149408,-0.109573931193616,-0.0800988261300781,-0.0505532193626863,
-0.0215812432970796,0.),.UNSPECIFIED.);
#6662=B_SPLINE_CURVE_WITH_KNOTS('',3,(#258289,#258290,#258291,#258292,#258293,
#258294,#258295,#258296,#258297),.UNSPECIFIED.,.F.,.F.,(4,1,1,1,1,1,4),
(10.3761157273101,11.3012043723659,12.2991133123542,13.2970222523425,14.2949311923308,
15.2928401323191,15.7079632679489),.UNSPECIFIED.);
#6663=B_SPLINE_CURVE_WITH_KNOTS('',3,(#258301,#258302,#258303,#258304,#258305,
#258306,#258307,#258308),.UNSPECIFIED.,.F.,.F.,(4,1,1,1,1,4),(11.6150328478182,
12.6129417878065,13.6108507277948,14.6087596677831,15.6066686077714,15.7079632679489),
 .UNSPECIFIED.);
#6664=B_SPLINE_CURVE_WITH_KNOTS('',3,(#258834,#258835,#258836,#258837,#258838,
#258839,#258840,#258841,#258842,#258843,#258844,#258845,#258846,#258847,
#258848,#258849,#258850,#258851,#258852,#258853,#258854,#258855,#258856,
#258857,#258858,#258859,#258860,#258861,#258862,#258863,#258864,#258865,
#258866,#258867,#258868,#258869,#258870,#258871,#258872,#258873,#258874,
#258875,#258876,#258877,#258878,#258879,#258880,#258881,#258882,#258883,
#258884,#258885,#258886,#258887,#258888,#258889,#258890,#258891,#258892,
#258893,#258894,#258895,#258896,#258897,#258898,#258899,#258900,#258901,
#258902,#258903,#258904,#258905,#258906,#258907,#258908,#258909,#258910,
#258911,#258912,#258913,#258914,#258915,#258916,#258917,#258918,#258919,
#258920,#258921,#258922,#258923,#258924),.UNSPECIFIED.,.F.,.F.,(4,3,3,3,
3,3,3,3,3,3,3,3,3,3,3,3,3,3,3,3,3,3,3,3,3,3,3,3,3,3,4),(0.,0.0174849238431529,
0.0419332631972337,0.0670144196872723,0.0926255346196509,0.0967052298288898,
0.122652670304572,0.149131552056777,0.175815054013557,0.187861423102457,
0.191997608729776,0.196039596500592,0.22346916945053,0.25081354005042,0.271903339146301,
0.289455966598097,0.293928127619864,0.298389623387338,0.325243438674775,
0.353681181137308,0.378564205792025,0.391569876135391,0.398068460749488,
0.403833210492476,0.432614996310579,0.462647591826694,0.472326582643484,
0.479347066777485,0.508920261877254,0.538120658281837,0.552745378375041),
 .UNSPECIFIED.);
#6665=B_SPLINE_CURVE_WITH_KNOTS('',3,(#258925,#258926,#258927,#258928,#258929,
#258930,#258931,#258932,#258933,#258934,#258935,#258936,#258937,#258938,
#258939,#258940,#258941,#258942,#258943,#258944,#258945,#258946,#258947,
#258948,#258949,#258950,#258951,#258952,#258953,#258954,#258955,#258956,
#258957,#258958,#258959,#258960,#258961,#258962,#258963,#258964,#258965,
#258966,#258967,#258968,#258969,#258970,#258971,#258972,#258973,#258974,
#258975,#258976,#258977,#258978,#258979,#258980,#258981,#258982,#258983,
#258984,#258985,#258986,#258987,#258988,#258989,#258990,#258991,#258992,
#258993,#258994,#258995,#258996,#258997,#258998,#258999,#259000,#259001,
#259002,#259003,#259004,#259005,#259006,#259007,#259008,#259009,#259010,
#259011,#259012,#259013,#259014,#259015,#259016,#259017,#259018),
 .UNSPECIFIED.,.F.,.F.,(4,3,3,3,3,3,3,3,3,3,3,3,3,3,3,3,3,3,3,3,3,3,3,3,
3,3,3,3,3,3,3,4),(-0.552745378375042,-0.531365175220741,-0.50199118119805,
-0.486392955571644,-0.478698871637525,-0.472093120190076,-0.443039610913716,
-0.419212105946447,-0.408417630877946,-0.402068045911971,-0.397493898918164,
-0.369186424191986,-0.339994710937879,-0.31287506792229,-0.297350354313209,
-0.291440280452355,-0.264636789556101,-0.252419571175559,-0.225055087621416,
-0.196923201668739,-0.192596225544785,-0.188249308569056,-0.161608602690815,
-0.135009133177477,-0.108835418443703,-0.0999141223704662,-0.0941324867604078,
-0.0901669524830973,-0.0646229578829025,-0.0394810387994913,-0.0151229871705641,
0.),.UNSPECIFIED.);
#6666=B_SPLINE_CURVE_WITH_KNOTS('',3,(#259019,#259020,#259021,#259022,#259023,
#259024,#259025,#259026,#259027,#259028,#259029,#259030,#259031,#259032,
#259033,#259034),.UNSPECIFIED.,.F.,.F.,(4,3,3,3,3,4),(-127.732344318501,
-126.734435378513,-125.736526438524,-124.738617498536,-123.740708558548,
-123.473451256543),.UNSPECIFIED.);
#7793=LINE('',#256112,#8978);
#7794=LINE('',#256136,#8979);
#7795=LINE('',#256184,#8980);
#7796=LINE('',#256232,#8981);
#7797=LINE('',#256283,#8982);
#7798=LINE('',#256334,#8983);
#7799=LINE('',#256382,#8984);
#7800=LINE('',#256430,#8985);
#7801=LINE('',#256484,#8986);
#7802=LINE('',#256532,#8987);
#7803=LINE('',#256580,#8988);
#7804=LINE('',#256634,#8989);
#7805=LINE('',#256682,#8990);
#7806=LINE('',#256730,#8991);
#7807=LINE('',#256778,#8992);
#7808=LINE('',#256832,#8993);
#7809=LINE('',#256880,#8994);
#7810=LINE('',#256928,#8995);
#7811=LINE('',#256982,#8996);
#7812=LINE('',#257030,#8997);
#7813=LINE('',#257078,#8998);
#7814=LINE('',#257095,#8999);
#7815=LINE('',#257120,#9000);
#7816=LINE('',#257144,#9001);
#7817=LINE('',#257169,#9002);
#7818=LINE('',#257194,#9003);
#7819=LINE('',#257218,#9004);
#7820=LINE('',#257243,#9005);
#7821=LINE('',#257268,#9006);
#7822=LINE('',#257292,#9007);
#7823=LINE('',#257316,#9008);
#7824=LINE('',#257341,#9009);
#7825=LINE('',#257366,#9010);
#7826=LINE('',#257390,#9011);
#7827=LINE('',#257415,#9012);
#7828=LINE('',#257440,#9013);
#7829=LINE('',#257464,#9014);
#7830=LINE('',#257489,#9015);
#7831=LINE('',#257513,#9016);
#7832=LINE('',#257538,#9017);
#7833=LINE('',#259040,#9018);
#7834=LINE('',#259042,#9019);
#7835=LINE('',#259044,#9020);
#7836=LINE('',#259045,#9021);
#7837=LINE('',#259048,#9022);
#7838=LINE('',#259050,#9023);
#7839=LINE('',#259051,#9024);
#7840=LINE('',#259054,#9025);
#7841=LINE('',#259056,#9026);
#7842=LINE('',#259057,#9027);
#7843=LINE('',#259060,#9028);
#7844=LINE('',#259062,#9029);
#7845=LINE('',#259063,#9030);
#7846=LINE('',#259066,#9031);
#7847=LINE('',#259068,#9032);
#7848=LINE('',#259069,#9033);
#7849=LINE('',#259071,#9034);
#7850=LINE('',#259072,#9035);
#7851=LINE('',#259079,#9036);
#8978=VECTOR('',#32034,3.);
#8979=VECTOR('',#32039,3.);
#8980=VECTOR('',#32042,3.);
#8981=VECTOR('',#32045,3.);
#8982=VECTOR('',#32048,3.);
#8983=VECTOR('',#32051,3.);
#8984=VECTOR('',#32054,3.);
#8985=VECTOR('',#32057,3.);
#8986=VECTOR('',#32060,3.);
#8987=VECTOR('',#32063,3.);
#8988=VECTOR('',#32066,3.);
#8989=VECTOR('',#32069,3.);
#8990=VECTOR('',#32072,3.);
#8991=VECTOR('',#32075,3.);
#8992=VECTOR('',#32078,3.);
#8993=VECTOR('',#32081,3.);
#8994=VECTOR('',#32084,3.);
#8995=VECTOR('',#32087,3.);
#8996=VECTOR('',#32090,3.);
#8997=VECTOR('',#32093,3.);
#8998=VECTOR('',#32096,2.37175);
#8999=VECTOR('',#32101,2.37175);
#9000=VECTOR('',#32104,2.37175);
#9001=VECTOR('',#32107,2.37175);
#9002=VECTOR('',#32110,2.37175);
#9003=VECTOR('',#32113,2.37175);
#9004=VECTOR('',#32116,2.37175);
#9005=VECTOR('',#32119,2.37175);
#9006=VECTOR('',#32122,2.37175);
#9007=VECTOR('',#32125,2.37175);
#9008=VECTOR('',#32128,2.37175);
#9009=VECTOR('',#32131,2.37175);
#9010=VECTOR('',#32134,2.37175);
#9011=VECTOR('',#32137,2.37175);
#9012=VECTOR('',#32140,2.37175);
#9013=VECTOR('',#32143,2.37175);
#9014=VECTOR('',#32146,2.37175);
#9015=VECTOR('',#32149,2.37175);
#9016=VECTOR('',#32152,2.37175);
#9017=VECTOR('',#32155,2.37175);
#9018=VECTOR('',#32166,10.);
#9019=VECTOR('',#32167,10.);
#9020=VECTOR('',#32168,10.);
#9021=VECTOR('',#32169,10.);
#9022=VECTOR('',#32172,10.);
#9023=VECTOR('',#32173,10.);
#9024=VECTOR('',#32174,10.);
#9025=VECTOR('',#32177,10.);
#9026=VECTOR('',#32178,10.);
#9027=VECTOR('',#32179,10.);
#9028=VECTOR('',#32182,10.);
#9029=VECTOR('',#32183,10.);
#9030=VECTOR('',#32184,10.);
#9031=VECTOR('',#32187,10.);
#9032=VECTOR('',#32188,10.);
#9033=VECTOR('',#32189,10.);
#9034=VECTOR('',#32192,10.);
#9035=VECTOR('',#32193,10.);
#9036=VECTOR('',#32202,5.);
#11495=VERTEX_POINT('',#256110);
#11496=VERTEX_POINT('',#256111);
#11497=VERTEX_POINT('',#256113);
#11498=VERTEX_POINT('',#256124);
#11499=VERTEX_POINT('',#256134);
#11500=VERTEX_POINT('',#256135);
#11501=VERTEX_POINT('',#256182);
#11502=VERTEX_POINT('',#256183);
#11503=VERTEX_POINT('',#256230);
#11504=VERTEX_POINT('',#256231);
#11505=VERTEX_POINT('',#256281);
#11506=VERTEX_POINT('',#256282);
#11507=VERTEX_POINT('',#256332);
#11508=VERTEX_POINT('',#256333);
#11509=VERTEX_POINT('',#256380);
#11510=VERTEX_POINT('',#256381);
#11511=VERTEX_POINT('',#256428);
#11512=VERTEX_POINT('',#256429);
#11513=VERTEX_POINT('',#256482);
#11514=VERTEX_POINT('',#256483);
#11515=VERTEX_POINT('',#256530);
#11516=VERTEX_POINT('',#256531);
#11517=VERTEX_POINT('',#256578);
#11518=VERTEX_POINT('',#256579);
#11519=VERTEX_POINT('',#256632);
#11520=VERTEX_POINT('',#256633);
#11521=VERTEX_POINT('',#256680);
#11522=VERTEX_POINT('',#256681);
#11523=VERTEX_POINT('',#256728);
#11524=VERTEX_POINT('',#256729);
#11525=VERTEX_POINT('',#256776);
#11526=VERTEX_POINT('',#256777);
#11527=VERTEX_POINT('',#256830);
#11528=VERTEX_POINT('',#256831);
#11529=VERTEX_POINT('',#256878);
#11530=VERTEX_POINT('',#256879);
#11531=VERTEX_POINT('',#256926);
#11532=VERTEX_POINT('',#256927);
#11533=VERTEX_POINT('',#256980);
#11534=VERTEX_POINT('',#256981);
#11535=VERTEX_POINT('',#257028);
#11536=VERTEX_POINT('',#257029);
#11537=VERTEX_POINT('',#257076);
#11538=VERTEX_POINT('',#257077);
#11539=VERTEX_POINT('',#257079);
#11540=VERTEX_POINT('',#257086);
#11541=VERTEX_POINT('',#257093);
#11542=VERTEX_POINT('',#257094);
#11543=VERTEX_POINT('',#257118);
#11544=VERTEX_POINT('',#257119);
#11545=VERTEX_POINT('',#257142);
#11546=VERTEX_POINT('',#257143);
#11547=VERTEX_POINT('',#257167);
#11548=VERTEX_POINT('',#257168);
#11549=VERTEX_POINT('',#257192);
#11550=VERTEX_POINT('',#257193);
#11551=VERTEX_POINT('',#257216);
#11552=VERTEX_POINT('',#257217);
#11553=VERTEX_POINT('',#257241);
#11554=VERTEX_POINT('',#257242);
#11555=VERTEX_POINT('',#257266);
#11556=VERTEX_POINT('',#257267);
#11557=VERTEX_POINT('',#257290);
#11558=VERTEX_POINT('',#257291);
#11559=VERTEX_POINT('',#257314);
#11560=VERTEX_POINT('',#257315);
#11561=VERTEX_POINT('',#257339);
#11562=VERTEX_POINT('',#257340);
#11563=VERTEX_POINT('',#257364);
#11564=VERTEX_POINT('',#257365);
#11565=VERTEX_POINT('',#257388);
#11566=VERTEX_POINT('',#257389);
#11567=VERTEX_POINT('',#257413);
#11568=VERTEX_POINT('',#257414);
#11569=VERTEX_POINT('',#257438);
#11570=VERTEX_POINT('',#257439);
#11571=VERTEX_POINT('',#257462);
#11572=VERTEX_POINT('',#257463);
#11573=VERTEX_POINT('',#257487);
#11574=VERTEX_POINT('',#257488);
#11575=VERTEX_POINT('',#257511);
#11576=VERTEX_POINT('',#257512);
#11577=VERTEX_POINT('',#257536);
#11578=VERTEX_POINT('',#257537);
#11579=VERTEX_POINT('',#258083);
#11580=VERTEX_POINT('',#258197);
#11581=VERTEX_POINT('',#258299);
#11582=VERTEX_POINT('',#258833);
#11583=VERTEX_POINT('',#259038);
#11584=VERTEX_POINT('',#259039);
#11585=VERTEX_POINT('',#259041);
#11586=VERTEX_POINT('',#259043);
#11587=VERTEX_POINT('',#259047);
#11588=VERTEX_POINT('',#259049);
#11589=VERTEX_POINT('',#259053);
#11590=VERTEX_POINT('',#259055);
#11591=VERTEX_POINT('',#259059);
#11592=VERTEX_POINT('',#259061);
#11593=VERTEX_POINT('',#259065);
#11594=VERTEX_POINT('',#259067);
#11595=VERTEX_POINT('',#259075);
#11596=VERTEX_POINT('',#259078);
#15271=EDGE_CURVE('',#11495,#11496,#7793,.T.);
#15272=EDGE_CURVE('',#11495,#11497,#6579,.T.);
#15273=EDGE_CURVE('',#11497,#11498,#5379,.F.);
#15274=EDGE_CURVE('',#11498,#11496,#6580,.T.);
#15275=EDGE_CURVE('',#11499,#11500,#7794,.T.);
#15276=EDGE_CURVE('',#11499,#11495,#6581,.T.);
#15277=EDGE_CURVE('',#11496,#11500,#6582,.T.);
#15278=EDGE_CURVE('',#11501,#11502,#7795,.T.);
#15279=EDGE_CURVE('',#11501,#11499,#6583,.T.);
#15280=EDGE_CURVE('',#11500,#11502,#6584,.T.);
#15281=EDGE_CURVE('',#11503,#11504,#7796,.T.);
#15282=EDGE_CURVE('',#11503,#11501,#6585,.T.);
#15283=EDGE_CURVE('',#11502,#11504,#6586,.T.);
#15284=EDGE_CURVE('',#11505,#11506,#7797,.T.);
#15285=EDGE_CURVE('',#11505,#11503,#6587,.T.);
#15286=EDGE_CURVE('',#11504,#11506,#6588,.T.);
#15287=EDGE_CURVE('',#11507,#11508,#7798,.T.);
#15288=EDGE_CURVE('',#11507,#11505,#6589,.T.);
#15289=EDGE_CURVE('',#11506,#11508,#6590,.T.);
#15290=EDGE_CURVE('',#11509,#11510,#7799,.T.);
#15291=EDGE_CURVE('',#11509,#11507,#6591,.T.);
#15292=EDGE_CURVE('',#11508,#11510,#6592,.T.);
#15293=EDGE_CURVE('',#11511,#11512,#7800,.T.);
#15294=EDGE_CURVE('',#11511,#11509,#6593,.T.);
#15295=EDGE_CURVE('',#11510,#11512,#6594,.T.);
#15296=EDGE_CURVE('',#11513,#11514,#7801,.T.);
#15297=EDGE_CURVE('',#11513,#11511,#6595,.T.);
#15298=EDGE_CURVE('',#11512,#11514,#6596,.T.);
#15299=EDGE_CURVE('',#11515,#11516,#7802,.T.);
#15300=EDGE_CURVE('',#11515,#11513,#6597,.T.);
#15301=EDGE_CURVE('',#11514,#11516,#6598,.T.);
#15302=EDGE_CURVE('',#11517,#11518,#7803,.T.);
#15303=EDGE_CURVE('',#11517,#11515,#6599,.T.);
#15304=EDGE_CURVE('',#11516,#11518,#6600,.T.);
#15305=EDGE_CURVE('',#11519,#11520,#7804,.T.);
#15306=EDGE_CURVE('',#11519,#11517,#6601,.T.);
#15307=EDGE_CURVE('',#11518,#11520,#6602,.T.);
#15308=EDGE_CURVE('',#11521,#11522,#7805,.T.);
#15309=EDGE_CURVE('',#11521,#11519,#6603,.T.);
#15310=EDGE_CURVE('',#11520,#11522,#6604,.T.);
#15311=EDGE_CURVE('',#11523,#11524,#7806,.T.);
#15312=EDGE_CURVE('',#11523,#11521,#6605,.T.);
#15313=EDGE_CURVE('',#11522,#11524,#6606,.T.);
#15314=EDGE_CURVE('',#11525,#11526,#7807,.T.);
#15315=EDGE_CURVE('',#11525,#11523,#6607,.T.);
#15316=EDGE_CURVE('',#11524,#11526,#6608,.T.);
#15317=EDGE_CURVE('',#11527,#11528,#7808,.T.);
#15318=EDGE_CURVE('',#11527,#11525,#6609,.T.);
#15319=EDGE_CURVE('',#11526,#11528,#6610,.T.);
#15320=EDGE_CURVE('',#11529,#11530,#7809,.T.);
#15321=EDGE_CURVE('',#11529,#11527,#6611,.T.);
#15322=EDGE_CURVE('',#11528,#11530,#6612,.T.);
#15323=EDGE_CURVE('',#11531,#11532,#7810,.T.);
#15324=EDGE_CURVE('',#11531,#11529,#6613,.T.);
#15325=EDGE_CURVE('',#11530,#11532,#6614,.T.);
#15326=EDGE_CURVE('',#11533,#11534,#7811,.T.);
#15327=EDGE_CURVE('',#11533,#11531,#6615,.T.);
#15328=EDGE_CURVE('',#11532,#11534,#6616,.T.);
#15329=EDGE_CURVE('',#11535,#11536,#7812,.T.);
#15330=EDGE_CURVE('',#11535,#11533,#6617,.T.);
#15331=EDGE_CURVE('',#11534,#11536,#6618,.T.);
#15332=EDGE_CURVE('',#11537,#11538,#7813,.T.);
#15333=EDGE_CURVE('',#11537,#11539,#6619,.T.);
#15334=EDGE_CURVE('',#11540,#11539,#5380,.T.);
#15335=EDGE_CURVE('',#11538,#11540,#6620,.T.);
#15336=EDGE_CURVE('',#11541,#11542,#7814,.T.);
#15337=EDGE_CURVE('',#11541,#11537,#6621,.T.);
#15338=EDGE_CURVE('',#11542,#11538,#6622,.T.);
#15339=EDGE_CURVE('',#11543,#11544,#7815,.T.);
#15340=EDGE_CURVE('',#11543,#11541,#6623,.T.);
#15341=EDGE_CURVE('',#11544,#11542,#6624,.T.);
#15342=EDGE_CURVE('',#11545,#11546,#7816,.T.);
#15343=EDGE_CURVE('',#11545,#11543,#6625,.T.);
#15344=EDGE_CURVE('',#11546,#11544,#6626,.T.);
#15345=EDGE_CURVE('',#11547,#11548,#7817,.T.);
#15346=EDGE_CURVE('',#11547,#11545,#6627,.T.);
#15347=EDGE_CURVE('',#11548,#11546,#6628,.T.);
#15348=EDGE_CURVE('',#11549,#11550,#7818,.T.);
#15349=EDGE_CURVE('',#11549,#11547,#6629,.T.);
#15350=EDGE_CURVE('',#11550,#11548,#6630,.T.);
#15351=EDGE_CURVE('',#11551,#11552,#7819,.T.);
#15352=EDGE_CURVE('',#11551,#11549,#6631,.T.);
#15353=EDGE_CURVE('',#11552,#11550,#6632,.T.);
#15354=EDGE_CURVE('',#11553,#11554,#7820,.T.);
#15355=EDGE_CURVE('',#11553,#11551,#6633,.T.);
#15356=EDGE_CURVE('',#11554,#11552,#6634,.T.);
#15357=EDGE_CURVE('',#11555,#11556,#7821,.T.);
#15358=EDGE_CURVE('',#11555,#11553,#6635,.T.);
#15359=EDGE_CURVE('',#11556,#11554,#6636,.T.);
#15360=EDGE_CURVE('',#11557,#11558,#7822,.T.);
#15361=EDGE_CURVE('',#11557,#11555,#6637,.T.);
#15362=EDGE_CURVE('',#11558,#11556,#6638,.T.);
#15363=EDGE_CURVE('',#11559,#11560,#7823,.T.);
#15364=EDGE_CURVE('',#11559,#11557,#6639,.T.);
#15365=EDGE_CURVE('',#11560,#11558,#6640,.T.);
#15366=EDGE_CURVE('',#11561,#11562,#7824,.T.);
#15367=EDGE_CURVE('',#11561,#11559,#6641,.T.);
#15368=EDGE_CURVE('',#11562,#11560,#6642,.T.);
#15369=EDGE_CURVE('',#11563,#11564,#7825,.T.);
#15370=EDGE_CURVE('',#11563,#11561,#6643,.T.);
#15371=EDGE_CURVE('',#11564,#11562,#6644,.T.);
#15372=EDGE_CURVE('',#11565,#11566,#7826,.T.);
#15373=EDGE_CURVE('',#11565,#11563,#6645,.T.);
#15374=EDGE_CURVE('',#11566,#11564,#6646,.T.);
#15375=EDGE_CURVE('',#11567,#11568,#7827,.T.);
#15376=EDGE_CURVE('',#11567,#11565,#6647,.T.);
#15377=EDGE_CURVE('',#11568,#11566,#6648,.T.);
#15378=EDGE_CURVE('',#11569,#11570,#7828,.T.);
#15379=EDGE_CURVE('',#11569,#11567,#6649,.T.);
#15380=EDGE_CURVE('',#11570,#11568,#6650,.T.);
#15381=EDGE_CURVE('',#11571,#11572,#7829,.T.);
#15382=EDGE_CURVE('',#11571,#11569,#6651,.T.);
#15383=EDGE_CURVE('',#11572,#11570,#6652,.T.);
#15384=EDGE_CURVE('',#11573,#11574,#7830,.T.);
#15385=EDGE_CURVE('',#11573,#11571,#6653,.T.);
#15386=EDGE_CURVE('',#11574,#11572,#6654,.T.);
#15387=EDGE_CURVE('',#11575,#11576,#7831,.T.);
#15388=EDGE_CURVE('',#11575,#11573,#6655,.T.);
#15389=EDGE_CURVE('',#11576,#11574,#6656,.T.);
#15390=EDGE_CURVE('',#11577,#11578,#7832,.T.);
#15391=EDGE_CURVE('',#11577,#11575,#6657,.T.);
#15392=EDGE_CURVE('',#11578,#11576,#6658,.T.);
#15393=EDGE_CURVE('',#11579,#11540,#6659,.T.);
#15394=EDGE_CURVE('',#11536,#11579,#6660,.T.);
#15395=EDGE_CURVE('',#11580,#11498,#6661,.T.);
#15396=EDGE_CURVE('',#11580,#11578,#6662,.T.);
#15397=EDGE_CURVE('',#11581,#11580,#5381,.T.);
#15398=EDGE_CURVE('',#11581,#11577,#6663,.T.);
#15399=EDGE_CURVE('',#11539,#11582,#6664,.T.);
#15400=EDGE_CURVE('',#11497,#11581,#6665,.T.);
#15401=EDGE_CURVE('',#11582,#11535,#6666,.T.);
#15402=EDGE_CURVE('',#11582,#11579,#5382,.F.);
#15403=EDGE_CURVE('',#11583,#11584,#7833,.T.);
#15404=EDGE_CURVE('',#11583,#11585,#7834,.T.);
#15405=EDGE_CURVE('',#11585,#11586,#7835,.T.);
#15406=EDGE_CURVE('',#11584,#11586,#7836,.T.);
#15407=EDGE_CURVE('',#11587,#11583,#7837,.T.);
#15408=EDGE_CURVE('',#11587,#11588,#7838,.T.);
#15409=EDGE_CURVE('',#11588,#11585,#7839,.T.);
#15410=EDGE_CURVE('',#11589,#11587,#7840,.T.);
#15411=EDGE_CURVE('',#11589,#11590,#7841,.T.);
#15412=EDGE_CURVE('',#11590,#11588,#7842,.T.);
#15413=EDGE_CURVE('',#11591,#11589,#7843,.T.);
#15414=EDGE_CURVE('',#11591,#11592,#7844,.T.);
#15415=EDGE_CURVE('',#11592,#11590,#7845,.T.);
#15416=EDGE_CURVE('',#11593,#11591,#7846,.T.);
#15417=EDGE_CURVE('',#11593,#11594,#7847,.T.);
#15418=EDGE_CURVE('',#11594,#11592,#7848,.T.);
#15419=EDGE_CURVE('',#11584,#11593,#7849,.T.);
#15420=EDGE_CURVE('',#11586,#11594,#7850,.T.);
#15421=EDGE_CURVE('',#11595,#11595,#5383,.T.);
#15422=EDGE_CURVE('',#11595,#11596,#7851,.T.);
#15423=EDGE_CURVE('',#11596,#11596,#5384,.T.);
#22772=ORIENTED_EDGE('',*,*,#15271,.F.);
#22773=ORIENTED_EDGE('',*,*,#15272,.T.);
#22774=ORIENTED_EDGE('',*,*,#15273,.T.);
#22775=ORIENTED_EDGE('',*,*,#15274,.T.);
#22776=ORIENTED_EDGE('',*,*,#15275,.F.);
#22777=ORIENTED_EDGE('',*,*,#15276,.T.);
#22778=ORIENTED_EDGE('',*,*,#15271,.T.);
#22779=ORIENTED_EDGE('',*,*,#15277,.T.);
#22780=ORIENTED_EDGE('',*,*,#15278,.F.);
#22781=ORIENTED_EDGE('',*,*,#15279,.T.);
#22782=ORIENTED_EDGE('',*,*,#15275,.T.);
#22783=ORIENTED_EDGE('',*,*,#15280,.T.);
#22784=ORIENTED_EDGE('',*,*,#15281,.F.);
#22785=ORIENTED_EDGE('',*,*,#15282,.T.);
#22786=ORIENTED_EDGE('',*,*,#15278,.T.);
#22787=ORIENTED_EDGE('',*,*,#15283,.T.);
#22788=ORIENTED_EDGE('',*,*,#15284,.F.);
#22789=ORIENTED_EDGE('',*,*,#15285,.T.);
#22790=ORIENTED_EDGE('',*,*,#15281,.T.);
#22791=ORIENTED_EDGE('',*,*,#15286,.T.);
#22792=ORIENTED_EDGE('',*,*,#15287,.F.);
#22793=ORIENTED_EDGE('',*,*,#15288,.T.);
#22794=ORIENTED_EDGE('',*,*,#15284,.T.);
#22795=ORIENTED_EDGE('',*,*,#15289,.T.);
#22796=ORIENTED_EDGE('',*,*,#15290,.F.);
#22797=ORIENTED_EDGE('',*,*,#15291,.T.);
#22798=ORIENTED_EDGE('',*,*,#15287,.T.);
#22799=ORIENTED_EDGE('',*,*,#15292,.T.);
#22800=ORIENTED_EDGE('',*,*,#15293,.F.);
#22801=ORIENTED_EDGE('',*,*,#15294,.T.);
#22802=ORIENTED_EDGE('',*,*,#15290,.T.);
#22803=ORIENTED_EDGE('',*,*,#15295,.T.);
#22804=ORIENTED_EDGE('',*,*,#15296,.F.);
#22805=ORIENTED_EDGE('',*,*,#15297,.T.);
#22806=ORIENTED_EDGE('',*,*,#15293,.T.);
#22807=ORIENTED_EDGE('',*,*,#15298,.T.);
#22808=ORIENTED_EDGE('',*,*,#15299,.F.);
#22809=ORIENTED_EDGE('',*,*,#15300,.T.);
#22810=ORIENTED_EDGE('',*,*,#15296,.T.);
#22811=ORIENTED_EDGE('',*,*,#15301,.T.);
#22812=ORIENTED_EDGE('',*,*,#15302,.F.);
#22813=ORIENTED_EDGE('',*,*,#15303,.T.);
#22814=ORIENTED_EDGE('',*,*,#15299,.T.);
#22815=ORIENTED_EDGE('',*,*,#15304,.T.);
#22816=ORIENTED_EDGE('',*,*,#15305,.F.);
#22817=ORIENTED_EDGE('',*,*,#15306,.T.);
#22818=ORIENTED_EDGE('',*,*,#15302,.T.);
#22819=ORIENTED_EDGE('',*,*,#15307,.T.);
#22820=ORIENTED_EDGE('',*,*,#15308,.F.);
#22821=ORIENTED_EDGE('',*,*,#15309,.T.);
#22822=ORIENTED_EDGE('',*,*,#15305,.T.);
#22823=ORIENTED_EDGE('',*,*,#15310,.T.);
#22824=ORIENTED_EDGE('',*,*,#15311,.F.);
#22825=ORIENTED_EDGE('',*,*,#15312,.T.);
#22826=ORIENTED_EDGE('',*,*,#15308,.T.);
#22827=ORIENTED_EDGE('',*,*,#15313,.T.);
#22828=ORIENTED_EDGE('',*,*,#15314,.F.);
#22829=ORIENTED_EDGE('',*,*,#15315,.T.);
#22830=ORIENTED_EDGE('',*,*,#15311,.T.);
#22831=ORIENTED_EDGE('',*,*,#15316,.T.);
#22832=ORIENTED_EDGE('',*,*,#15317,.F.);
#22833=ORIENTED_EDGE('',*,*,#15318,.T.);
#22834=ORIENTED_EDGE('',*,*,#15314,.T.);
#22835=ORIENTED_EDGE('',*,*,#15319,.T.);
#22836=ORIENTED_EDGE('',*,*,#15320,.F.);
#22837=ORIENTED_EDGE('',*,*,#15321,.T.);
#22838=ORIENTED_EDGE('',*,*,#15317,.T.);
#22839=ORIENTED_EDGE('',*,*,#15322,.T.);
#22840=ORIENTED_EDGE('',*,*,#15323,.F.);
#22841=ORIENTED_EDGE('',*,*,#15324,.T.);
#22842=ORIENTED_EDGE('',*,*,#15320,.T.);
#22843=ORIENTED_EDGE('',*,*,#15325,.T.);
#22844=ORIENTED_EDGE('',*,*,#15326,.F.);
#22845=ORIENTED_EDGE('',*,*,#15327,.T.);
#22846=ORIENTED_EDGE('',*,*,#15323,.T.);
#22847=ORIENTED_EDGE('',*,*,#15328,.T.);
#22848=ORIENTED_EDGE('',*,*,#15329,.F.);
#22849=ORIENTED_EDGE('',*,*,#15330,.T.);
#22850=ORIENTED_EDGE('',*,*,#15326,.T.);
#22851=ORIENTED_EDGE('',*,*,#15331,.T.);
#22852=ORIENTED_EDGE('',*,*,#15332,.F.);
#22853=ORIENTED_EDGE('',*,*,#15333,.T.);
#22854=ORIENTED_EDGE('',*,*,#15334,.F.);
#22855=ORIENTED_EDGE('',*,*,#15335,.F.);
#22856=ORIENTED_EDGE('',*,*,#15336,.F.);
#22857=ORIENTED_EDGE('',*,*,#15337,.T.);
#22858=ORIENTED_EDGE('',*,*,#15332,.T.);
#22859=ORIENTED_EDGE('',*,*,#15338,.F.);
#22860=ORIENTED_EDGE('',*,*,#15339,.F.);
#22861=ORIENTED_EDGE('',*,*,#15340,.T.);
#22862=ORIENTED_EDGE('',*,*,#15336,.T.);
#22863=ORIENTED_EDGE('',*,*,#15341,.F.);
#22864=ORIENTED_EDGE('',*,*,#15342,.F.);
#22865=ORIENTED_EDGE('',*,*,#15343,.T.);
#22866=ORIENTED_EDGE('',*,*,#15339,.T.);
#22867=ORIENTED_EDGE('',*,*,#15344,.F.);
#22868=ORIENTED_EDGE('',*,*,#15345,.F.);
#22869=ORIENTED_EDGE('',*,*,#15346,.T.);
#22870=ORIENTED_EDGE('',*,*,#15342,.T.);
#22871=ORIENTED_EDGE('',*,*,#15347,.F.);
#22872=ORIENTED_EDGE('',*,*,#15348,.F.);
#22873=ORIENTED_EDGE('',*,*,#15349,.T.);
#22874=ORIENTED_EDGE('',*,*,#15345,.T.);
#22875=ORIENTED_EDGE('',*,*,#15350,.F.);
#22876=ORIENTED_EDGE('',*,*,#15351,.F.);
#22877=ORIENTED_EDGE('',*,*,#15352,.T.);
#22878=ORIENTED_EDGE('',*,*,#15348,.T.);
#22879=ORIENTED_EDGE('',*,*,#15353,.F.);
#22880=ORIENTED_EDGE('',*,*,#15354,.F.);
#22881=ORIENTED_EDGE('',*,*,#15355,.T.);
#22882=ORIENTED_EDGE('',*,*,#15351,.T.);
#22883=ORIENTED_EDGE('',*,*,#15356,.F.);
#22884=ORIENTED_EDGE('',*,*,#15357,.F.);
#22885=ORIENTED_EDGE('',*,*,#15358,.T.);
#22886=ORIENTED_EDGE('',*,*,#15354,.T.);
#22887=ORIENTED_EDGE('',*,*,#15359,.F.);
#22888=ORIENTED_EDGE('',*,*,#15360,.F.);
#22889=ORIENTED_EDGE('',*,*,#15361,.T.);
#22890=ORIENTED_EDGE('',*,*,#15357,.T.);
#22891=ORIENTED_EDGE('',*,*,#15362,.F.);
#22892=ORIENTED_EDGE('',*,*,#15363,.F.);
#22893=ORIENTED_EDGE('',*,*,#15364,.T.);
#22894=ORIENTED_EDGE('',*,*,#15360,.T.);
#22895=ORIENTED_EDGE('',*,*,#15365,.F.);
#22896=ORIENTED_EDGE('',*,*,#15366,.F.);
#22897=ORIENTED_EDGE('',*,*,#15367,.T.);
#22898=ORIENTED_EDGE('',*,*,#15363,.T.);
#22899=ORIENTED_EDGE('',*,*,#15368,.F.);
#22900=ORIENTED_EDGE('',*,*,#15369,.F.);
#22901=ORIENTED_EDGE('',*,*,#15370,.T.);
#22902=ORIENTED_EDGE('',*,*,#15366,.T.);
#22903=ORIENTED_EDGE('',*,*,#15371,.F.);
#22904=ORIENTED_EDGE('',*,*,#15372,.F.);
#22905=ORIENTED_EDGE('',*,*,#15373,.T.);
#22906=ORIENTED_EDGE('',*,*,#15369,.T.);
#22907=ORIENTED_EDGE('',*,*,#15374,.F.);
#22908=ORIENTED_EDGE('',*,*,#15375,.F.);
#22909=ORIENTED_EDGE('',*,*,#15376,.T.);
#22910=ORIENTED_EDGE('',*,*,#15372,.T.);
#22911=ORIENTED_EDGE('',*,*,#15377,.F.);
#22912=ORIENTED_EDGE('',*,*,#15378,.F.);
#22913=ORIENTED_EDGE('',*,*,#15379,.T.);
#22914=ORIENTED_EDGE('',*,*,#15375,.T.);
#22915=ORIENTED_EDGE('',*,*,#15380,.F.);
#22916=ORIENTED_EDGE('',*,*,#15381,.F.);
#22917=ORIENTED_EDGE('',*,*,#15382,.T.);
#22918=ORIENTED_EDGE('',*,*,#15378,.T.);
#22919=ORIENTED_EDGE('',*,*,#15383,.F.);
#22920=ORIENTED_EDGE('',*,*,#15384,.F.);
#22921=ORIENTED_EDGE('',*,*,#15385,.T.);
#22922=ORIENTED_EDGE('',*,*,#15381,.T.);
#22923=ORIENTED_EDGE('',*,*,#15386,.F.);
#22924=ORIENTED_EDGE('',*,*,#15387,.F.);
#22925=ORIENTED_EDGE('',*,*,#15388,.T.);
#22926=ORIENTED_EDGE('',*,*,#15384,.T.);
#22927=ORIENTED_EDGE('',*,*,#15389,.F.);
#22928=ORIENTED_EDGE('',*,*,#15390,.F.);
#22929=ORIENTED_EDGE('',*,*,#15391,.T.);
#22930=ORIENTED_EDGE('',*,*,#15387,.T.);
#22931=ORIENTED_EDGE('',*,*,#15392,.F.);
#22932=ORIENTED_EDGE('',*,*,#15393,.F.);
#22933=ORIENTED_EDGE('',*,*,#15394,.F.);
#22934=ORIENTED_EDGE('',*,*,#15331,.F.);
#22935=ORIENTED_EDGE('',*,*,#15328,.F.);
#22936=ORIENTED_EDGE('',*,*,#15325,.F.);
#22937=ORIENTED_EDGE('',*,*,#15322,.F.);
#22938=ORIENTED_EDGE('',*,*,#15319,.F.);
#22939=ORIENTED_EDGE('',*,*,#15316,.F.);
#22940=ORIENTED_EDGE('',*,*,#15313,.F.);
#22941=ORIENTED_EDGE('',*,*,#15310,.F.);
#22942=ORIENTED_EDGE('',*,*,#15307,.F.);
#22943=ORIENTED_EDGE('',*,*,#15304,.F.);
#22944=ORIENTED_EDGE('',*,*,#15301,.F.);
#22945=ORIENTED_EDGE('',*,*,#15298,.F.);
#22946=ORIENTED_EDGE('',*,*,#15295,.F.);
#22947=ORIENTED_EDGE('',*,*,#15292,.F.);
#22948=ORIENTED_EDGE('',*,*,#15289,.F.);
#22949=ORIENTED_EDGE('',*,*,#15286,.F.);
#22950=ORIENTED_EDGE('',*,*,#15283,.F.);
#22951=ORIENTED_EDGE('',*,*,#15280,.F.);
#22952=ORIENTED_EDGE('',*,*,#15277,.F.);
#22953=ORIENTED_EDGE('',*,*,#15274,.F.);
#22954=ORIENTED_EDGE('',*,*,#15395,.F.);
#22955=ORIENTED_EDGE('',*,*,#15396,.T.);
#22956=ORIENTED_EDGE('',*,*,#15392,.T.);
#22957=ORIENTED_EDGE('',*,*,#15389,.T.);
#22958=ORIENTED_EDGE('',*,*,#15386,.T.);
#22959=ORIENTED_EDGE('',*,*,#15383,.T.);
#22960=ORIENTED_EDGE('',*,*,#15380,.T.);
#22961=ORIENTED_EDGE('',*,*,#15377,.T.);
#22962=ORIENTED_EDGE('',*,*,#15374,.T.);
#22963=ORIENTED_EDGE('',*,*,#15371,.T.);
#22964=ORIENTED_EDGE('',*,*,#15368,.T.);
#22965=ORIENTED_EDGE('',*,*,#15365,.T.);
#22966=ORIENTED_EDGE('',*,*,#15362,.T.);
#22967=ORIENTED_EDGE('',*,*,#15359,.T.);
#22968=ORIENTED_EDGE('',*,*,#15356,.T.);
#22969=ORIENTED_EDGE('',*,*,#15353,.T.);
#22970=ORIENTED_EDGE('',*,*,#15350,.T.);
#22971=ORIENTED_EDGE('',*,*,#15347,.T.);
#22972=ORIENTED_EDGE('',*,*,#15344,.T.);
#22973=ORIENTED_EDGE('',*,*,#15341,.T.);
#22974=ORIENTED_EDGE('',*,*,#15338,.T.);
#22975=ORIENTED_EDGE('',*,*,#15335,.T.);
#22976=ORIENTED_EDGE('',*,*,#15390,.T.);
#22977=ORIENTED_EDGE('',*,*,#15396,.F.);
#22978=ORIENTED_EDGE('',*,*,#15397,.F.);
#22979=ORIENTED_EDGE('',*,*,#15398,.T.);
#22980=ORIENTED_EDGE('',*,*,#15399,.F.);
#22981=ORIENTED_EDGE('',*,*,#15333,.F.);
#22982=ORIENTED_EDGE('',*,*,#15337,.F.);
#22983=ORIENTED_EDGE('',*,*,#15340,.F.);
#22984=ORIENTED_EDGE('',*,*,#15343,.F.);
#22985=ORIENTED_EDGE('',*,*,#15346,.F.);
#22986=ORIENTED_EDGE('',*,*,#15349,.F.);
#22987=ORIENTED_EDGE('',*,*,#15352,.F.);
#22988=ORIENTED_EDGE('',*,*,#15355,.F.);
#22989=ORIENTED_EDGE('',*,*,#15358,.F.);
#22990=ORIENTED_EDGE('',*,*,#15361,.F.);
#22991=ORIENTED_EDGE('',*,*,#15364,.F.);
#22992=ORIENTED_EDGE('',*,*,#15367,.F.);
#22993=ORIENTED_EDGE('',*,*,#15370,.F.);
#22994=ORIENTED_EDGE('',*,*,#15373,.F.);
#22995=ORIENTED_EDGE('',*,*,#15376,.F.);
#22996=ORIENTED_EDGE('',*,*,#15379,.F.);
#22997=ORIENTED_EDGE('',*,*,#15382,.F.);
#22998=ORIENTED_EDGE('',*,*,#15385,.F.);
#22999=ORIENTED_EDGE('',*,*,#15388,.F.);
#23000=ORIENTED_EDGE('',*,*,#15391,.F.);
#23001=ORIENTED_EDGE('',*,*,#15398,.F.);
#23002=ORIENTED_EDGE('',*,*,#15400,.F.);
#23003=ORIENTED_EDGE('',*,*,#15272,.F.);
#23004=ORIENTED_EDGE('',*,*,#15276,.F.);
#23005=ORIENTED_EDGE('',*,*,#15279,.F.);
#23006=ORIENTED_EDGE('',*,*,#15282,.F.);
#23007=ORIENTED_EDGE('',*,*,#15285,.F.);
#23008=ORIENTED_EDGE('',*,*,#15288,.F.);
#23009=ORIENTED_EDGE('',*,*,#15291,.F.);
#23010=ORIENTED_EDGE('',*,*,#15294,.F.);
#23011=ORIENTED_EDGE('',*,*,#15297,.F.);
#23012=ORIENTED_EDGE('',*,*,#15300,.F.);
#23013=ORIENTED_EDGE('',*,*,#15303,.F.);
#23014=ORIENTED_EDGE('',*,*,#15306,.F.);
#23015=ORIENTED_EDGE('',*,*,#15309,.F.);
#23016=ORIENTED_EDGE('',*,*,#15312,.F.);
#23017=ORIENTED_EDGE('',*,*,#15315,.F.);
#23018=ORIENTED_EDGE('',*,*,#15318,.F.);
#23019=ORIENTED_EDGE('',*,*,#15321,.F.);
#23020=ORIENTED_EDGE('',*,*,#15324,.F.);
#23021=ORIENTED_EDGE('',*,*,#15327,.F.);
#23022=ORIENTED_EDGE('',*,*,#15330,.F.);
#23023=ORIENTED_EDGE('',*,*,#15401,.F.);
#23024=ORIENTED_EDGE('',*,*,#15329,.T.);
#23025=ORIENTED_EDGE('',*,*,#15394,.T.);
#23026=ORIENTED_EDGE('',*,*,#15402,.F.);
#23027=ORIENTED_EDGE('',*,*,#15401,.T.);
#23028=ORIENTED_EDGE('',*,*,#15403,.F.);
#23029=ORIENTED_EDGE('',*,*,#15404,.T.);
#23030=ORIENTED_EDGE('',*,*,#15405,.T.);
#23031=ORIENTED_EDGE('',*,*,#15406,.F.);
#23032=ORIENTED_EDGE('',*,*,#15407,.F.);
#23033=ORIENTED_EDGE('',*,*,#15408,.T.);
#23034=ORIENTED_EDGE('',*,*,#15409,.T.);
#23035=ORIENTED_EDGE('',*,*,#15404,.F.);
#23036=ORIENTED_EDGE('',*,*,#15410,.F.);
#23037=ORIENTED_EDGE('',*,*,#15411,.T.);
#23038=ORIENTED_EDGE('',*,*,#15412,.T.);
#23039=ORIENTED_EDGE('',*,*,#15408,.F.);
#23040=ORIENTED_EDGE('',*,*,#15413,.F.);
#23041=ORIENTED_EDGE('',*,*,#15414,.T.);
#23042=ORIENTED_EDGE('',*,*,#15415,.T.);
#23043=ORIENTED_EDGE('',*,*,#15411,.F.);
#23044=ORIENTED_EDGE('',*,*,#15416,.F.);
#23045=ORIENTED_EDGE('',*,*,#15417,.T.);
#23046=ORIENTED_EDGE('',*,*,#15418,.T.);
#23047=ORIENTED_EDGE('',*,*,#15414,.F.);
#23048=ORIENTED_EDGE('',*,*,#15419,.F.);
#23049=ORIENTED_EDGE('',*,*,#15406,.T.);
#23050=ORIENTED_EDGE('',*,*,#15420,.T.);
#23051=ORIENTED_EDGE('',*,*,#15417,.F.);
#23052=ORIENTED_EDGE('',*,*,#15420,.F.);
#23053=ORIENTED_EDGE('',*,*,#15405,.F.);
#23054=ORIENTED_EDGE('',*,*,#15409,.F.);
#23055=ORIENTED_EDGE('',*,*,#15412,.F.);
#23056=ORIENTED_EDGE('',*,*,#15415,.F.);
#23057=ORIENTED_EDGE('',*,*,#15418,.F.);
#23058=ORIENTED_EDGE('',*,*,#15421,.T.);
#23059=ORIENTED_EDGE('',*,*,#15400,.T.);
#23060=ORIENTED_EDGE('',*,*,#15397,.T.);
#23061=ORIENTED_EDGE('',*,*,#15395,.T.);
#23062=ORIENTED_EDGE('',*,*,#15273,.F.);
#23063=ORIENTED_EDGE('',*,*,#15421,.F.);
#23064=ORIENTED_EDGE('',*,*,#15422,.T.);
#23065=ORIENTED_EDGE('',*,*,#15423,.T.);
#23066=ORIENTED_EDGE('',*,*,#15422,.F.);
#23067=ORIENTED_EDGE('',*,*,#15423,.F.);
#23068=ORIENTED_EDGE('',*,*,#15403,.T.);
#23069=ORIENTED_EDGE('',*,*,#15419,.T.);
#23070=ORIENTED_EDGE('',*,*,#15416,.T.);
#23071=ORIENTED_EDGE('',*,*,#15413,.T.);
#23072=ORIENTED_EDGE('',*,*,#15410,.T.);
#23073=ORIENTED_EDGE('',*,*,#15407,.T.);
#23074=ORIENTED_EDGE('',*,*,#15399,.T.);
#23075=ORIENTED_EDGE('',*,*,#15402,.T.);
#23076=ORIENTED_EDGE('',*,*,#15393,.T.);
#23077=ORIENTED_EDGE('',*,*,#15334,.T.);
#23761=CYLINDRICAL_SURFACE('',#27177,2.942);
#23762=CYLINDRICAL_SURFACE('',#27179,2.942);
#23763=CYLINDRICAL_SURFACE('',#27180,2.942);
#23764=CYLINDRICAL_SURFACE('',#27181,2.942);
#23765=CYLINDRICAL_SURFACE('',#27182,2.942);
#23766=CYLINDRICAL_SURFACE('',#27183,2.942);
#23767=CYLINDRICAL_SURFACE('',#27184,2.942);
#23768=CYLINDRICAL_SURFACE('',#27185,2.942);
#23769=CYLINDRICAL_SURFACE('',#27186,2.942);
#23770=CYLINDRICAL_SURFACE('',#27187,2.942);
#23771=CYLINDRICAL_SURFACE('',#27188,2.942);
#23772=CYLINDRICAL_SURFACE('',#27189,2.942);
#23773=CYLINDRICAL_SURFACE('',#27190,2.942);
#23774=CYLINDRICAL_SURFACE('',#27191,2.942);
#23775=CYLINDRICAL_SURFACE('',#27192,2.942);
#23776=CYLINDRICAL_SURFACE('',#27193,2.942);
#23777=CYLINDRICAL_SURFACE('',#27194,2.942);
#23778=CYLINDRICAL_SURFACE('',#27195,2.942);
#23779=CYLINDRICAL_SURFACE('',#27196,2.942);
#23780=CYLINDRICAL_SURFACE('',#27197,2.942);
#23781=CYLINDRICAL_SURFACE('',#27198,2.37175);
#23782=CYLINDRICAL_SURFACE('',#27200,2.37175);
#23783=CYLINDRICAL_SURFACE('',#27201,2.37175);
#23784=CYLINDRICAL_SURFACE('',#27202,2.37175);
#23785=CYLINDRICAL_SURFACE('',#27203,2.37175);
#23786=CYLINDRICAL_SURFACE('',#27204,2.37175);
#23787=CYLINDRICAL_SURFACE('',#27205,2.37175);
#23788=CYLINDRICAL_SURFACE('',#27206,2.37175);
#23789=CYLINDRICAL_SURFACE('',#27207,2.37175);
#23790=CYLINDRICAL_SURFACE('',#27208,2.37175);
#23791=CYLINDRICAL_SURFACE('',#27209,2.37175);
#23792=CYLINDRICAL_SURFACE('',#27210,2.37175);
#23793=CYLINDRICAL_SURFACE('',#27211,2.37175);
#23794=CYLINDRICAL_SURFACE('',#27212,2.37175);
#23795=CYLINDRICAL_SURFACE('',#27213,2.37175);
#23796=CYLINDRICAL_SURFACE('',#27214,2.37175);
#23797=CYLINDRICAL_SURFACE('',#27215,2.37175);
#23798=CYLINDRICAL_SURFACE('',#27216,2.37175);
#23799=CYLINDRICAL_SURFACE('',#27217,2.37175);
#23800=CYLINDRICAL_SURFACE('',#27218,2.37175);
#23801=CYLINDRICAL_SURFACE('',#27219,2.37175);
#23802=CYLINDRICAL_SURFACE('',#27221,2.942);
#23803=CYLINDRICAL_SURFACE('',#27232,5.);
#25095=ADVANCED_FACE('',(#2989),#23761,.T.);
#25096=ADVANCED_FACE('',(#2990),#23762,.T.);
#25097=ADVANCED_FACE('',(#2991),#23763,.T.);
#25098=ADVANCED_FACE('',(#2992),#23764,.T.);
#25099=ADVANCED_FACE('',(#2993),#23765,.T.);
#25100=ADVANCED_FACE('',(#2994),#23766,.T.);
#25101=ADVANCED_FACE('',(#2995),#23767,.T.);
#25102=ADVANCED_FACE('',(#2996),#23768,.T.);
#25103=ADVANCED_FACE('',(#2997),#23769,.T.);
#25104=ADVANCED_FACE('',(#2998),#23770,.T.);
#25105=ADVANCED_FACE('',(#2999),#23771,.T.);
#25106=ADVANCED_FACE('',(#3000),#23772,.T.);
#25107=ADVANCED_FACE('',(#3001),#23773,.T.);
#25108=ADVANCED_FACE('',(#3002),#23774,.T.);
#25109=ADVANCED_FACE('',(#3003),#23775,.T.);
#25110=ADVANCED_FACE('',(#3004),#23776,.T.);
#25111=ADVANCED_FACE('',(#3005),#23777,.T.);
#25112=ADVANCED_FACE('',(#3006),#23778,.T.);
#25113=ADVANCED_FACE('',(#3007),#23779,.T.);
#25114=ADVANCED_FACE('',(#3008),#23780,.T.);
#25115=ADVANCED_FACE('',(#3009),#23781,.T.);
#25116=ADVANCED_FACE('',(#3010),#23782,.T.);
#25117=ADVANCED_FACE('',(#3011),#23783,.T.);
#25118=ADVANCED_FACE('',(#3012),#23784,.T.);
#25119=ADVANCED_FACE('',(#3013),#23785,.T.);
#25120=ADVANCED_FACE('',(#3014),#23786,.T.);
#25121=ADVANCED_FACE('',(#3015),#23787,.T.);
#25122=ADVANCED_FACE('',(#3016),#23788,.T.);
#25123=ADVANCED_FACE('',(#3017),#23789,.T.);
#25124=ADVANCED_FACE('',(#3018),#23790,.T.);
#25125=ADVANCED_FACE('',(#3019),#23791,.T.);
#25126=ADVANCED_FACE('',(#3020),#23792,.T.);
#25127=ADVANCED_FACE('',(#3021),#23793,.T.);
#25128=ADVANCED_FACE('',(#3022),#23794,.T.);
#25129=ADVANCED_FACE('',(#3023),#23795,.T.);
#25130=ADVANCED_FACE('',(#3024),#23796,.T.);
#25131=ADVANCED_FACE('',(#3025),#23797,.T.);
#25132=ADVANCED_FACE('',(#3026),#23798,.T.);
#25133=ADVANCED_FACE('',(#3027),#23799,.T.);
#25134=ADVANCED_FACE('',(#3028),#23800,.T.);
#25135=ADVANCED_FACE('',(#3029),#1478,.F.);
#25136=ADVANCED_FACE('',(#3030),#23801,.T.);
#25137=ADVANCED_FACE('',(#3031),#1479,.F.);
#25138=ADVANCED_FACE('',(#3032),#23802,.T.);
#25139=ADVANCED_FACE('',(#3033),#1688,.F.);
#25140=ADVANCED_FACE('',(#3034),#1689,.F.);
#25141=ADVANCED_FACE('',(#3035),#1690,.F.);
#25142=ADVANCED_FACE('',(#3036),#1691,.F.);
#25143=ADVANCED_FACE('',(#3037),#1692,.F.);
#25144=ADVANCED_FACE('',(#3038),#1693,.F.);
#25145=ADVANCED_FACE('',(#3039),#1694,.F.);
#25146=ADVANCED_FACE('',(#3040,#1316),#1695,.T.);
#25147=ADVANCED_FACE('',(#3041),#23803,.T.);
#25148=ADVANCED_FACE('',(#3042,#1317),#1696,.F.);
#25149=ADVANCED_FACE('',(#3043),#1697,.T.);
#25169=CLOSED_SHELL('',(#25095,#25096,#25097,#25098,#25099,#25100,#25101,
#25102,#25103,#25104,#25105,#25106,#25107,#25108,#25109,#25110,#25111,#25112,
#25113,#25114,#25115,#25116,#25117,#25118,#25119,#25120,#25121,#25122,#25123,
#25124,#25125,#25126,#25127,#25128,#25129,#25130,#25131,#25132,#25133,#25134,
#25135,#25136,#25137,#25138,#25139,#25140,#25141,#25142,#25143,#25144,#25145,
#25146,#25147,#25148,#25149));
#27176=AXIS2_PLACEMENT_3D('',#256108,#32030,#32031);
#27177=AXIS2_PLACEMENT_3D('',#256109,#32032,#32033);
#27178=AXIS2_PLACEMENT_3D('',#256125,#32035,#32036);
#27179=AXIS2_PLACEMENT_3D('',#256133,#32037,#32038);
#27180=AXIS2_PLACEMENT_3D('',#256181,#32040,#32041);
#27181=AXIS2_PLACEMENT_3D('',#256229,#32043,#32044);
#27182=AXIS2_PLACEMENT_3D('',#256280,#32046,#32047);
#27183=AXIS2_PLACEMENT_3D('',#256331,#32049,#32050);
#27184=AXIS2_PLACEMENT_3D('',#256379,#32052,#32053);
#27185=AXIS2_PLACEMENT_3D('',#256427,#32055,#32056);
#27186=AXIS2_PLACEMENT_3D('',#256481,#32058,#32059);
#27187=AXIS2_PLACEMENT_3D('',#256529,#32061,#32062);
#27188=AXIS2_PLACEMENT_3D('',#256577,#32064,#32065);
#27189=AXIS2_PLACEMENT_3D('',#256631,#32067,#32068);
#27190=AXIS2_PLACEMENT_3D('',#256679,#32070,#32071);
#27191=AXIS2_PLACEMENT_3D('',#256727,#32073,#32074);
#27192=AXIS2_PLACEMENT_3D('',#256775,#32076,#32077);
#27193=AXIS2_PLACEMENT_3D('',#256829,#32079,#32080);
#27194=AXIS2_PLACEMENT_3D('',#256877,#32082,#32083);
#27195=AXIS2_PLACEMENT_3D('',#256925,#32085,#32086);
#27196=AXIS2_PLACEMENT_3D('',#256979,#32088,#32089);
#27197=AXIS2_PLACEMENT_3D('',#257027,#32091,#32092);
#27198=AXIS2_PLACEMENT_3D('',#257075,#32094,#32095);
#27199=AXIS2_PLACEMENT_3D('',#257087,#32097,#32098);
#27200=AXIS2_PLACEMENT_3D('',#257092,#32099,#32100);
#27201=AXIS2_PLACEMENT_3D('',#257117,#32102,#32103);
#27202=AXIS2_PLACEMENT_3D('',#257141,#32105,#32106);
#27203=AXIS2_PLACEMENT_3D('',#257166,#32108,#32109);
#27204=AXIS2_PLACEMENT_3D('',#257191,#32111,#32112);
#27205=AXIS2_PLACEMENT_3D('',#257215,#32114,#32115);
#27206=AXIS2_PLACEMENT_3D('',#257240,#32117,#32118);
#27207=AXIS2_PLACEMENT_3D('',#257265,#32120,#32121);
#27208=AXIS2_PLACEMENT_3D('',#257289,#32123,#32124);
#27209=AXIS2_PLACEMENT_3D('',#257313,#32126,#32127);
#27210=AXIS2_PLACEMENT_3D('',#257338,#32129,#32130);
#27211=AXIS2_PLACEMENT_3D('',#257363,#32132,#32133);
#27212=AXIS2_PLACEMENT_3D('',#257387,#32135,#32136);
#27213=AXIS2_PLACEMENT_3D('',#257412,#32138,#32139);
#27214=AXIS2_PLACEMENT_3D('',#257437,#32141,#32142);
#27215=AXIS2_PLACEMENT_3D('',#257461,#32144,#32145);
#27216=AXIS2_PLACEMENT_3D('',#257486,#32147,#32148);
#27217=AXIS2_PLACEMENT_3D('',#257510,#32150,#32151);
#27218=AXIS2_PLACEMENT_3D('',#257535,#32153,#32154);
#27219=AXIS2_PLACEMENT_3D('',#258298,#32156,#32157);
#27220=AXIS2_PLACEMENT_3D('',#258300,#32158,#32159);
#27221=AXIS2_PLACEMENT_3D('',#259035,#32160,#32161);
#27222=AXIS2_PLACEMENT_3D('',#259036,#32162,#32163);
#27223=AXIS2_PLACEMENT_3D('',#259037,#32164,#32165);
#27224=AXIS2_PLACEMENT_3D('',#259046,#32170,#32171);
#27225=AXIS2_PLACEMENT_3D('',#259052,#32175,#32176);
#27226=AXIS2_PLACEMENT_3D('',#259058,#32180,#32181);
#27227=AXIS2_PLACEMENT_3D('',#259064,#32185,#32186);
#27228=AXIS2_PLACEMENT_3D('',#259070,#32190,#32191);
#27229=AXIS2_PLACEMENT_3D('',#259073,#32194,#32195);
#27230=AXIS2_PLACEMENT_3D('',#259074,#32196,#32197);
#27231=AXIS2_PLACEMENT_3D('',#259076,#32198,#32199);
#27232=AXIS2_PLACEMENT_3D('',#259077,#32200,#32201);
#27233=AXIS2_PLACEMENT_3D('',#259080,#32203,#32204);
#27234=AXIS2_PLACEMENT_3D('',#259081,#32205,#32206);
#27235=AXIS2_PLACEMENT_3D('',#259082,#32207,#32208);
#32030=DIRECTION('axis',(0.,0.,1.));
#32031=DIRECTION('refdir',(1.,0.,0.));
#32032=DIRECTION('center_axis',(0.,0.,1.));
#32033=DIRECTION('ref_axis',(1.,0.,0.));
#32034=DIRECTION('',(0.,0.,-1.));
#32035=DIRECTION('center_axis',(0.,0.,-1.));
#32036=DIRECTION('ref_axis',(1.,0.,0.));
#32037=DIRECTION('center_axis',(0.,0.,1.));
#32038=DIRECTION('ref_axis',(1.,0.,0.));
#32039=DIRECTION('',(0.,0.,-1.));
#32040=DIRECTION('center_axis',(0.,0.,1.));
#32041=DIRECTION('ref_axis',(1.,0.,0.));
#32042=DIRECTION('',(0.,0.,-1.));
#32043=DIRECTION('center_axis',(0.,0.,1.));
#32044=DIRECTION('ref_axis',(1.,0.,0.));
#32045=DIRECTION('',(0.,0.,-1.));
#32046=DIRECTION('center_axis',(0.,0.,1.));
#32047=DIRECTION('ref_axis',(1.,0.,0.));
#32048=DIRECTION('',(0.,0.,-1.));
#32049=DIRECTION('center_axis',(0.,0.,1.));
#32050=DIRECTION('ref_axis',(1.,0.,0.));
#32051=DIRECTION('',(0.,0.,-1.));
#32052=DIRECTION('center_axis',(0.,0.,1.));
#32053=DIRECTION('ref_axis',(1.,0.,0.));
#32054=DIRECTION('',(0.,0.,-1.));
#32055=DIRECTION('center_axis',(0.,0.,1.));
#32056=DIRECTION('ref_axis',(1.,0.,0.));
#32057=DIRECTION('',(0.,0.,-1.));
#32058=DIRECTION('center_axis',(0.,0.,1.));
#32059=DIRECTION('ref_axis',(1.,0.,0.));
#32060=DIRECTION('',(0.,0.,-1.));
#32061=DIRECTION('center_axis',(0.,0.,1.));
#32062=DIRECTION('ref_axis',(1.,0.,0.));
#32063=DIRECTION('',(0.,0.,-1.));
#32064=DIRECTION('center_axis',(0.,0.,1.));
#32065=DIRECTION('ref_axis',(1.,0.,0.));
#32066=DIRECTION('',(0.,0.,-1.));
#32067=DIRECTION('center_axis',(0.,0.,1.));
#32068=DIRECTION('ref_axis',(1.,0.,0.));
#32069=DIRECTION('',(0.,0.,-1.));
#32070=DIRECTION('center_axis',(0.,0.,1.));
#32071=DIRECTION('ref_axis',(1.,0.,0.));
#32072=DIRECTION('',(0.,0.,-1.));
#32073=DIRECTION('center_axis',(0.,0.,1.));
#32074=DIRECTION('ref_axis',(1.,0.,0.));
#32075=DIRECTION('',(0.,0.,-1.));
#32076=DIRECTION('center_axis',(0.,0.,1.));
#32077=DIRECTION('ref_axis',(1.,0.,0.));
#32078=DIRECTION('',(0.,0.,-1.));
#32079=DIRECTION('center_axis',(0.,0.,1.));
#32080=DIRECTION('ref_axis',(1.,0.,0.));
#32081=DIRECTION('',(0.,0.,-1.));
#32082=DIRECTION('center_axis',(0.,0.,1.));
#32083=DIRECTION('ref_axis',(1.,0.,0.));
#32084=DIRECTION('',(0.,0.,-1.));
#32085=DIRECTION('center_axis',(0.,0.,1.));
#32086=DIRECTION('ref_axis',(1.,0.,0.));
#32087=DIRECTION('',(0.,0.,-1.));
#32088=DIRECTION('center_axis',(0.,0.,1.));
#32089=DIRECTION('ref_axis',(1.,0.,0.));
#32090=DIRECTION('',(0.,0.,-1.));
#32091=DIRECTION('center_axis',(0.,0.,1.));
#32092=DIRECTION('ref_axis',(1.,0.,0.));
#32093=DIRECTION('',(0.,0.,-1.));
#32094=DIRECTION('center_axis',(0.,0.,1.));
#32095=DIRECTION('ref_axis',(-0.45780573334585,-0.889052254097401,0.));
#32096=DIRECTION('',(0.,0.,1.));
#32097=DIRECTION('center_axis',(0.,0.,1.));
#32098=DIRECTION('ref_axis',(1.,7.52212518638754E-14,0.));
#32099=DIRECTION('center_axis',(0.,0.,1.));
#32100=DIRECTION('ref_axis',(1.,7.52212518638754E-14,0.));
#32101=DIRECTION('',(0.,0.,1.));
#32102=DIRECTION('center_axis',(0.,0.,1.));
#32103=DIRECTION('ref_axis',(1.,7.52212518638754E-14,0.));
#32104=DIRECTION('',(0.,0.,1.));
#32105=DIRECTION('center_axis',(0.,0.,1.));
#32106=DIRECTION('ref_axis',(1.,7.52212518638754E-14,0.));
#32107=DIRECTION('',(0.,0.,1.));
#32108=DIRECTION('center_axis',(0.,0.,1.));
#32109=DIRECTION('ref_axis',(1.,7.52212518638754E-14,0.));
#32110=DIRECTION('',(0.,0.,1.));
#32111=DIRECTION('center_axis',(0.,0.,1.));
#32112=DIRECTION('ref_axis',(1.,7.52212518638754E-14,0.));
#32113=DIRECTION('',(0.,0.,1.));
#32114=DIRECTION('center_axis',(0.,0.,1.));
#32115=DIRECTION('ref_axis',(1.,7.52212518638754E-14,0.));
#32116=DIRECTION('',(0.,0.,1.));
#32117=DIRECTION('center_axis',(0.,0.,1.));
#32118=DIRECTION('ref_axis',(1.,7.52212518638754E-14,0.));
#32119=DIRECTION('',(0.,0.,1.));
#32120=DIRECTION('center_axis',(0.,0.,1.));
#32121=DIRECTION('ref_axis',(1.,7.52212518638754E-14,0.));
#32122=DIRECTION('',(0.,0.,1.));
#32123=DIRECTION('center_axis',(0.,0.,1.));
#32124=DIRECTION('ref_axis',(1.,7.52212518638754E-14,0.));
#32125=DIRECTION('',(0.,0.,1.));
#32126=DIRECTION('center_axis',(0.,0.,1.));
#32127=DIRECTION('ref_axis',(1.,7.52212518638754E-14,0.));
#32128=DIRECTION('',(0.,0.,1.));
#32129=DIRECTION('center_axis',(0.,0.,1.));
#32130=DIRECTION('ref_axis',(1.,7.52212518638754E-14,0.));
#32131=DIRECTION('',(0.,0.,1.));
#32132=DIRECTION('center_axis',(0.,0.,1.));
#32133=DIRECTION('ref_axis',(1.,7.52212518638754E-14,0.));
#32134=DIRECTION('',(0.,0.,1.));
#32135=DIRECTION('center_axis',(0.,0.,1.));
#32136=DIRECTION('ref_axis',(1.,7.52212518638754E-14,0.));
#32137=DIRECTION('',(0.,0.,1.));
#32138=DIRECTION('center_axis',(0.,0.,1.));
#32139=DIRECTION('ref_axis',(1.,7.52212518638754E-14,0.));
#32140=DIRECTION('',(0.,0.,1.));
#32141=DIRECTION('center_axis',(0.,0.,1.));
#32142=DIRECTION('ref_axis',(1.,7.52212518638754E-14,0.));
#32143=DIRECTION('',(0.,0.,1.));
#32144=DIRECTION('center_axis',(0.,0.,1.));
#32145=DIRECTION('ref_axis',(1.,7.52212518638754E-14,0.));
#32146=DIRECTION('',(0.,0.,1.));
#32147=DIRECTION('center_axis',(0.,0.,1.));
#32148=DIRECTION('ref_axis',(1.,7.52212518638754E-14,0.));
#32149=DIRECTION('',(0.,0.,1.));
#32150=DIRECTION('center_axis',(0.,0.,1.));
#32151=DIRECTION('ref_axis',(1.,7.52212518638754E-14,0.));
#32152=DIRECTION('',(0.,0.,1.));
#32153=DIRECTION('center_axis',(0.,0.,1.));
#32154=DIRECTION('ref_axis',(1.,7.52212518638754E-14,0.));
#32155=DIRECTION('',(0.,0.,1.));
#32156=DIRECTION('center_axis',(0.,0.,1.));
#32157=DIRECTION('ref_axis',(1.,7.52212518638754E-14,0.));
#32158=DIRECTION('center_axis',(0.,0.,-1.));
#32159=DIRECTION('ref_axis',(1.,7.52212518638754E-14,0.));
#32160=DIRECTION('center_axis',(0.,0.,1.));
#32161=DIRECTION('ref_axis',(1.,0.,0.));
#32162=DIRECTION('center_axis',(0.,0.,-1.));
#32163=DIRECTION('ref_axis',(1.,0.,0.));
#32164=DIRECTION('center_axis',(-1.92296268638356E-16,-1.,0.));
#32165=DIRECTION('ref_axis',(1.,-1.92296268638356E-16,0.));
#32166=DIRECTION('',(1.,-1.92296268638356E-16,0.));
#32167=DIRECTION('',(0.,0.,1.));
#32168=DIRECTION('',(1.,-1.92296268638356E-16,0.));
#32169=DIRECTION('',(0.,0.,1.));
#32170=DIRECTION('center_axis',(-0.866025403784439,-0.5,0.));
#32171=DIRECTION('ref_axis',(0.5,-0.866025403784439,0.));
#32172=DIRECTION('',(0.5,-0.866025403784439,0.));
#32173=DIRECTION('',(0.,0.,1.));
#32174=DIRECTION('',(0.5,-0.866025403784439,0.));
#32175=DIRECTION('center_axis',(-0.866025403784439,0.5,0.));
#32176=DIRECTION('ref_axis',(-0.5,-0.866025403784438,0.));
#32177=DIRECTION('',(-0.5,-0.866025403784438,0.));
#32178=DIRECTION('',(0.,0.,1.));
#32179=DIRECTION('',(-0.5,-0.866025403784439,0.));
#32180=DIRECTION('center_axis',(1.92296268638356E-16,1.,0.));
#32181=DIRECTION('ref_axis',(-1.,1.92296268638356E-16,0.));
#32182=DIRECTION('',(-1.,1.92296268638356E-16,0.));
#32183=DIRECTION('',(0.,0.,1.));
#32184=DIRECTION('',(-1.,1.92296268638356E-16,0.));
#32185=DIRECTION('center_axis',(0.866025403784439,0.5,0.));
#32186=DIRECTION('ref_axis',(-0.5,0.866025403784439,0.));
#32187=DIRECTION('',(-0.5,0.866025403784439,0.));
#32188=DIRECTION('',(0.,0.,1.));
#32189=DIRECTION('',(-0.5,0.866025403784439,0.));
#32190=DIRECTION('center_axis',(0.866025403784439,-0.5,0.));
#32191=DIRECTION('ref_axis',(0.5,0.866025403784439,0.));
#32192=DIRECTION('',(0.5,0.866025403784439,0.));
#32193=DIRECTION('',(0.5,0.866025403784439,0.));
#32194=DIRECTION('center_axis',(0.,0.,1.));
#32195=DIRECTION('ref_axis',(1.,0.,0.));
#32196=DIRECTION('center_axis',(0.,0.,1.));
#32197=DIRECTION('ref_axis',(1.,0.,0.));
#32198=DIRECTION('center_axis',(0.,0.,1.));
#32199=DIRECTION('ref_axis',(1.,0.,0.));
#32200=DIRECTION('center_axis',(0.,0.,1.));
#32201=DIRECTION('ref_axis',(1.,0.,0.));
#32202=DIRECTION('',(0.,0.,-1.));
#32203=DIRECTION('center_axis',(0.,0.,1.));
#32204=DIRECTION('ref_axis',(1.,0.,0.));
#32205=DIRECTION('center_axis',(0.,0.,1.));
#32206=DIRECTION('ref_axis',(1.,0.,0.));
#32207=DIRECTION('center_axis',(0.,0.,1.));
#32208=DIRECTION('ref_axis',(1.,0.,0.));
#256108=CARTESIAN_POINT('',(0.,0.,0.));
#256109=CARTESIAN_POINT('Origin',(0.,0.,0.));
#256110=CARTESIAN_POINT('',(-2.94557004194935,0.00189169806540372,0.322176117089595));
#256111=CARTESIAN_POINT('',(-2.9447355781443,0.00314069784331926,0.177823882910384));
#256112=CARTESIAN_POINT('',(-2.942,-3.60291088309151E-16,0.));
#256113=CARTESIAN_POINT('',(1.28892185405323,2.64462557919717,0.));
#256114=CARTESIAN_POINT('Ctrl Pts',(-2.94557004194935,0.00189169806540372,
0.322176117089595));
#256115=CARTESIAN_POINT('Ctrl Pts',(-2.94624968390491,0.100877667946963,
0.316802268464241));
#256116=CARTESIAN_POINT('Ctrl Pts',(-2.94169413341334,0.199796244590278,
0.311428419838886));
#256117=CARTESIAN_POINT('Ctrl Pts',(-2.93169775767856,0.298156773010515,
0.306054571213531));
#256118=CARTESIAN_POINT('Ctrl Pts',(-2.8332180086401,1.26715998088469,0.253113857695288));
#256119=CARTESIAN_POINT('Ctrl Pts',(-2.20669014063059,2.18200296465327,
0.200173144177046));
#256120=CARTESIAN_POINT('Ctrl Pts',(-1.33882305771969,2.62485694228654,
0.147232430658803));
#256121=CARTESIAN_POINT('Ctrl Pts',(-0.534286740179597,3.03539458726557,
0.0981549537725353));
#256122=CARTESIAN_POINT('Ctrl Pts',(0.477651495878826,3.0403146643246,0.0490774768862676));
#256123=CARTESIAN_POINT('Ctrl Pts',(1.29201717055307,2.64849452802569,4.33680868994202E-18));
#256124=CARTESIAN_POINT('',(-1.28892185405326,2.64462557919716,0.));
#256125=CARTESIAN_POINT('Origin',(0.,0.,0.));
#256126=CARTESIAN_POINT('Ctrl Pts',(-1.28892185405326,2.64462557919716,
1.59594559789866E-15));
#256127=CARTESIAN_POINT('Ctrl Pts',(-2.16862035685409,2.21588336549516,
0.0529407135182443));
#256128=CARTESIAN_POINT('Ctrl Pts',(-2.80996338750092,1.31741950685156,
0.105881427036487));
#256129=CARTESIAN_POINT('Ctrl Pts',(-2.92551917741274,0.351793993740128,
0.15882214055473));
#256130=CARTESIAN_POINT('Ctrl Pts',(-2.93934446235059,0.236264967698149,
0.165156054673281));
#256131=CARTESIAN_POINT('Ctrl Pts',(-2.94564356378168,0.119774581438611,
0.171489968791833));
#256132=CARTESIAN_POINT('Ctrl Pts',(-2.9447355781443,0.00314069784331926,
0.177823882910384));
#256133=CARTESIAN_POINT('Origin',(0.,0.,0.));
#256134=CARTESIAN_POINT('',(-2.93798487825769,0.00155454897156224,1.3221761170896));
#256135=CARTESIAN_POINT('',(-2.93771757447194,0.00132355291632602,1.17782388291039));
#256136=CARTESIAN_POINT('',(-2.942,-3.60291088309151E-16,0.));
#256137=CARTESIAN_POINT('Ctrl Pts',(-2.93798487825769,0.00155454897156224,
1.3221761170896));
#256138=CARTESIAN_POINT('Ctrl Pts',(-2.93985103439238,0.392136713800161,
1.30111321624037));
#256139=CARTESIAN_POINT('Ctrl Pts',(-2.86747910744294,0.782054648384103,
1.28005031539114));
#256140=CARTESIAN_POINT('Ctrl Pts',(-2.71761372677595,1.13947848623566,
1.25898741454191));
#256141=CARTESIAN_POINT('Ctrl Pts',(-2.34093340904641,2.03784823785433,
1.20604670102367));
#256142=CARTESIAN_POINT('Ctrl Pts',(-1.47469049342653,2.73093749609884,
1.15310598750542));
#256143=CARTESIAN_POINT('Ctrl Pts',(-0.515567473276226,2.90137621497648,
1.10016527398718));
#256144=CARTESIAN_POINT('Ctrl Pts',(0.443555546874085,3.07181493385413,
1.04722456046894));
#256145=CARTESIAN_POINT('Ctrl Pts',(1.49555867155482,2.7196031133649,0.994283846950693));
#256146=CARTESIAN_POINT('Ctrl Pts',(2.15868031522846,2.00598891393562,0.94134313343245));
#256147=CARTESIAN_POINT('Ctrl Pts',(2.82180195890208,1.29237471450635,0.888402419914207));
#256148=CARTESIAN_POINT('Ctrl Pts',(3.09604212156861,0.217358136137037,
0.835461706395964));
#256149=CARTESIAN_POINT('Ctrl Pts',(2.85583072731624,-0.726685455261021,
0.782520992877721));
#256150=CARTESIAN_POINT('Ctrl Pts',(2.61561933306387,-1.67072904665908,
0.729580279359478));
#256151=CARTESIAN_POINT('Ctrl Pts',(1.86095638189261,-2.48379965108589,
0.676639565841234));
#256152=CARTESIAN_POINT('Ctrl Pts',(0.937402540044778,-2.79371879385104,
0.623698852322991));
#256153=CARTESIAN_POINT('Ctrl Pts',(0.0138486981969448,-3.1036379366162,
0.570758138804748));
#256154=CARTESIAN_POINT('Ctrl Pts',(-1.07859603432746,-2.91040561771969,
0.517817425286505));
#256155=CARTESIAN_POINT('Ctrl Pts',(-1.83960258555595,-2.30220774228156,
0.464876711768262));
#256156=CARTESIAN_POINT('Ctrl Pts',(-2.52336170777509,-1.75574615824684,
0.417309846875373));
#256157=CARTESIAN_POINT('Ctrl Pts',(-2.93955416034762,-0.874287104856683,
0.369742981982484));
#256158=CARTESIAN_POINT('Ctrl Pts',(-2.94557004194935,0.00189169806540372,
0.322176117089595));
#256159=CARTESIAN_POINT('Ctrl Pts',(-2.9447355781443,0.00314069784331926,
0.177823882910384));
#256160=CARTESIAN_POINT('Ctrl Pts',(-2.93805435328604,-0.85508565543347,
0.224430682310076));
#256161=CARTESIAN_POINT('Ctrl Pts',(-2.54114911827883,-1.72108159790374,
0.271037481709768));
#256162=CARTESIAN_POINT('Ctrl Pts',(-1.88115140643926,-2.26900155522438,
0.31764428110946));
#256163=CARTESIAN_POINT('Ctrl Pts',(-1.13145929637718,-2.89138442349815,
0.370584994627703));
#256164=CARTESIAN_POINT('Ctrl Pts',(-0.0423065270762356,-3.10336299246639,
0.423525708145946));
#256165=CARTESIAN_POINT('Ctrl Pts',(0.88679629592561,-2.80996731425714,
0.476466421664189));
#256166=CARTESIAN_POINT('Ctrl Pts',(1.81589911892745,-2.51657163604789,
0.529407135182432));
#256167=CARTESIAN_POINT('Ctrl Pts',(2.5849519956302,-1.71780171066114,0.582347848700675));
#256168=CARTESIAN_POINT('Ctrl Pts',(2.84215968009143,-0.778381688792158,
0.635288562218918));
#256169=CARTESIAN_POINT('Ctrl Pts',(3.09936736455265,0.161038333076827,
0.688229275737162));
#256170=CARTESIAN_POINT('Ctrl Pts',(2.84472985677235,1.24110845142804,0.741169989255405));
#256171=CARTESIAN_POINT('Ctrl Pts',(2.19465508113817,1.9666691917807,0.794110702773649));
#256172=CARTESIAN_POINT('Ctrl Pts',(1.54458030550399,2.69222993213336,0.847051416291892));
#256173=CARTESIAN_POINT('Ctrl Pts',(0.499068262015925,3.06328129448748,
0.899992129810135));
#256174=CARTESIAN_POINT('Ctrl Pts',(-0.462995013488164,2.91019332193529,
0.952932843328378));
#256175=CARTESIAN_POINT('Ctrl Pts',(-1.42505828899225,2.75710534938309,
1.00587355684662));
#256176=CARTESIAN_POINT('Ctrl Pts',(-2.30367279651237,2.0798780419246,1.05881427036486));
#256177=CARTESIAN_POINT('Ctrl Pts',(-2.69654137432937,1.18848910114619,
1.11175498388311));
#256178=CARTESIAN_POINT('Ctrl Pts',(-2.85997195339173,0.817677539756684,
1.13377795022553));
#256179=CARTESIAN_POINT('Ctrl Pts',(-2.93934411301125,0.409805269668763,
1.15580091656796));
#256180=CARTESIAN_POINT('Ctrl Pts',(-2.93771757447194,0.00132355291632602,
1.17782388291039));
#256181=CARTESIAN_POINT('Origin',(0.,0.,0.));
#256182=CARTESIAN_POINT('',(-2.93994176176976,-0.00248389711332564,2.32217611708959));
#256183=CARTESIAN_POINT('',(-2.94042627567403,-0.00258468312704599,2.17782388291038));
#256184=CARTESIAN_POINT('',(-2.942,-3.60291088309151E-16,0.));
#256185=CARTESIAN_POINT('Ctrl Pts',(-2.93994176176976,-0.00248389711332564,
2.32217611708959));
#256186=CARTESIAN_POINT('Ctrl Pts',(-2.93449635628973,0.677888284957744,
2.28542416401649));
#256187=CARTESIAN_POINT('Ctrl Pts',(-2.69945487914443,1.36165532324218,
2.24867221094339));
#256188=CARTESIAN_POINT('Ctrl Pts',(-2.26755203286641,1.88203058384677,
2.21192025787029));
#256189=CARTESIAN_POINT('Ctrl Pts',(-1.64540156355562,2.63162442281503,
2.15897954435204));
#256190=CARTESIAN_POINT('Ctrl Pts',(-0.61476315801349,3.04217982902399,
2.1060388308338));
#256191=CARTESIAN_POINT('Ctrl Pts',(0.352393429603434,2.92568781287356,
2.05309811731556));
#256192=CARTESIAN_POINT('Ctrl Pts',(1.31955001722035,2.80919579672313,2.00015740379731));
#256193=CARTESIAN_POINT('Ctrl Pts',(2.22322478691207,2.16565635821333,1.94721669027907));
#256194=CARTESIAN_POINT('Ctrl Pts',(2.64958937276608,1.28977060664693,1.89427597676083));
#256195=CARTESIAN_POINT('Ctrl Pts',(3.0759539586201,0.413884855080523,1.84133526324259));
#256196=CARTESIAN_POINT('Ctrl Pts',(3.02500836063641,-0.694347209542482,
1.78839454972434));
#256197=CARTESIAN_POINT('Ctrl Pts',(2.52008288608448,-1.52742084653071,
1.7354538362061));
#256198=CARTESIAN_POINT('Ctrl Pts',(2.01515741153255,-2.36049448351894,
1.68251312268785));
#256199=CARTESIAN_POINT('Ctrl Pts',(1.05625206041239,-2.91840969287239,
1.62957240916961));
#256200=CARTESIAN_POINT('Ctrl Pts',(0.0824866859396203,-2.94567843973959,
1.57663169565137));
#256201=CARTESIAN_POINT('Ctrl Pts',(-0.891278688533154,-2.9729471866068,
1.52369098213313));
#256202=CARTESIAN_POINT('Ctrl Pts',(-1.87990408635854,-2.46956947098774,
1.47075026861488));
#256203=CARTESIAN_POINT('Ctrl Pts',(-2.43065792535163,-1.66605549068179,
1.41780955509664));
#256204=CARTESIAN_POINT('Ctrl Pts',(-2.7622897931411,-1.18222619487337,
1.38593174242762));
#256205=CARTESIAN_POINT('Ctrl Pts',(-2.93516052960321,-0.589575095106889,
1.35405392975861));
#256206=CARTESIAN_POINT('Ctrl Pts',(-2.93798487825769,0.00155454897156224,
1.3221761170896));
#256207=CARTESIAN_POINT('Ctrl Pts',(-2.93771757447194,0.00132355291632602,
1.17782388291039));
#256208=CARTESIAN_POINT('Ctrl Pts',(-2.93543409882438,-0.572138452525019,
1.2087416300862));
#256209=CARTESIAN_POINT('Ctrl Pts',(-2.77351048623348,-1.14680161491326,
1.23965937726202));
#256210=CARTESIAN_POINT('Ctrl Pts',(-2.46041273051419,-1.62180832981924,
1.27057712443784));
#256211=CARTESIAN_POINT('Ctrl Pts',(-1.92429286076815,-2.43516624590794,
1.32351783795608));
#256212=CARTESIAN_POINT('Ctrl Pts',(-0.944930473162187,-2.95633150398703,
1.37645855147432));
#256213=CARTESIAN_POINT('Ctrl Pts',(0.029170826245073,-2.94668352979876,
1.42939926499257));
#256214=CARTESIAN_POINT('Ctrl Pts',(1.00327212565234,-2.93703555561049,
1.48233997851081));
#256215=CARTESIAN_POINT('Ctrl Pts',(1.9721123368609,-2.39657434915485,1.53528069202905));
#256216=CARTESIAN_POINT('Ctrl Pts',(2.49202933291632,-1.57277661940358,
1.5882214055473));
#256217=CARTESIAN_POINT('Ctrl Pts',(3.01194632897174,-0.74897888965232,
1.64116211906554));
#256218=CARTESIAN_POINT('Ctrl Pts',(3.08294010987402,0.358155363394565,
1.69410283258378));
#256219=CARTESIAN_POINT('Ctrl Pts',(2.67249570036986,1.24161446820423,1.74704354610203));
#256220=CARTESIAN_POINT('Ctrl Pts',(2.2620512908657,2.1250735730139,1.79998425962027));
#256221=CARTESIAN_POINT('Ctrl Pts',(1.37016869095509,2.78485752958635,1.85292497313851));
#256222=CARTESIAN_POINT('Ctrl Pts',(0.405278167142355,2.91883128448651,
1.90586568665676));
#256223=CARTESIAN_POINT('Ctrl Pts',(-0.559612356670371,3.05280503938667,
1.958806400175));
#256224=CARTESIAN_POINT('Ctrl Pts',(-1.59751080438521,2.66096859261455,
2.01174711369324));
#256225=CARTESIAN_POINT('Ctrl Pts',(-2.23312380973047,1.92275613721379,
2.06468782721148));
#256226=CARTESIAN_POINT('Ctrl Pts',(-2.6858991477565,1.39689465983959,2.10239984577778));
#256227=CARTESIAN_POINT('Ctrl Pts',(-2.9345409799455,0.695270051284926,
2.14011186434408));
#256228=CARTESIAN_POINT('Ctrl Pts',(-2.94042627567403,-0.00258468312704599,
2.17782388291038));
#256229=CARTESIAN_POINT('Origin',(0.,0.,0.));
#256230=CARTESIAN_POINT('',(-2.94682150487212,-0.000171940033828477,3.3221761170896));
#256231=CARTESIAN_POINT('',(-2.94682355286865,0.000158414420006351,3.17782388291039));
#256232=CARTESIAN_POINT('',(-2.942,-3.60291088309151E-16,0.));
#256233=CARTESIAN_POINT('Ctrl Pts',(-2.94682150487212,-0.000171940033828477,
3.3221761170896));
#256234=CARTESIAN_POINT('Ctrl Pts',(-2.9460050992064,0.964791128401366,
3.26973511179262));
#256235=CARTESIAN_POINT('Ctrl Pts',(-2.42654136012265,1.93050781252574,
3.21729410649564));
#256236=CARTESIAN_POINT('Ctrl Pts',(-1.62061705181913,2.46118498029747,
3.16485310119866));
#256237=CARTESIAN_POINT('Ctrl Pts',(-0.80701312333486,2.99691894936566,
3.11191238768042));
#256238=CARTESIAN_POINT('Ctrl Pts',(0.298536727682353,3.08928295206887,
3.05897167416218));
#256239=CARTESIAN_POINT('Ctrl Pts',(1.18975776670605,2.6959798904096,3.00603096064393));
#256240=CARTESIAN_POINT('Ctrl Pts',(2.08097880572974,2.30267682875033,2.95309024712569));
#256241=CARTESIAN_POINT('Ctrl Pts',(2.75787103275992,1.42370670272858,2.90014953360745));
#256242=CARTESIAN_POINT('Ctrl Pts',(2.91045888477416,0.461584467135937,
2.84720882008921));
#256243=CARTESIAN_POINT('Ctrl Pts',(3.0630467367884,-0.500537768456714,
2.79426810657096));
#256244=CARTESIAN_POINT('Ctrl Pts',(2.69133021378669,-1.54581211362026,
2.74132739305272));
#256245=CARTESIAN_POINT('Ctrl Pts',(1.96553293045783,-2.19556632026221,
2.68838667953447));
#256246=CARTESIAN_POINT('Ctrl Pts',(1.23973564712899,-2.84532052690416,
2.63544596601623));
#256247=CARTESIAN_POINT('Ctrl Pts',(0.159857603473006,-3.09955459502451,
2.58250525249799));
#256248=CARTESIAN_POINT('Ctrl Pts',(-0.779582606380496,-2.84184481832332,
2.52956453897975));
#256249=CARTESIAN_POINT('Ctrl Pts',(-1.719022816234,-2.58413504162213,2.4766238254615));
#256250=CARTESIAN_POINT('Ctrl Pts',(-2.51802519228503,-1.81448142009939,
2.42368311194326));
#256251=CARTESIAN_POINT('Ctrl Pts',(-2.81069511377083,-0.885338473474232,
2.37074239842502));
#256252=CARTESIAN_POINT('Ctrl Pts',(-2.90019075773866,-0.601215506808447,
2.35455363797988));
#256253=CARTESIAN_POINT('Ctrl Pts',(-2.94234039252192,-0.302179052012372,
2.33836487753473));
#256254=CARTESIAN_POINT('Ctrl Pts',(-2.93994176176976,-0.00248389711332564,
2.32217611708959));
#256255=CARTESIAN_POINT('Ctrl Pts',(-2.94042627567403,-0.00258468312704599,
2.17782388291038));
#256256=CARTESIAN_POINT('Ctrl Pts',(-2.94280284889284,-0.284389192011812,
2.19305257786233));
#256257=CARTESIAN_POINT('Ctrl Pts',(-2.90559386610683,-0.565578959204417,
2.20828127281427));
#256258=CARTESIAN_POINT('Ctrl Pts',(-2.82625604206022,-0.834331928330834,
2.22350996776621));
#256259=CARTESIAN_POINT('Ctrl Pts',(-2.55044770606905,-1.76861907444532,
2.27645068128446));
#256260=CARTESIAN_POINT('Ctrl Pts',(-1.76550347111102,-2.55260490264487,
2.3293913948027));
#256261=CARTESIAN_POINT('Ctrl Pts',(-0.830880469484507,-2.82727233874327,
2.38233210832095));
#256262=CARTESIAN_POINT('Ctrl Pts',(0.103742532142001,-3.10193977484166,
2.43527282183919));
#256263=CARTESIAN_POINT('Ctrl Pts',(1.188044300437,-2.8672888188389,2.48821353535743));
#256264=CARTESIAN_POINT('Ctrl Pts',(1.92548059413032,-2.23077491982669,
2.54115424887567));
#256265=CARTESIAN_POINT('Ctrl Pts',(2.66291688782364,-1.59426102081447,
2.59409496239392));
#256266=CARTESIAN_POINT('Ctrl Pts',(3.05348770691528,-0.555884178792804,
2.64703567591216));
#256267=CARTESIAN_POINT('Ctrl Pts',(2.91833523468123,0.408841796814555,
2.6999763894304));
#256268=CARTESIAN_POINT('Ctrl Pts',(2.78318276244717,1.37356777242192,2.75291710294865));
#256269=CARTESIAN_POINT('Ctrl Pts',(2.1223069988874,2.26464288161497,2.80585781646689));
#256270=CARTESIAN_POINT('Ctrl Pts',(1.23834897999233,2.67400892624479,2.85879852998513));
#256271=CARTESIAN_POINT('Ctrl Pts',(0.354390961097264,3.08337497087461,
2.91173924350338));
#256272=CARTESIAN_POINT('Ctrl Pts',(-0.752649313133101,3.0110319509412,
2.96467995702162));
#256273=CARTESIAN_POINT('Ctrl Pts',(-1.57581460636975,2.49010851479218,
3.01762067053986));
#256274=CARTESIAN_POINT('Ctrl Pts',(-2.39897989960641,1.96918507864315,
3.07056138405811));
#256275=CARTESIAN_POINT('Ctrl Pts',(-2.93827021184934,0.999681226278506,
3.12350209757635));
#256276=CARTESIAN_POINT('Ctrl Pts',(-2.94672329720919,0.0255709168879045,
3.17644281109459));
#256277=CARTESIAN_POINT('Ctrl Pts',(-2.94679680281682,0.0171003328177383,
3.17690316836652));
#256278=CARTESIAN_POINT('Ctrl Pts',(-2.94683016893847,0.00862940042833639,
3.17736352563846));
#256279=CARTESIAN_POINT('Ctrl Pts',(-2.94682355286865,0.000158414420006351,
3.17782388291039));
#256280=CARTESIAN_POINT('Origin',(0.,0.,0.));
#256281=CARTESIAN_POINT('',(-2.94044650265958,0.0025882162845009,4.3221761170896));
#256282=CARTESIAN_POINT('',(-2.9399612768956,0.00248864850571281,4.17782388291038));
#256283=CARTESIAN_POINT('',(-2.942,-3.60291088309151E-16,0.));
#256284=CARTESIAN_POINT('Ctrl Pts',(-2.94044650265958,0.0025882162845009,
4.3221761170896));
#256285=CARTESIAN_POINT('Ctrl Pts',(-2.94282130517145,0.283659464351577,
4.30698677308699));
#256286=CARTESIAN_POINT('Ctrl Pts',(-2.90580786785067,0.5641179787111,4.29179742908438));
#256287=CARTESIAN_POINT('Ctrl Pts',(-2.82687388743177,0.832235035317424,
4.27660808508177));
#256288=CARTESIAN_POINT('Ctrl Pts',(-2.55175856688243,1.76672623393097,
4.22366737156353));
#256289=CARTESIAN_POINT('Ctrl Pts',(-1.76739628630419,2.55129452175516,
4.17072665804528));
#256290=CARTESIAN_POINT('Ctrl Pts',(-0.832977367533957,2.82665523805142,
4.11778594452704));
#256291=CARTESIAN_POINT('Ctrl Pts',(0.101441551236281,3.10201595434767,
4.0648452310088));
#256292=CARTESIAN_POINT('Ctrl Pts',(1.18591710819853,2.86816909911599,4.01190451749056));
#256293=CARTESIAN_POINT('Ctrl Pts',(1.92382531476357,2.23220234016443,3.95896380397231));
#256294=CARTESIAN_POINT('Ctrl Pts',(2.6617335213286,1.59623558121286,3.90602309045407));
#256295=CARTESIAN_POINT('Ctrl Pts',(3.05307437749644,0.558148918541431,
3.85308237693583));
#256296=CARTESIAN_POINT('Ctrl Pts',(2.91863752141895,-0.406676957864641,
3.80014166341758));
#256297=CARTESIAN_POINT('Ctrl Pts',(2.78420066534145,-1.37150283427072,
3.74720094989934));
#256298=CARTESIAN_POINT('Ctrl Pts',(2.12398609701859,-2.26306792441144,
3.6942602363811));
#256299=CARTESIAN_POINT('Ctrl Pts',(1.24033202067288,-2.67308952506278,
3.64131952286285));
#256300=CARTESIAN_POINT('Ctrl Pts',(0.356677944327172,-3.08311112571411,
3.58837880934461));
#256301=CARTESIAN_POINT('Ctrl Pts',(-0.750415640041392,-3.01158923687608,
3.53543809582637));
#256302=CARTESIAN_POINT('Ctrl Pts',(-1.57396706019169,-2.49127654439024,
3.48249738230812));
#256303=CARTESIAN_POINT('Ctrl Pts',(-2.39751848034199,-1.97096385190439,
3.42955666878988));
#256304=CARTESIAN_POINT('Ctrl Pts',(-2.93752773627403,-1.00186035577074,
3.37661595527164));
#256305=CARTESIAN_POINT('Ctrl Pts',(-2.94670336126438,-0.0277566399873261,
3.3236752417534));
#256306=CARTESIAN_POINT('Ctrl Pts',(-2.94678997013189,-0.0185620598089631,
3.32317553353213));
#256307=CARTESIAN_POINT('Ctrl Pts',(-2.94682928436873,-0.00936703413595167,
3.32267582531086));
#256308=CARTESIAN_POINT('Ctrl Pts',(-2.94682150487212,-0.000171940033828477,
3.3221761170896));
#256309=CARTESIAN_POINT('Ctrl Pts',(-2.94682355286865,0.000158414420006351,
3.17782388291039));
#256310=CARTESIAN_POINT('Ctrl Pts',(-2.94606932626624,-0.965527131525665,
3.2303042391567));
#256311=CARTESIAN_POINT('Ctrl Pts',(-2.42571392052528,-1.93190949916178,
3.28278459540301));
#256312=CARTESIAN_POINT('Ctrl Pts',(-1.61879111254203,-2.46238651897324,
3.33526495164932));
#256313=CARTESIAN_POINT('Ctrl Pts',(-0.80478998403827,-2.99751687902722,
3.38820566516757));
#256314=CARTESIAN_POINT('Ctrl Pts',(0.300828131446,-3.08906083271863,3.44114637868581));
#256315=CARTESIAN_POINT('Ctrl Pts',(1.19175723997081,-2.6950967957953,3.49408709220405));
#256316=CARTESIAN_POINT('Ctrl Pts',(2.08268634849563,-2.30113275887196,
3.5470278057223));
#256317=CARTESIAN_POINT('Ctrl Pts',(2.75892645006097,-1.42166073133388,
3.59996851924054));
#256318=CARTESIAN_POINT('Ctrl Pts',(2.91080061718145,-0.459425531762414,
3.65290923275878));
#256319=CARTESIAN_POINT('Ctrl Pts',(3.06267478430194,0.502809667809053,
3.70584994627703));
#256320=CARTESIAN_POINT('Ctrl Pts',(2.69018301697755,1.54780803941391,3.75879065979527));
#256321=CARTESIAN_POINT('Ctrl Pts',(1.96390393916053,2.19702375199443,3.81173137331351));
#256322=CARTESIAN_POINT('Ctrl Pts',(1.23762486134351,2.84623946457495,3.86467208683175));
#256323=CARTESIAN_POINT('Ctrl Pts',(0.157558473033873,3.09967251813113,
3.91761280035));
#256324=CARTESIAN_POINT('Ctrl Pts',(-0.781690369275895,2.84126595357656,
3.97055351386824));
#256325=CARTESIAN_POINT('Ctrl Pts',(-1.72093921158567,2.58285938902198,
4.02349422738649));
#256326=CARTESIAN_POINT('Ctrl Pts',(-2.51937050789556,1.81261320635664,
4.07643494090473));
#256327=CARTESIAN_POINT('Ctrl Pts',(-2.81135118077459,0.883253411949605,
4.12937565442297));
#256328=CARTESIAN_POINT('Ctrl Pts',(-2.90041902927571,0.599754930508779,
4.14552506391878));
#256329=CARTESIAN_POINT('Ctrl Pts',(-2.94235976611751,0.301450336487282,
4.16167447341458));
#256330=CARTESIAN_POINT('Ctrl Pts',(-2.9399612768956,0.00248864850571281,
4.17782388291038));
#256331=CARTESIAN_POINT('Origin',(0.,0.,0.));
#256332=CARTESIAN_POINT('',(-2.93771571390321,-0.00129109254332599,5.3221761170896));
#256333=CARTESIAN_POINT('',(-2.93797409250287,-0.00154122909697584,5.17782388291039));
#256334=CARTESIAN_POINT('',(-2.942,-3.60291088309151E-16,0.));
#256335=CARTESIAN_POINT('Ctrl Pts',(-2.93771571390321,-0.00129109254332599,
5.3221761170896));
#256336=CARTESIAN_POINT('Ctrl Pts',(-2.93545056844751,0.571435936275613,
5.29129772086311));
#256337=CARTESIAN_POINT('Ctrl Pts',(-2.7739600267295,1.14534299189815,5.26041932463663));
#256338=CARTESIAN_POINT('Ctrl Pts',(-2.46161048164032,1.61997066829654,
5.22954092841015));
#256339=CARTESIAN_POINT('Ctrl Pts',(-1.92609018897895,2.4337152572233,5.17660021489191));
#256340=CARTESIAN_POINT('Ctrl Pts',(-0.947123281983236,2.95563036559962,
5.12365950137366));
#256341=CARTESIAN_POINT('Ctrl Pts',(0.0269828091199985,2.94671054864219,
5.07071878785542));
#256342=CARTESIAN_POINT('Ctrl Pts',(1.00108890022323,2.93779073168476,5.01777807433718));
#256343=CARTESIAN_POINT('Ctrl Pts',(1.97033417543399,2.39803598939359,4.96483736081894));
#256344=CARTESIAN_POINT('Ctrl Pts',(2.4908631218815,1.57462123620547,4.91189664730069));
#256345=CARTESIAN_POINT('Ctrl Pts',(3.01139206832902,0.751206483017347,
4.85895593378245));
#256346=CARTESIAN_POINT('Ctrl Pts',(3.08320468601329,-0.355868281067734,
4.8060152202642));
#256347=CARTESIAN_POINT('Ctrl Pts',(2.67341515431747,-1.23963000210775,
4.75307450674596));
#256348=CARTESIAN_POINT('Ctrl Pts',(2.26362562262165,-2.12339172314776,
4.70013379322772));
#256349=CARTESIAN_POINT('Ctrl Pts',(1.37223394154574,-2.78384040114272,
4.64719307970947));
#256350=CARTESIAN_POINT('Ctrl Pts',(0.407443402759136,-2.91853062396757,
4.59425236619123));
#256351=CARTESIAN_POINT('Ctrl Pts',(-0.55734713602746,-3.05322084679241,
4.54131165267299));
#256352=CARTESIAN_POINT('Ctrl Pts',(-1.59553653252474,-2.66215261444716,
4.48837093915474));
#256353=CARTESIAN_POINT('Ctrl Pts',(-2.23169705051315,-1.92441144357309,
4.4354302256365));
#256354=CARTESIAN_POINT('Ctrl Pts',(-2.68533526559998,-1.39833731842992,
4.39767885612087));
#256355=CARTESIAN_POINT('Ctrl Pts',(-2.93454420384162,-0.695982080377398,
4.35992748660523));
#256356=CARTESIAN_POINT('Ctrl Pts',(-2.94044650265958,0.0025882162845009,
4.3221761170896));
#256357=CARTESIAN_POINT('Ctrl Pts',(-2.9399612768956,0.00248864850571281,
4.17782388291038));
#256358=CARTESIAN_POINT('Ctrl Pts',(-2.93449708043811,-0.678600672837507,
4.21461518693282));
#256359=CARTESIAN_POINT('Ctrl Pts',(-2.69890715531692,-1.36310038808667,
4.25140649095526));
#256360=CARTESIAN_POINT('Ctrl Pts',(-2.26615555049358,-1.88371204593479,
4.2881977949777));
#256361=CARTESIAN_POINT('Ctrl Pts',(-1.64344919788537,-2.63284430326346,
4.34113850849594));
#256362=CARTESIAN_POINT('Ctrl Pts',(-0.612506443220769,-3.04263541177207,
4.39407922201419));
#256363=CARTESIAN_POINT('Ctrl Pts',(0.354563499507598,-2.92542591366007,
4.44701993553243));
#256364=CARTESIAN_POINT('Ctrl Pts',(1.32163344223596,-2.80821641554808,
4.49996064905067));
#256365=CARTESIAN_POINT('Ctrl Pts',(2.22483057302809,-2.16400631081546,
4.55290136256892));
#256366=CARTESIAN_POINT('Ctrl Pts',(2.65054542067995,-1.28780473063139,
4.60584207608716));
#256367=CARTESIAN_POINT('Ctrl Pts',(3.07626026833181,-0.411603150447325,
4.65878278960541));
#256368=CARTESIAN_POINT('Ctrl Pts',(3.02449283284339,0.696589905188196,
4.71172350312365));
#256369=CARTESIAN_POINT('Ctrl Pts',(2.51894945793883,1.52928927271612,4.76466421664189));
#256370=CARTESIAN_POINT('Ctrl Pts',(2.01340608303427,2.36198864024403,4.81760493016013));
#256371=CARTESIAN_POINT('Ctrl Pts',(1.05408676871357,2.91919431966434,4.87054564367837));
#256372=CARTESIAN_POINT('Ctrl Pts',(0.0803015401539713,2.94573992640351,
4.92348635719662));
#256373=CARTESIAN_POINT('Ctrl Pts',(-0.893483688405635,2.97228553314268,
4.97642707071486));
#256374=CARTESIAN_POINT('Ctrl Pts',(-1.88173483120415,2.46817106720069,
5.02936778423311));
#256375=CARTESIAN_POINT('Ctrl Pts',(-2.43189284146947,1.66425035945319,
5.08230849775135));
#256376=CARTESIAN_POINT('Ctrl Pts',(-2.76275700225513,1.18077371211907,
5.11414695947103));
#256377=CARTESIAN_POINT('Ctrl Pts',(-2.93517161021586,0.588863123642047,
5.14598542119071));
#256378=CARTESIAN_POINT('Ctrl Pts',(-2.93797409250287,-0.00154122909697584,
5.17782388291039));
#256379=CARTESIAN_POINT('Origin',(0.,0.,0.));
#256380=CARTESIAN_POINT('',(-2.94517248244385,-0.00193699951557325,6.3221761170896));
#256381=CARTESIAN_POINT('',(-2.94559088235875,-0.00170176706889942,6.17782388291039));
#256382=CARTESIAN_POINT('',(-2.942,-3.60291088309151E-16,0.));
#256383=CARTESIAN_POINT('Ctrl Pts',(-2.94517248244385,-0.00193699951557325,
6.3221761170896));
#256384=CARTESIAN_POINT('Ctrl Pts',(-2.9386420685114,0.856218115624555,
6.27560866863924));
#256385=CARTESIAN_POINT('Ctrl Pts',(-2.54183626857632,1.71963167034793,
6.22904122018889));
#256386=CARTESIAN_POINT('Ctrl Pts',(-1.88262592526034,2.26705773084874,
6.18247377173853));
#256387=CARTESIAN_POINT('Ctrl Pts',(-1.13319543045971,2.88940504009179,
6.12953305822029));
#256388=CARTESIAN_POINT('Ctrl Pts',(-0.0446194458096424,3.10335342402028,
6.07659234470204));
#256389=CARTESIAN_POINT('Ctrl Pts',(0.884600293036423,2.81092750725154,
6.0236516311838));
#256390=CARTESIAN_POINT('Ctrl Pts',(1.81382003188248,2.51850159048281,5.97071091766556));
#256391=CARTESIAN_POINT('Ctrl Pts',(2.58368352492452,1.71970137301683,5.91777020414732));
#256392=CARTESIAN_POINT('Ctrl Pts',(2.84164001510992,0.780328875532278,
5.86482949062907));
#256393=CARTESIAN_POINT('Ctrl Pts',(3.09959650529531,-0.159043621952279,
5.81188877711083));
#256394=CARTESIAN_POINT('Ctrl Pts',(2.84564599262406,-1.23898839945542,
5.75894806359258));
#256395=CARTESIAN_POINT('Ctrl Pts',(2.196082399727,-1.96495629037203,5.70600735007434));
#256396=CARTESIAN_POINT('Ctrl Pts',(1.54651880682993,-2.69092418128863,
5.65306663655609));
#256397=CARTESIAN_POINT('Ctrl Pts',(0.501342133707051,-3.06291518561871,
5.60012592303785));
#256398=CARTESIAN_POINT('Ctrl Pts',(-0.460820134777716,-2.91057999938971,
5.54718520951961));
#256399=CARTESIAN_POINT('Ctrl Pts',(-1.42298240326247,-2.75824481316072,
5.49424449600136));
#256400=CARTESIAN_POINT('Ctrl Pts',(-2.30213026710911,-2.08158343637267,
5.44130378248312));
#256401=CARTESIAN_POINT('Ctrl Pts',(-2.69566735986892,-1.19046571324005,
5.38836306896488));
#256402=CARTESIAN_POINT('Ctrl Pts',(-2.85966855345979,-0.819104606720612,
5.36630075167312));
#256403=CARTESIAN_POINT('Ctrl Pts',(-2.93933413855808,-0.41049904941688,
5.34423843438136));
#256404=CARTESIAN_POINT('Ctrl Pts',(-2.93771571390321,-0.00129109254332599,
5.3221761170896));
#256405=CARTESIAN_POINT('Ctrl Pts',(-2.93797409250287,-0.00154122909697584,
5.17782388291039));
#256406=CARTESIAN_POINT('Ctrl Pts',(-2.93983155306118,-0.39285603017501,
5.19892613470895));
#256407=CARTESIAN_POINT('Ctrl Pts',(-2.86717973724354,-0.783509153708209,
5.22002838650751));
#256408=CARTESIAN_POINT('Ctrl Pts',(-2.71676856184761,-1.14149053114142,
5.24113063830608));
#256409=CARTESIAN_POINT('Ctrl Pts',(-2.3394213942283,-2.03958376443549,
5.29407135182432));
#256410=CARTESIAN_POINT('Ctrl Pts',(-1.47266218125755,-2.7320432814706,
5.34701206534256));
#256411=CARTESIAN_POINT('Ctrl Pts',(-0.51341403914473,-2.90176464857968,
5.39995277886081));
#256412=CARTESIAN_POINT('Ctrl Pts',(0.445834102968095,-3.07148601568877,
5.45289349237905));
#256413=CARTESIAN_POINT('Ctrl Pts',(1.49757117422299,-2.71846923287181,
5.5058342058973));
#256414=CARTESIAN_POINT('Ctrl Pts',(2.16016542555926,-2.00437456218931,
5.55877491941554));
#256415=CARTESIAN_POINT('Ctrl Pts',(2.82275967689551,-1.29027989150683,
5.61171563293378));
#256416=CARTESIAN_POINT('Ctrl Pts',(3.09621110831315,-0.215107332958816,
5.66465634645202));
#256417=CARTESIAN_POINT('Ctrl Pts',(2.85529555990017,0.728779333507592,
5.71759705997026));
#256418=CARTESIAN_POINT('Ctrl Pts',(2.61438001148719,1.67266599997401,5.77053777348851));
#256419=CARTESIAN_POINT('Ctrl Pts',(1.85909748324357,2.48526677435882,5.82347848700676));
#256420=CARTESIAN_POINT('Ctrl Pts',(0.935321535258006,2.7944598184653,5.876419200525));
#256421=CARTESIAN_POINT('Ctrl Pts',(0.0115455872724497,3.10365286257177,
5.92935991404324));
#256422=CARTESIAN_POINT('Ctrl Pts',(-1.08072378045507,2.90943817639992,
5.98230062756148));
#256423=CARTESIAN_POINT('Ctrl Pts',(-1.84129348697169,2.30075429939171,
6.03524134107972));
#256424=CARTESIAN_POINT('Ctrl Pts',(-2.52409477409559,1.75430848237877,
6.08276885502328));
#256425=CARTESIAN_POINT('Ctrl Pts',(-2.93956117072973,0.873819286065656,
6.13029636896684));
#256426=CARTESIAN_POINT('Ctrl Pts',(-2.94559088235875,-0.00170176706889942,
6.17782388291039));
#256427=CARTESIAN_POINT('Origin',(0.,0.,0.));
#256428=CARTESIAN_POINT('',(-2.94368178595509,0.00247084038202318,7.3221761170896));
#256429=CARTESIAN_POINT('',(-2.94315318334351,0.00257818642023648,7.17782388291039));
#256430=CARTESIAN_POINT('',(-2.942,-3.60291088309151E-16,0.));
#256431=CARTESIAN_POINT('Ctrl Pts',(-2.94368178595509,0.00247084038202318,
7.3221761170896));
#256432=CARTESIAN_POINT('Ctrl Pts',(-2.94522564461956,0.17437048182408,
7.31286032993361));
#256433=CARTESIAN_POINT('Ctrl Pts',(-2.93146429530118,0.346023191581102,
7.30354454277762));
#256434=CARTESIAN_POINT('Ctrl Pts',(-2.90151816454975,0.51480430286788,
7.29422875562163));
#256435=CARTESIAN_POINT('Ctrl Pts',(-2.7313372123076,1.4739709637528,7.24128804210339));
#256436=CARTESIAN_POINT('Ctrl Pts',(-2.03846251298597,2.3403982465541,7.18834732858515));
#256437=CARTESIAN_POINT('Ctrl Pts',(-1.14018862853796,2.71731503893386,
7.13540661506691));
#256438=CARTESIAN_POINT('Ctrl Pts',(-0.241914744089952,3.09423183131363,
7.08246590154866));
#256439=CARTESIAN_POINT('Ctrl Pts',(0.861758325484441,2.98163813327185,
7.02952518803042));
#256440=CARTESIAN_POINT('Ctrl Pts',(1.6654152958735,2.43109502523739,6.97658447451217));
#256441=CARTESIAN_POINT('Ctrl Pts',(2.46907226626257,1.88055191720293,6.92364376099393));
#256442=CARTESIAN_POINT('Ctrl Pts',(2.97271313746631,0.892059399175779,
6.87070304747569));
#256443=CARTESIAN_POINT('Ctrl Pts',(2.94570095627119,-0.0817129468714171,
6.81776233395745));
#256444=CARTESIAN_POINT('Ctrl Pts',(2.91868877507608,-1.05548529291861,
6.76482162043921));
#256445=CARTESIAN_POINT('Ctrl Pts',(2.36102354148214,-2.01453746698584,
6.71188090692096));
#256446=CARTESIAN_POINT('Ctrl Pts',(1.5280820879569,-2.5196817779094,6.65894019340271));
#256447=CARTESIAN_POINT('Ctrl Pts',(0.695140634431661,-3.02482608883297,
6.60599947988447));
#256448=CARTESIAN_POINT('Ctrl Pts',(-0.413077039024869,-3.07606253661285,
6.55305876636623));
#256449=CARTESIAN_POINT('Ctrl Pts',(-1.28907449533346,-2.64992793768891,
6.50011805284799));
#256450=CARTESIAN_POINT('Ctrl Pts',(-2.16507195164203,-2.22379333876499,
6.44717733932974));
#256451=CARTESIAN_POINT('Ctrl Pts',(-2.80884919080268,-1.32028769313726,
6.3942366258115));
#256452=CARTESIAN_POINT('Ctrl Pts',(-2.92559530790742,-0.353161753044597,
6.34129591229326));
#256453=CARTESIAN_POINT('Ctrl Pts',(-2.939649783197,-0.236734346600298,
6.33492264722537));
#256454=CARTESIAN_POINT('Ctrl Pts',(-2.94606624107525,-0.119384920759988,
6.32854938215748));
#256455=CARTESIAN_POINT('Ctrl Pts',(-2.94517248244385,-0.00193699951557325,
6.3221761170896));
#256456=CARTESIAN_POINT('Ctrl Pts',(-2.94559088235875,-0.00170176706889942,
6.17782388291039));
#256457=CARTESIAN_POINT('Ctrl Pts',(-2.94627764313619,-0.101420220638511,
6.18323708248508));
#256458=CARTESIAN_POINT('Ctrl Pts',(-2.94165305741639,-0.201074225831034,
6.18865028205977));
#256459=CARTESIAN_POINT('Ctrl Pts',(-2.93150717012004,-0.300162893890445,
6.19406348163446));
#256460=CARTESIAN_POINT('Ctrl Pts',(-2.83228110144603,-1.26924314231981,
6.2470041951527));
#256461=CARTESIAN_POINT('Ctrl Pts',(-2.20495891879229,-2.18425057133397,
6.29994490867094));
#256462=CARTESIAN_POINT('Ctrl Pts',(-1.33681610983853,-2.62616730994242,
6.35288562218918));
#256463=CARTESIAN_POINT('Ctrl Pts',(-0.468673300884761,-3.06808404855088,
6.40582633570743));
#256464=CARTESIAN_POINT('Ctrl Pts',(0.640290134369015,-3.03691009675363,
6.45876704922568));
#256465=CARTESIAN_POINT('Ctrl Pts',(1.48223624520047,-2.54692123253703,
6.51170776274392));
#256466=CARTESIAN_POINT('Ctrl Pts',(2.32418235603191,-2.05693236832044,
6.56464847626216));
#256467=CARTESIAN_POINT('Ctrl Pts',(2.89911114244103,-1.1081285916845,6.6175891897804));
#256468=CARTESIAN_POINT('Ctrl Pts',(2.94374011249023,-0.135004449741251,
6.67052990329864));
#256469=CARTESIAN_POINT('Ctrl Pts',(2.98836908253944,0.838119692202002,
6.72347061681688));
#256470=CARTESIAN_POINT('Ctrl Pts',(2.50269823622873,1.83556419945258,6.77641133033513));
#256471=CARTESIAN_POINT('Ctrl Pts',(1.70913534596548,2.40056002226677,6.82935204385338));
#256472=CARTESIAN_POINT('Ctrl Pts',(0.915572455702211,2.96555584508097,
6.88229275737162));
#256473=CARTESIAN_POINT('Ctrl Pts',(-0.185882478513599,3.09810298345876,
6.93523347088986));
#256474=CARTESIAN_POINT('Ctrl Pts',(-1.09082994374658,2.7375028922651,6.9881741844081));
#256475=CARTESIAN_POINT('Ctrl Pts',(-1.99577740897954,2.37690280107145,
7.04111489792634));
#256476=CARTESIAN_POINT('Ctrl Pts',(-2.70421740522968,1.52315548030635,
7.0940556114446));
#256477=CARTESIAN_POINT('Ctrl Pts',(-2.89172740920335,0.567225389237848,
7.14699632496284));
#256478=CARTESIAN_POINT('Ctrl Pts',(-2.92812331403787,0.381678272360454,
7.15727217761202));
#256479=CARTESIAN_POINT('Ctrl Pts',(-2.94489305060584,0.19228139395339,
7.16754803026121));
#256480=CARTESIAN_POINT('Ctrl Pts',(-2.94315318334351,0.00257818642023648,
7.17782388291039));
#256481=CARTESIAN_POINT('Origin',(0.,0.,0.));
#256482=CARTESIAN_POINT('',(-2.93722985491238,0.00044505069937778,8.3221761170896));
#256483=CARTESIAN_POINT('',(-2.93717599790887,0.000154098632716083,8.17782388291039));
#256484=CARTESIAN_POINT('',(-2.942,-3.60291088309151E-16,0.));
#256485=CARTESIAN_POINT('Ctrl Pts',(-2.93722985491238,0.00044505069937778,
8.3221761170896));
#256486=CARTESIAN_POINT('Ctrl Pts',(-2.93785622278809,0.464421997225427,
8.29717127770974));
#256487=CARTESIAN_POINT('Ctrl Pts',(-2.83444790412075,0.928134993578535,
8.27216643832987));
#256488=CARTESIAN_POINT('Ctrl Pts',(-2.62552634776407,1.33807418578346,
8.24716159895001));
#256489=CARTESIAN_POINT('Ctrl Pts',(-2.18319372187359,2.20600510926297,
8.19422088543177));
#256490=CARTESIAN_POINT('Ctrl Pts',(-1.26788587165546,2.83288877045659,
8.14128017191352));
#256491=CARTESIAN_POINT('Ctrl Pts',(-0.298758242779041,2.9316504978996,
8.08833945839528));
#256492=CARTESIAN_POINT('Ctrl Pts',(0.670369386097388,3.03041222534262,
8.03539874487704));
#256493=CARTESIAN_POINT('Ctrl Pts',(1.6933167936321,2.60105201903501,7.9824580313588));
#256494=CARTESIAN_POINT('Ctrl Pts',(2.30163614951384,1.84019079573682,7.92951731784056));
#256495=CARTESIAN_POINT('Ctrl Pts',(2.90995550539557,1.07932957243865,7.87657660432231));
#256496=CARTESIAN_POINT('Ctrl Pts',(3.10364680962433,-0.0130326678500794,
7.82363589080407));
#256497=CARTESIAN_POINT('Ctrl Pts',(2.79401119992451,-0.936660314180018,
7.77069517728582));
#256498=CARTESIAN_POINT('Ctrl Pts',(2.48437559022469,-1.86028796050997,
7.71775446376758));
#256499=CARTESIAN_POINT('Ctrl Pts',(1.67141306659626,-2.61518101288112,
7.66481375024934));
#256500=CARTESIAN_POINT('Ctrl Pts',(0.727411126434527,-2.855644267517,7.61187303673109));
#256501=CARTESIAN_POINT('Ctrl Pts',(-0.21659081372719,-3.09610752215287,
7.55893232321285));
#256502=CARTESIAN_POINT('Ctrl Pts',(-1.29163217042221,-2.82214097905349,
7.50599160969461));
#256503=CARTESIAN_POINT('Ctrl Pts',(-2.00540924618839,-2.15920468801954,
7.45305089617636));
#256504=CARTESIAN_POINT('Ctrl Pts',(-2.59358553434202,-1.61292291436613,
7.40942596981411));
#256505=CARTESIAN_POINT('Ctrl Pts',(-2.93645204579212,-0.802518483014787,
7.36580104345185));
#256506=CARTESIAN_POINT('Ctrl Pts',(-2.94368178595509,0.00247084038202318,
7.3221761170896));
#256507=CARTESIAN_POINT('Ctrl Pts',(-2.94315318334351,0.00257818642023648,
7.17782388291039));
#256508=CARTESIAN_POINT('Ctrl Pts',(-2.93592933562868,-0.785060682307407,
7.22048874377945));
#256509=CARTESIAN_POINT('Ctrl Pts',(-2.60962367215334,-1.57798027204179,
7.2631536046485));
#256510=CARTESIAN_POINT('Ctrl Pts',(-2.04415356378889,-2.12256172088897,
7.30581846551756));
#256511=CARTESIAN_POINT('Ctrl Pts',(-1.34248970270355,-2.79830587857536,
7.3587591790358));
#256512=CARTESIAN_POINT('Ctrl Pts',(-0.272581968835661,-3.09168133257619,
7.41169989255405));
#256513=CARTESIAN_POINT('Ctrl Pts',(0.675616828049579,-2.86833992981832,
7.4646406060723));
#256514=CARTESIAN_POINT('Ctrl Pts',(1.62381562493482,-2.64499852706046,
7.51758131959054));
#256515=CARTESIAN_POINT('Ctrl Pts',(2.45030548483741,-1.90494026754388,
7.57052203310878));
#256516=CARTESIAN_POINT('Ctrl Pts',(2.77660421131805,-0.987066920236321,
7.62346274662702));
#256517=CARTESIAN_POINT('Ctrl Pts',(3.10290293779869,-0.0691935729287693,
7.67640346014526));
#256518=CARTESIAN_POINT('Ctrl Pts',(2.92901053085739,1.02649486216977,7.72934417366351));
#256519=CARTESIAN_POINT('Ctrl Pts',(2.33455915940062,1.79823957875268,7.78228488718175));
#256520=CARTESIAN_POINT('Ctrl Pts',(1.74010778794386,2.56998429533559,7.8352256007));
#256521=CARTESIAN_POINT('Ctrl Pts',(0.725097451971645,3.01778529340287,
7.88816631421824));
#256522=CARTESIAN_POINT('Ctrl Pts',(-0.245658715282151,2.9365768927341,
7.94110702773649));
#256523=CARTESIAN_POINT('Ctrl Pts',(-1.21641488253595,2.85536849206534,
7.99404774125473));
#256524=CARTESIAN_POINT('Ctrl Pts',(-2.14291688107131,2.24515069266052,
8.04698845477297));
#256525=CARTESIAN_POINT('Ctrl Pts',(-2.60088302465875,1.38536621273075,
8.09992916829121));
#256526=CARTESIAN_POINT('Ctrl Pts',(-2.82549366103092,0.963682771969861,
8.12589407316427));
#256527=CARTESIAN_POINT('Ctrl Pts',(-2.9374009741482,0.481967651729552,
8.15185897803733));
#256528=CARTESIAN_POINT('Ctrl Pts',(-2.93717599790887,0.000154098632716083,
8.17782388291039));
#256529=CARTESIAN_POINT('Origin',(0.,0.,0.));
#256530=CARTESIAN_POINT('',(-2.94204712377748,-0.00269013877321395,9.3221761170896));
#256531=CARTESIAN_POINT('',(-2.94258699139408,-0.00265391868664876,9.17782388291039));
#256532=CARTESIAN_POINT('',(-2.942,-3.60291088309151E-16,0.));
#256533=CARTESIAN_POINT('Ctrl Pts',(-2.94204712377748,-0.00269013877321395,
9.3221761170896));
#256534=CARTESIAN_POINT('Ctrl Pts',(-2.93512682590844,0.749287554217331,
9.28148222548586));
#256535=CARTESIAN_POINT('Ctrl Pts',(-2.6412639315254,1.50607184887019,9.24078833388212));
#256536=CARTESIAN_POINT('Ctrl Pts',(-2.12158192997297,2.04517022369181,
9.20009444227839));
#256537=CARTESIAN_POINT('Ctrl Pts',(-1.44550169088747,2.74651019130897,
9.14715372876014));
#256538=CARTESIAN_POINT('Ctrl Pts',(-0.387229252469055,3.07942314003042,
9.0942130152419));
#256539=CARTESIAN_POINT('Ctrl Pts',(0.56861083469072,2.89145514371842,9.04127230172366));
#256540=CARTESIAN_POINT('Ctrl Pts',(1.5244509218505,2.70348714740643,8.98833158820542));
#256541=CARTESIAN_POINT('Ctrl Pts',(2.37785865775163,1.99463820606099,8.93539087468717));
#256542=CARTESIAN_POINT('Ctrl Pts',(2.73802509238449,1.08951811501063,8.88245016116893));
#256543=CARTESIAN_POINT('Ctrl Pts',(3.09819152701736,0.184398023960259,
8.82950944765069));
#256544=CARTESIAN_POINT('Ctrl Pts',(2.96511666038193,-0.916993216795031,
8.77656873413245));
#256545=CARTESIAN_POINT('Ctrl Pts',(2.39974070512762,-1.71028526205923,
8.7236280206142));
#256546=CARTESIAN_POINT('Ctrl Pts',(1.83436474987331,-2.50357730732343,
8.67068730709596));
#256547=CARTESIAN_POINT('Ctrl Pts',(0.836687706000118,-2.98877015709654,
8.61774659357772));
#256548=CARTESIAN_POINT('Ctrl Pts',(-0.136414889087667,-2.94367493237596,
8.56480588005947));
#256549=CARTESIAN_POINT('Ctrl Pts',(-1.10951748417545,-2.89857970765538,
8.51186516654123));
#256550=CARTESIAN_POINT('Ctrl Pts',(-2.05804563047783,-2.32319640844112,
8.45892445302298));
#256551=CARTESIAN_POINT('Ctrl Pts',(-2.5476310028476,-1.48101566595129,
8.40598373950474));
#256552=CARTESIAN_POINT('Ctrl Pts',(-2.80597650734862,-1.03661184778483,
8.37804786536636));
#256553=CARTESIAN_POINT('Ctrl Pts',(-2.93653006500875,-0.517918670193003,
8.35011199122798));
#256554=CARTESIAN_POINT('Ctrl Pts',(-2.93722985491238,0.00044505069937778,
8.3221761170896));
#256555=CARTESIAN_POINT('Ctrl Pts',(-2.93717599790887,0.000154098632716083,
8.17782388291039));
#256556=CARTESIAN_POINT('Ctrl Pts',(-2.9369422625645,-0.500418126628262,
8.20479969155557));
#256557=CARTESIAN_POINT('Ctrl Pts',(-2.81567486845355,-1.00109659861654,
8.23177550020076));
#256558=CARTESIAN_POINT('Ctrl Pts',(-2.57401417690804,-1.43467176330002,
8.25875130884594));
#256559=CARTESIAN_POINT('Ctrl Pts',(-2.09974889693042,-2.28557409894624,
8.31169202236419));
#256560=CARTESIAN_POINT('Ctrl Pts',(-1.1617880483357,-2.87802760978395,
8.36463273588243));
#256561=CARTESIAN_POINT('Ctrl Pts',(-0.189660775246745,-2.94072454365702,
8.41757344940067));
#256562=CARTESIAN_POINT('Ctrl Pts',(0.782466497842209,-3.00342147753008,
8.47051416291892));
#256563=CARTESIAN_POINT('Ctrl Pts',(1.7887601954254,-2.53636183443847,8.52345487643716));
#256564=CARTESIAN_POINT('Ctrl Pts',(2.36839887564121,-1.75343058522299,
8.5763955899554));
#256565=CARTESIAN_POINT('Ctrl Pts',(2.94803755585702,-0.97049933600749,
8.62933630347364));
#256566=CARTESIAN_POINT('Ctrl Pts',(3.10102121870546,0.128303519331893,
8.68227701699189));
#256567=CARTESIAN_POINT('Ctrl Pts',(2.7572926311298,1.0397929590314,8.73521773051013));
#256568=CARTESIAN_POINT('Ctrl Pts',(2.41356404355414,1.9512823987309,8.78815844402838));
#256569=CARTESIAN_POINT('Ctrl Pts',(1.57312320555439,2.67545842279051,8.84109915754662));
#256570=CARTESIAN_POINT('Ctrl Pts',(0.620841014858106,2.88069236219419,
8.89403987106487));
#256571=CARTESIAN_POINT('Ctrl Pts',(-0.331441175838184,3.08592630159786,
8.94698058458311));
#256572=CARTESIAN_POINT('Ctrl Pts',(-1.395564719231,2.77221815634559,8.99992129810135));
#256573=CARTESIAN_POINT('Ctrl Pts',(-2.08422561375214,2.08322721811939,
9.05286201161959));
#256574=CARTESIAN_POINT('Ctrl Pts',(-2.62606665533224,1.54112649688225,
9.09451596871652));
#256575=CARTESIAN_POINT('Ctrl Pts',(-2.93547367882327,0.766703099201119,
9.13616992581345));
#256576=CARTESIAN_POINT('Ctrl Pts',(-2.94258699139408,-0.00265391868664876,
9.17782388291039));
#256577=CARTESIAN_POINT('Origin',(0.,0.,0.));
#256578=CARTESIAN_POINT('',(-2.946293830078,0.00114127199139325,10.3221761170896));
#256579=CARTESIAN_POINT('',(-2.94598056703706,0.00142614341313253,10.1778238829104));
#256580=CARTESIAN_POINT('',(-2.942,-3.60291088309151E-16,0.));
#256581=CARTESIAN_POINT('Ctrl Pts',(-2.946293830078,0.00114127199139325,
10.3221761170896));
#256582=CARTESIAN_POINT('Ctrl Pts',(-2.94660735229615,0.0645118181007279,
10.3187338867802));
#256583=CARTESIAN_POINT('Ctrl Pts',(-2.94474004527922,0.127863547905195,
10.3152916564709));
#256584=CARTESIAN_POINT('Ctrl Pts',(-2.94063317604738,0.19106976054023,
10.3118494261615));
#256585=CARTESIAN_POINT('Ctrl Pts',(-2.87747046817515,1.16316682986685,
10.2589087126433));
#256586=CARTESIAN_POINT('Ctrl Pts',(-2.28456764274864,2.10084365316138,
10.205967999125));
#256587=CARTESIAN_POINT('Ctrl Pts',(-1.43343821073695,2.57470115265106,
10.1530272856068));
#256588=CARTESIAN_POINT('Ctrl Pts',(-0.582308778725255,3.04855865214073,
10.1000865720885));
#256589=CARTESIAN_POINT('Ctrl Pts',(0.527047259871636,3.05859682782553,
10.0471458585703));
#256590=CARTESIAN_POINT('Ctrl Pts',(1.38661216582722,2.60021880445538,9.99420514505204));
#256591=CARTESIAN_POINT('Ctrl Pts',(2.24617707178282,2.14184078108523,9.9412644315338));
#256592=CARTESIAN_POINT('Ctrl Pts',(2.8559508450971,1.21504655866011,9.88832371801555));
#256593=CARTESIAN_POINT('Ctrl Pts',(2.93669410456063,0.244251644216089,
9.83538300449731));
#256594=CARTESIAN_POINT('Ctrl Pts',(3.01743736402416,-0.726543270227937,
9.78244229097906));
#256595=CARTESIAN_POINT('Ctrl Pts',(2.56915010963695,-1.74133887669088,
9.72950157746082));
#256596=CARTESIAN_POINT('Ctrl Pts',(1.79712069750322,-2.33542037502223,
9.67656086394258));
#256597=CARTESIAN_POINT('Ctrl Pts',(1.02509128536949,-2.92950187335358,
9.62362015042434));
#256598=CARTESIAN_POINT('Ctrl Pts',(-0.0706802845107621,-3.10286926355335,
9.57067943690609));
#256599=CARTESIAN_POINT('Ctrl Pts',(-0.988397135146327,-2.77613080251957,
9.51773872338785));
#256600=CARTESIAN_POINT('Ctrl Pts',(-1.90611398578189,-2.4493923414858,
9.4647980098696));
#256601=CARTESIAN_POINT('Ctrl Pts',(-2.64577611717277,-1.62254802921848,
9.41185729635136));
#256602=CARTESIAN_POINT('Ctrl Pts',(-2.86866316299192,-0.674242379828374,
9.35891658283312));
#256603=CARTESIAN_POINT('Ctrl Pts',(-2.92022381973027,-0.454869998218924,
9.34666976091862));
#256604=CARTESIAN_POINT('Ctrl Pts',(-2.94412978661107,-0.228997737451993,
9.33442293900411));
#256605=CARTESIAN_POINT('Ctrl Pts',(-2.94204712377748,-0.00269013877321395,
9.3221761170896));
#256606=CARTESIAN_POINT('Ctrl Pts',(-2.94258699139408,-0.00265391868664876,
9.17782388291039));
#256607=CARTESIAN_POINT('Ctrl Pts',(-2.94451444875782,-0.211122594104875,
9.1891106393317));
#256608=CARTESIAN_POINT('Ctrl Pts',(-2.92424691955225,-0.419219286159219,
9.20039739575301));
#256609=CARTESIAN_POINT('Ctrl Pts',(-2.88039456209096,-0.622221197011802,
9.21168415217432));
#256610=CARTESIAN_POINT('Ctrl Pts',(-2.67470437025918,-1.57440494271673,
9.26462486569256));
#256611=CARTESIAN_POINT('Ctrl Pts',(-1.95012574094615,-2.41449870292648,
9.3175655792108));
#256612=CARTESIAN_POINT('Ctrl Pts',(-1.03847171194,-2.75779052047728,9.37050629272905));
#256613=CARTESIAN_POINT('Ctrl Pts',(-0.126817682933869,-3.10108233802808,
9.42344700624729));
#256614=CARTESIAN_POINT('Ctrl Pts',(0.971911745765368,-2.94757221291993,
9.47638771976554));
#256615=CARTESIAN_POINT('Ctrl Pts',(1.7545651773389,-2.36755846597369,9.52932843328378));
#256616=CARTESIAN_POINT('Ctrl Pts',(2.53721860891243,-1.78754471902744,
9.58226914680202));
#256617=CARTESIAN_POINT('Ctrl Pts',(3.00379604336026,-0.781027350243069,
9.63520986032027));
#256618=CARTESIAN_POINT('Ctrl Pts',(2.94063333213535,0.191069770682194,
9.68815057383851));
#256619=CARTESIAN_POINT('Ctrl Pts',(2.87747062091044,1.16316689160746,9.74109128735675));
#256620=CARTESIAN_POINT('Ctrl Pts',(2.28456776401279,2.10084376467362,9.794032000875));
#256621=CARTESIAN_POINT('Ctrl Pts',(1.43343828682337,2.57470128931549,9.84697271439324));
#256622=CARTESIAN_POINT('Ctrl Pts',(0.582308809633943,3.04855881395736,
9.89991342791148));
#256623=CARTESIAN_POINT('Ctrl Pts',(-0.527047287847267,3.05859699017495,
9.95285414142973));
#256624=CARTESIAN_POINT('Ctrl Pts',(-1.3866122394283,2.60021894247419,10.005794854948));
#256625=CARTESIAN_POINT('Ctrl Pts',(-2.24617719100933,2.14184089477343,
10.0587355684662));
#256626=CARTESIAN_POINT('Ctrl Pts',(-2.85595099669019,1.21504662315432,
10.1116762819844));
#256627=CARTESIAN_POINT('Ctrl Pts',(-2.93669426043952,0.244251657180776,
10.1646169955027));
#256628=CARTESIAN_POINT('Ctrl Pts',(-2.94340848296254,0.163525004292322,
10.1690192913053));
#256629=CARTESIAN_POINT('Ctrl Pts',(-2.94646457151759,0.0824940959367936,
10.1734215871078));
#256630=CARTESIAN_POINT('Ctrl Pts',(-2.94598056703706,0.00142614341313253,
10.1778238829104));
#256631=CARTESIAN_POINT('Origin',(0.,0.,0.));
#256632=CARTESIAN_POINT('',(-2.93864369880353,0.00199559307489716,11.3221761170896));
#256633=CARTESIAN_POINT('',(-2.9382951498277,0.00178522549583758,11.1778238829104));
#256634=CARTESIAN_POINT('',(-2.942,-3.60291088309151E-16,0.));
#256635=CARTESIAN_POINT('Ctrl Pts',(-2.93864369880353,0.00199559307489716,
11.3221761170896));
#256636=CARTESIAN_POINT('Ctrl Pts',(-2.94085467865027,0.356558542189881,
11.3030448345564));
#256637=CARTESIAN_POINT('Ctrl Pts',(-2.88150630694549,0.71040631434159,
11.2839135520231));
#256638=CARTESIAN_POINT('Ctrl Pts',(-2.75729248477352,1.03979290383945,
11.2647822694899));
#256639=CARTESIAN_POINT('Ctrl Pts',(-2.4135639154429,1.95128229515734,11.2118415559716));
#256640=CARTESIAN_POINT('Ctrl Pts',(-1.57312312205356,2.6754582807779,11.1589008424534));
#256641=CARTESIAN_POINT('Ctrl Pts',(-0.620840981904164,2.88069220928785,
11.1059601289351));
#256642=CARTESIAN_POINT('Ctrl Pts',(0.331441158245256,3.0859261377978,11.0530194154169));
#256643=CARTESIAN_POINT('Ctrl Pts',(1.39556464515472,2.77221800919711,11.0000787018987));
#256644=CARTESIAN_POINT('Ctrl Pts',(2.08422550312197,2.08322710754239,10.9471379883804));
#256645=CARTESIAN_POINT('Ctrl Pts',(2.77288636108922,1.39423620588766,10.8941972748622));
#256646=CARTESIAN_POINT('Ctrl Pts',(3.08608459011425,0.329962531178855,
10.8412565613439));
#256647=CARTESIAN_POINT('Ctrl Pts',(2.88039440920046,-0.622221163984446,
10.7883158478257));
#256648=CARTESIAN_POINT('Ctrl Pts',(2.67470422828667,-1.57440485914773,
10.7353751343074));
#256649=CARTESIAN_POINT('Ctrl Pts',(1.95012563743409,-2.41449857476555,
10.6824344207892));
#256650=CARTESIAN_POINT('Ctrl Pts',(1.0384716568183,-2.75779037409454,10.629493707271));
#256651=CARTESIAN_POINT('Ctrl Pts',(0.12681767620249,-3.10108217342353,
10.5765529937527));
#256652=CARTESIAN_POINT('Ctrl Pts',(-0.971911694176526,-2.94757205646368,
10.5236122802345));
#256653=CARTESIAN_POINT('Ctrl Pts',(-1.75456508420706,-2.3675583403044,
10.4706715667162));
#256654=CARTESIAN_POINT('Ctrl Pts',(-2.48632997950726,-1.82525739114296,
10.4211730835074));
#256655=CARTESIAN_POINT('Ctrl Pts',(-2.94178545241125,-0.910112662410656,
10.3716746002985));
#256656=CARTESIAN_POINT('Ctrl Pts',(-2.946293830078,0.00114127199139325,
10.3221761170896));
#256657=CARTESIAN_POINT('Ctrl Pts',(-2.94598056703706,0.00142614341313253,
10.1778238829104));
#256658=CARTESIAN_POINT('Ctrl Pts',(-2.94064407610001,-0.892405238989152,
10.2263623006261));
#256659=CARTESIAN_POINT('Ctrl Pts',(-2.50495197977583,-1.79073993959316,
10.2749007183418));
#256660=CARTESIAN_POINT('Ctrl Pts',(-1.79712079289381,-2.33542049898572,
10.3234391360574));
#256661=CARTESIAN_POINT('Ctrl Pts',(-1.02509133978096,-2.92950202885072,
10.3763798495757));
#256662=CARTESIAN_POINT('Ctrl Pts',(0.0706802882625301,-3.10286942825275,
10.4293205630939));
#256663=CARTESIAN_POINT('Ctrl Pts',(0.988397187610237,-2.77613094987577,
10.4822612766122));
#256664=CARTESIAN_POINT('Ctrl Pts',(1.90611408695794,-2.44939247149879,
10.5352019901304));
#256665=CARTESIAN_POINT('Ctrl Pts',(2.64577625760985,-1.6225481153428,10.5881427036486));
#256666=CARTESIAN_POINT('Ctrl Pts',(2.86866331525975,-0.674242415616888,
10.6410834171669));
#256667=CARTESIAN_POINT('Ctrl Pts',(3.09155037290965,0.274063284109008,
10.6940241306851));
#256668=CARTESIAN_POINT('Ctrl Pts',(2.79766231755754,1.34383032740484,10.7469648442034));
#256669=CARTESIAN_POINT('Ctrl Pts',(2.12158204258587,2.04517033224891,10.7999055577216));
#256670=CARTESIAN_POINT('Ctrl Pts',(1.4455017676142,2.74651033709298,10.8528462712399));
#256671=CARTESIAN_POINT('Ctrl Pts',(0.387229273022993,3.07942330348533,
10.9057869847581));
#256672=CARTESIAN_POINT('Ctrl Pts',(-0.568610864872497,2.89145529719602,
10.9587276982763));
#256673=CARTESIAN_POINT('Ctrl Pts',(-1.524451002768,2.70348729090671,11.0116684117946));
#256674=CARTESIAN_POINT('Ctrl Pts',(-2.37785878396776,1.99463831193572,
11.0646091253128));
#256675=CARTESIAN_POINT('Ctrl Pts',(-2.73802523771812,1.08951817284182,
11.1175498388311));
#256676=CARTESIAN_POINT('Ctrl Pts',(-2.87471076930343,0.746019143233786,
11.1376411868575));
#256677=CARTESIAN_POINT('Ctrl Pts',(-2.94035710602654,0.374252114952768,
11.157732534884));
#256678=CARTESIAN_POINT('Ctrl Pts',(-2.9382951498277,0.00178522549583758,
11.1778238829104));
#256679=CARTESIAN_POINT('Origin',(0.,0.,0.));
#256680=CARTESIAN_POINT('',(-2.9390533811986,-0.0021916646264461,12.3221761170896));
#256681=CARTESIAN_POINT('',(-2.93947917419302,-0.0023511949260692,12.1778238829104));
#256682=CARTESIAN_POINT('',(-2.942,-3.60291088309151E-16,0.));
#256683=CARTESIAN_POINT('Ctrl Pts',(-2.9390533811986,-0.0021916646264461,
12.3221761170896));
#256684=CARTESIAN_POINT('Ctrl Pts',(-2.93459418397931,0.64291277294828,
12.2873557823325));
#256685=CARTESIAN_POINT('Ctrl Pts',(-2.7255434646052,1.29064511658111,12.2525354475754));
#256686=CARTESIAN_POINT('Ctrl Pts',(-2.33455903548297,1.79823948330255,
12.2177151128183));
#256687=CARTESIAN_POINT('Ctrl Pts',(-1.74010769557955,2.5699841589215,12.1647743993));
#256688=CARTESIAN_POINT('Ctrl Pts',(-0.725097413483787,3.01778513321968,
12.1118336857818));
#256689=CARTESIAN_POINT('Ctrl Pts',(0.245658702242558,2.93657673686146,
12.0588929722635));
#256690=CARTESIAN_POINT('Ctrl Pts',(1.21641481796892,2.85536834050325,12.0059522587453));
#256691=CARTESIAN_POINT('Ctrl Pts',(2.14291676732584,2.24515057348865,11.953011545227));
#256692=CARTESIAN_POINT('Ctrl Pts',(2.6008828866046,1.38536613919598,11.9000708317088));
#256693=CARTESIAN_POINT('Ctrl Pts',(3.05884900588334,0.525581704903325,
11.8471301181905));
#256694=CARTESIAN_POINT('Ctrl Pts',(3.0482792950839,-0.583769396667378,
11.7941894046723));
#256695=CARTESIAN_POINT('Ctrl Pts',(2.57401404028016,-1.43467168714797,
11.7412486911541));
#256696=CARTESIAN_POINT('Ctrl Pts',(2.09974878547643,-2.28557397762857,
11.6883079776358));
#256697=CARTESIAN_POINT('Ctrl Pts',(1.16178798666839,-2.87802745701906,
11.6353672641176));
#256698=CARTESIAN_POINT('Ctrl Pts',(0.189660765179664,-2.94072438756421,
11.5824265505993));
#256699=CARTESIAN_POINT('Ctrl Pts',(-0.782466456309061,-3.00342131810935,
11.5294858370811));
#256700=CARTESIAN_POINT('Ctrl Pts',(-1.78876010047849,-2.53636169980915,
11.4765451235628));
#256701=CARTESIAN_POINT('Ctrl Pts',(-2.36839874992726,-1.75343049215143,
11.4236044100446));
#256702=CARTESIAN_POINT('Ctrl Pts',(-2.73857231980224,-1.25342856788223,
11.3897949790596));
#256703=CARTESIAN_POINT('Ctrl Pts',(-2.93473638258426,-0.624599698542917,
11.3559855480746));
#256704=CARTESIAN_POINT('Ctrl Pts',(-2.93864369880353,0.00199559307489716,
11.3221761170896));
#256705=CARTESIAN_POINT('Ctrl Pts',(-2.9382951498277,0.00178522549583758,
11.1778238829104));
#256706=CARTESIAN_POINT('Ctrl Pts',(-2.93492385026559,-0.607198351378453,
11.2106732484022));
#256707=CARTESIAN_POINT('Ctrl Pts',(-2.75055292297376,-1.21805281595107,
11.243522613894));
#256708=CARTESIAN_POINT('Ctrl Pts',(-2.3997408325051,-1.71028535284078,
11.2763719793858));
#256709=CARTESIAN_POINT('Ctrl Pts',(-1.83436484724077,-2.50357744021265,
11.329312692904));
#256710=CARTESIAN_POINT('Ctrl Pts',(-0.836687750411167,-2.98877031573962,
11.3822534064223));
#256711=CARTESIAN_POINT('Ctrl Pts',(0.136414896328608,-2.94367508862538,
11.4351941199405));
#256712=CARTESIAN_POINT('Ctrl Pts',(1.10951754306841,-2.89857986151113,
11.4881348334588));
#256713=CARTESIAN_POINT('Ctrl Pts',(2.05804573971839,-2.32319653175565,
11.541075546977));
#256714=CARTESIAN_POINT('Ctrl Pts',(2.54763113807518,-1.48101574456307,
11.5940162604953));
#256715=CARTESIAN_POINT('Ctrl Pts',(3.03721653643197,-0.638834957370519,
11.6469569740135));
#256716=CARTESIAN_POINT('Ctrl Pts',(3.06785913649561,0.470143287259109,
11.6998976875318));
#256717=CARTESIAN_POINT('Ctrl Pts',(2.62552648712622,1.33807425680813,11.75283840105));
#256718=CARTESIAN_POINT('Ctrl Pts',(2.18319383775683,2.20600522635714,11.8057791145682));
#256719=CARTESIAN_POINT('Ctrl Pts',(1.2678859389544,2.83288892082555,11.8587198280865));
#256720=CARTESIAN_POINT('Ctrl Pts',(0.298758258636965,2.93165065351078,
11.9116605416047));
#256721=CARTESIAN_POINT('Ctrl Pts',(-0.670369421680497,3.03041238619601,
11.964601255123));
#256722=CARTESIAN_POINT('Ctrl Pts',(-1.69331688351297,2.60105215709804,
12.0175419686412));
#256723=CARTESIAN_POINT('Ctrl Pts',(-2.3016362716841,1.84019089341353,12.0704826821594));
#256724=CARTESIAN_POINT('Ctrl Pts',(-2.71277374495007,1.32595678623232,
12.1062630824098));
#256725=CARTESIAN_POINT('Ctrl Pts',(-2.93451578093251,0.66029833662526,
12.1420434826601));
#256726=CARTESIAN_POINT('Ctrl Pts',(-2.93947917419302,-0.00235119492606921,
12.1778238829104));
#256727=CARTESIAN_POINT('Origin',(0.,0.,0.));
#256728=CARTESIAN_POINT('',(-2.9465548750618,-0.00082129130520664,13.3221761170896));
#256729=CARTESIAN_POINT('',(-2.94672861832122,-0.000503025179204854,13.1778238829104));
#256730=CARTESIAN_POINT('',(-2.942,-3.60291088309151E-16,0.));
#256731=CARTESIAN_POINT('Ctrl Pts',(-2.9465548750618,-0.00082129130520664,
13.3221761170896));
#256732=CARTESIAN_POINT('Ctrl Pts',(-2.94311022400094,0.928823737220892,
13.2716667301086));
#256733=CARTESIAN_POINT('Ctrl Pts',(-2.46625336580265,1.86151179281048,
13.2211573431276));
#256734=CARTESIAN_POINT('Ctrl Pts',(-1.70913525524513,2.4005598948457,13.1706479561466));
#256735=CARTESIAN_POINT('Ctrl Pts',(-0.915572407103973,2.9655556876701,
13.1177072426284));
#256736=CARTESIAN_POINT('Ctrl Pts',(0.185882468646932,3.09810281901236,
13.0647665291101));
#256737=CARTESIAN_POINT('Ctrl Pts',(1.09082988584557,2.73750274695927,13.0118258155919));
#256738=CARTESIAN_POINT('Ctrl Pts',(1.99577730304421,2.37690267490618,12.9588851020737));
#256739=CARTESIAN_POINT('Ctrl Pts',(2.70421726169058,1.52315539945775,12.9059443885554));
#256740=CARTESIAN_POINT('Ctrl Pts',(2.8917272557113,0.567225359129726,12.8530036750372));
#256741=CARTESIAN_POINT('Ctrl Pts',(3.07923724973201,-0.388704681198295,
12.8000629615189));
#256742=CARTESIAN_POINT('Ctrl Pts',(2.74581727912706,-1.4468174864059,12.7471222480007));
#256743=CARTESIAN_POINT('Ctrl Pts',(2.04415345528584,-2.12256160822399,
12.6941815344824));
#256744=CARTESIAN_POINT('Ctrl Pts',(1.34248963144462,-2.79830573004207,
12.6412408209642));
#256745=CARTESIAN_POINT('Ctrl Pts',(0.272581954367126,-3.09168116847064,
12.588300107446));
#256746=CARTESIAN_POINT('Ctrl Pts',(-0.675616792187998,-2.86833977756768,
12.5353593939277));
#256747=CARTESIAN_POINT('Ctrl Pts',(-1.62381553874312,-2.64499838666472,
12.4824186804095));
#256748=CARTESIAN_POINT('Ctrl Pts',(-2.45030535477588,-1.90494016643023,
12.4294779668912));
#256749=CARTESIAN_POINT('Ctrl Pts',(-2.77660406393669,-0.98706686784313,
12.376537253373));
#256750=CARTESIAN_POINT('Ctrl Pts',(-2.88828854656504,-0.672900119421985,
12.3584168746119));
#256751=CARTESIAN_POINT('Ctrl Pts',(-2.94137393162258,-0.337901726889642,
12.3402964958507));
#256752=CARTESIAN_POINT('Ctrl Pts',(-2.9390533811986,-0.0021916646264461,
12.3221761170896));
#256753=CARTESIAN_POINT('Ctrl Pts',(-2.93947917419302,-0.00235119492606921,
12.1778238829104));
#256754=CARTESIAN_POINT('Ctrl Pts',(-2.94185962222118,-0.320158527116781,
12.1949841961783));
#256755=CARTESIAN_POINT('Ctrl Pts',(-2.89437728571495,-0.637273756843844,
12.2121445094463));
#256756=CARTESIAN_POINT('Ctrl Pts',(-2.79401134822979,-0.936660363897793,
12.2293048227142));
#256757=CARTESIAN_POINT('Ctrl Pts',(-2.48437572209456,-1.86028805925362,
12.2822455362324));
#256758=CARTESIAN_POINT('Ctrl Pts',(-1.67141315531429,-2.61518115169423,
12.3351862497507));
#256759=CARTESIAN_POINT('Ctrl Pts',(-0.727411165045203,-2.8556444190938,
12.3881269632689));
#256760=CARTESIAN_POINT('Ctrl Pts',(0.216590825223855,-3.09610768649335,
12.4410676767871));
#256761=CARTESIAN_POINT('Ctrl Pts',(1.29163223898172,-2.82214112885189,
12.4940083903054));
#256762=CARTESIAN_POINT('Ctrl Pts',(2.00540935263496,-2.15920480262948,
12.5469491038236));
#256763=CARTESIAN_POINT('Ctrl Pts',(2.71918646628823,-1.49626847640703,
12.5998898173419));
#256764=CARTESIAN_POINT('Ctrl Pts',(3.07169927983683,-0.444362381603572,
12.6528305308601));
#256765=CARTESIAN_POINT('Ctrl Pts',(2.90151831856148,0.514804330193662,
12.7057712443784));
#256766=CARTESIAN_POINT('Ctrl Pts',(2.73133735728613,1.47397104199087,12.7587119578966));
#256767=CARTESIAN_POINT('Ctrl Pts',(2.03846262118687,2.34039837078186,12.8116526714149));
#256768=CARTESIAN_POINT('Ctrl Pts',(1.14018868905871,2.71731518316822,12.8645933849331));
#256769=CARTESIAN_POINT('Ctrl Pts',(0.241914756930561,3.09423199555458,
12.9175340984513));
#256770=CARTESIAN_POINT('Ctrl Pts',(-0.861758371226483,2.9816382915363,
12.9704748119696));
#256771=CARTESIAN_POINT('Ctrl Pts',(-1.6654153842734,2.43109515427912,13.0234155254878));
#256772=CARTESIAN_POINT('Ctrl Pts',(-2.44673818273382,1.89585201237694,
13.074884977962));
#256773=CARTESIAN_POINT('Ctrl Pts',(-2.94448848959189,0.946663066484181,
13.1263544304362));
#256774=CARTESIAN_POINT('Ctrl Pts',(-2.94672861832122,-0.000503025179204854,
13.1778238829104));
#256775=CARTESIAN_POINT('Origin',(0.,0.,0.));
#256776=CARTESIAN_POINT('',(-2.94148383545301,0.00269085865063343,14.3221761170896));
#256777=CARTESIAN_POINT('',(-2.94096005475604,0.00265658997900563,14.1778238829104));
#256778=CARTESIAN_POINT('',(-2.942,-3.60291088309151E-16,0.));
#256779=CARTESIAN_POINT('Ctrl Pts',(-2.94148383545301,0.00269085865063343,
14.3221761170896));
#256780=CARTESIAN_POINT('Ctrl Pts',(-2.94370082512592,0.247798640329141,
14.308918391403));
#256781=CARTESIAN_POINT('Ctrl Pts',(-2.91562689752491,0.492405641969356,
14.2956606657164));
#256782=CARTESIAN_POINT('Ctrl Pts',(-2.85529540834193,0.728779294824118,
14.2824029400297));
#256783=CARTESIAN_POINT('Ctrl Pts',(-2.6143798727167,1.67266591118932,14.2294622265115));
#256784=CARTESIAN_POINT('Ctrl Pts',(-1.85909738456329,2.48526664244153,
14.1765215129932));
#256785=CARTESIAN_POINT('Ctrl Pts',(-0.935321485611485,2.79445967013616,
14.123580799475));
#256786=CARTESIAN_POINT('Ctrl Pts',(-0.0115455866596831,3.10365269783079,
14.0706400859568));
#256787=CARTESIAN_POINT('Ctrl Pts',(1.0807237230905,2.90943802196782,14.0176993724385));
#256788=CARTESIAN_POINT('Ctrl Pts',(1.84129338923632,2.30075417726838,13.9647586589203));
#256789=CARTESIAN_POINT('Ctrl Pts',(2.60186305538213,1.69207033256895,13.911817945402));
#256790=CARTESIAN_POINT('Ctrl Pts',(3.0307330779236,0.668917319033036,13.8588772318838));
#256791=CARTESIAN_POINT('Ctrl Pts',(2.9315070145165,-0.300162877957828,
13.8059365183655));
#256792=CARTESIAN_POINT('Ctrl Pts',(2.8322809511094,-1.26924307494871,13.7529958048473));
#256793=CARTESIAN_POINT('Ctrl Pts',(2.20495880175375,-2.18425045539455,
13.7000550913291));
#256794=CARTESIAN_POINT('Ctrl Pts',(1.33681603888075,-2.62616717054621,
13.6471143778108));
#256795=CARTESIAN_POINT('Ctrl Pts',(0.468673276007757,-3.06808388569787,
13.5941736642926));
#256796=CARTESIAN_POINT('Ctrl Pts',(-0.640290100382566,-3.03690993555533,
13.5412329507743));
#256797=CARTESIAN_POINT('Ctrl Pts',(-1.48223616652377,-2.54692109734721,
13.4882922372561));
#256798=CARTESIAN_POINT('Ctrl Pts',(-2.32418223266497,-2.05693225913909,
13.4353515237378));
#256799=CARTESIAN_POINT('Ctrl Pts',(-2.89911098855705,-1.10812853286539,
13.3824108102196));
#256800=CARTESIAN_POINT('Ctrl Pts',(-2.94373995623737,-0.135004442575269,
13.3294700967013));
#256801=CARTESIAN_POINT('Ctrl Pts',(-2.94578956203676,-0.0903132726320247,
13.3270387701641));
#256802=CARTESIAN_POINT('Ctrl Pts',(-2.9467206872412,-0.045570807448204,
13.3246074436268));
#256803=CARTESIAN_POINT('Ctrl Pts',(-2.9465548750618,-0.00082129130520664,
13.3221761170896));
#256804=CARTESIAN_POINT('Ctrl Pts',(-2.94672861832122,-0.000503025179204854,
13.1778238829104));
#256805=CARTESIAN_POINT('Ctrl Pts',(-2.94679265269451,-0.0275778920356812,
13.1792951439544));
#256806=CARTESIAN_POINT('Ctrl Pts',(-2.94645180088631,-0.0546511059983106,
13.1807664049985));
#256807=CARTESIAN_POINT('Ctrl Pts',(-2.94570111262815,-0.0817129512087959,
13.1822376660426));
#256808=CARTESIAN_POINT('Ctrl Pts',(-2.91868892999921,-1.05548534894355,
13.2351783795608));
#256809=CARTESIAN_POINT('Ctrl Pts',(-2.36102366680452,-2.01453757391699,
13.2881190930791));
#256810=CARTESIAN_POINT('Ctrl Pts',(-1.52808216906697,-2.51968191165344,
13.3410598065973));
#256811=CARTESIAN_POINT('Ctrl Pts',(-0.695140671329426,-3.02482624938989,
13.3940005201155));
#256812=CARTESIAN_POINT('Ctrl Pts',(0.413077060950985,-3.07606269988935,
13.4469412336338));
#256813=CARTESIAN_POINT('Ctrl Pts',(1.28907456375725,-2.64992807834628,
13.499881947152));
#256814=CARTESIAN_POINT('Ctrl Pts',(2.16507206656352,-2.22379345680322,
13.5528226606703));
#256815=CARTESIAN_POINT('Ctrl Pts',(2.80884933989565,-1.32028776321762,
13.6057633741885));
#256816=CARTESIAN_POINT('Ctrl Pts',(2.92559546319719,-0.35316177179018,
13.6587040877068));
#256817=CARTESIAN_POINT('Ctrl Pts',(3.04234158649873,0.613964219637249,
13.711644801225));
#256818=CARTESIAN_POINT('Ctrl Pts',(2.63205655976973,1.64471050890651,13.7645855147432));
#256819=CARTESIAN_POINT('Ctrl Pts',(1.88262602518954,2.26705785118355,13.8175262282615));
#256820=CARTESIAN_POINT('Ctrl Pts',(1.13319549060933,2.88940519346061,13.8704669417797));
#256821=CARTESIAN_POINT('Ctrl Pts',(0.0446194481779108,3.10335358874539,
13.923407655298));
#256822=CARTESIAN_POINT('Ctrl Pts',(-0.884600339990867,2.81092765645473,
13.9763483688162));
#256823=CARTESIAN_POINT('Ctrl Pts',(-1.81382012815963,2.51850172416407,
14.0292890823345));
#256824=CARTESIAN_POINT('Ctrl Pts',(-2.58368366206577,1.71970146429798,
14.0822297958527));
#256825=CARTESIAN_POINT('Ctrl Pts',(-2.84164016594338,0.780328916951795,
14.1351705093709));
#256826=CARTESIAN_POINT('Ctrl Pts',(-2.91091712618578,0.528050437297014,
14.1493883005507));
#256827=CARTESIAN_POINT('Ctrl Pts',(-2.94327288914735,0.265633208115812,
14.1636060917306));
#256828=CARTESIAN_POINT('Ctrl Pts',(-2.94096005475604,0.00265658997900563,
14.1778238829104));
#256829=CARTESIAN_POINT('Origin',(0.,0.,0.));
#256830=CARTESIAN_POINT('',(-2.9373430723748,-0.000745847102335828,15.3221761170896));
#256831=CARTESIAN_POINT('',(-2.93750327725234,-0.00102280351065573,15.1778238829104));
#256832=CARTESIAN_POINT('',(-2.942,-3.60291088309151E-16,0.));
#256833=CARTESIAN_POINT('Ctrl Pts',(-2.9373430723748,-0.000745847102335828,
15.3221761170896));
#256834=CARTESIAN_POINT('Ctrl Pts',(-2.93612524862381,0.536324027848074,
15.2932293391791));
#256835=CARTESIAN_POINT('Ctrl Pts',(-2.79536892737495,1.07398814293945,
15.2642825612686));
#256836=CARTESIAN_POINT('Ctrl Pts',(-2.51894932423377,1.52928919154174,
15.2353357833581));
#256837=CARTESIAN_POINT('Ctrl Pts',(-2.01340597616332,2.36198851487021,
15.1823950698399));
#256838=CARTESIAN_POINT('Ctrl Pts',(-1.05408671276304,2.91919416471434,
15.1294543563216));
#256839=CARTESIAN_POINT('Ctrl Pts',(-0.0803015358916538,2.94573977004452,
15.0765136428034));
#256840=CARTESIAN_POINT('Ctrl Pts',(0.893483640979715,2.97228537537469,
15.0235729292851));
#256841=CARTESIAN_POINT('Ctrl Pts',(1.88173473132218,2.46817093619092,14.9706322157669));
#256842=CARTESIAN_POINT('Ctrl Pts',(2.43189271238529,1.66425027111528,14.9176915022486));
#256843=CARTESIAN_POINT('Ctrl Pts',(2.9820506934484,0.860329606039647,14.8647507887304));
#256844=CARTESIAN_POINT('Ctrl Pts',(3.09411556523217,-0.243397284927852,
14.8118100752122));
#256845=CARTESIAN_POINT('Ctrl Pts',(2.71676841764234,-1.1414904705514,14.7588693616939));
#256846=CARTESIAN_POINT('Ctrl Pts',(2.33942127005251,-2.03958365617494,
14.7059286481757));
#256847=CARTESIAN_POINT('Ctrl Pts',(1.47266210308909,-2.73204313645453,
14.6529879346574));
#256848=CARTESIAN_POINT('Ctrl Pts',(0.513414011892879,-2.90176449455486,
14.6000472211392));
#256849=CARTESIAN_POINT('Ctrl Pts',(-0.445834079303328,-3.07148585265519,
14.5471065076209));
#256850=CARTESIAN_POINT('Ctrl Pts',(-1.49757109473232,-2.71846908857627,
14.4941657941027));
#256851=CARTESIAN_POINT('Ctrl Pts',(-2.16016531089828,-2.00437445579772,
14.4412250805845));
#256852=CARTESIAN_POINT('Ctrl Pts',(-2.65682877593363,-1.46910761219142,
14.4015420927528));
#256853=CARTESIAN_POINT('Ctrl Pts',(-2.93484794810006,-0.730965075081445,
14.3618591049212));
#256854=CARTESIAN_POINT('Ctrl Pts',(-2.94148383545301,0.00269085865063343,
14.3221761170896));
#256855=CARTESIAN_POINT('Ctrl Pts',(-2.94096005475604,0.00265658997900563,
14.1778238829104));
#256856=CARTESIAN_POINT('Ctrl Pts',(-2.93466092534955,-0.713574435792997,
14.2165468052488));
#256857=CARTESIAN_POINT('Ctrl Pts',(-2.67119892907313,-1.43395486703575,
14.2552697275872));
#256858=CARTESIAN_POINT('Ctrl Pts',(-2.19608251629437,-1.9649563946714,
14.2939926499257));
#256859=CARTESIAN_POINT('Ctrl Pts',(-1.54651888891863,-2.69092432412216,
14.3469333634439));
#256860=CARTESIAN_POINT('Ctrl Pts',(-0.501342160318069,-3.06291534819738,
14.3998740769621));
#256861=CARTESIAN_POINT('Ctrl Pts',(0.460820159237994,-2.91058015388245,
14.4528147904804));
#256862=CARTESIAN_POINT('Ctrl Pts',(1.42298247879406,-2.75824495956752,
14.5057555039986));
#256863=CARTESIAN_POINT('Ctrl Pts',(2.3021303893056,-2.08158354686245,14.5586962175169));
#256864=CARTESIAN_POINT('Ctrl Pts',(2.69566750295422,-1.19046577642952,
14.6116369310351));
#256865=CARTESIAN_POINT('Ctrl Pts',(3.08920461660283,-0.299348005996613,
14.6645776445534));
#256866=CARTESIAN_POINT('Ctrl Pts',(2.9971309333885,0.806226122164165,14.7175183580716));
#256867=CARTESIAN_POINT('Ctrl Pts',(2.46161061230183,1.61997075428422,14.7704590715898));
#256868=CARTESIAN_POINT('Ctrl Pts',(1.92609029121516,2.43371538640428,14.8233997851081));
#256869=CARTESIAN_POINT('Ctrl Pts',(0.947123332256163,2.95563052248365,
14.8763404986263));
#256870=CARTESIAN_POINT('Ctrl Pts',(-0.0269828105523374,2.94671070505273,
14.9292812121446));
#256871=CARTESIAN_POINT('Ctrl Pts',(-1.00108895336087,2.93779088762181,
14.9822219256628));
#256872=CARTESIAN_POINT('Ctrl Pts',(-1.97033428001888,2.39803611668058,
15.0351626391811));
#256873=CARTESIAN_POINT('Ctrl Pts',(-2.49086325409589,1.57462131978578,
15.0881033526993));
#256874=CARTESIAN_POINT('Ctrl Pts',(-2.78491630854596,1.10946443483882,
15.118010196103));
#256875=CARTESIAN_POINT('Ctrl Pts',(-2.93577251133268,0.553784388822177,
15.1479170395067));
#256876=CARTESIAN_POINT('Ctrl Pts',(-2.93750327725234,-0.00102280351065573,
15.1778238829104));
#256877=CARTESIAN_POINT('Origin',(0.,0.,0.));
#256878=CARTESIAN_POINT('',(-2.94422130955314,-0.00232131633852328,16.3221761170896));
#256879=CARTESIAN_POINT('',(-2.94470991062246,-0.00214590136519504,16.1778238829104));
#256880=CARTESIAN_POINT('',(-2.942,-3.60291088309151E-16,0.));
#256881=CARTESIAN_POINT('Ctrl Pts',(-2.94422130955314,-0.00232131633852328,
16.3221761170896));
#256882=CARTESIAN_POINT('Ctrl Pts',(-2.93710180263276,0.82093065071311,
16.2775402869552));
#256883=CARTESIAN_POINT('Ctrl Pts',(-2.57625047085104,1.64965132391019,
16.2329044568209));
#256884=CARTESIAN_POINT('Ctrl Pts',(-1.96390383491667,2.19702363537515,
16.1882686266865));
#256885=CARTESIAN_POINT('Ctrl Pts',(-1.23762479565001,2.846239313494,16.1353279131683));
#256886=CARTESIAN_POINT('Ctrl Pts',(-0.157558464670802,3.09967235360161,
16.08238719965));
#256887=CARTESIAN_POINT('Ctrl Pts',(0.781690327783711,2.84126580276401,
16.0294464861318));
#256888=CARTESIAN_POINT('Ctrl Pts',(1.72093912023825,2.5828592519264,15.9765057726135));
#256889=CARTESIAN_POINT('Ctrl Pts',(2.51937037416811,1.81261311014359,15.9235650590953));
#256890=CARTESIAN_POINT('Ctrl Pts',(2.81135103154901,0.883253365066257,
15.870624345577));
#256891=CARTESIAN_POINT('Ctrl Pts',(3.10333168892991,-0.0461063800110671,
15.8176836320588));
#256892=CARTESIAN_POINT('Ctrl Pts',(2.88886174976182,-1.1345797283829,15.7647429185406));
#256893=CARTESIAN_POINT('Ctrl Pts',(2.26615543020662,-1.8837119459476,15.7118022050223));
#256894=CARTESIAN_POINT('Ctrl Pts',(1.64344911065142,-2.63284416351231,
15.6588614915041));
#256895=CARTESIAN_POINT('Ctrl Pts',(0.612506410709106,-3.0426352502699,
15.6059207779858));
#256896=CARTESIAN_POINT('Ctrl Pts',(-0.354563480687433,-2.92542575837948,
15.5529800644676));
#256897=CARTESIAN_POINT('Ctrl Pts',(-1.32163337208394,-2.80821626648906,
15.5000393509493));
#256898=CARTESIAN_POINT('Ctrl Pts',(-2.22483045493469,-2.16400619595065,
15.4470986374311));
#256899=CARTESIAN_POINT('Ctrl Pts',(-2.65054527998976,-1.28780466227508,
15.3941579239129));
#256900=CARTESIAN_POINT('Ctrl Pts',(-2.84348892243074,-0.890690196275744,
15.3701639883051));
#256901=CARTESIAN_POINT('Ctrl Pts',(-2.93835252443724,-0.445922164696833,
15.3461700526974));
#256902=CARTESIAN_POINT('Ctrl Pts',(-2.9373430723748,-0.000745847102335828,
15.3221761170896));
#256903=CARTESIAN_POINT('Ctrl Pts',(-2.93750327725234,-0.00102280351065573,
15.1778238829104));
#256904=CARTESIAN_POINT('Ctrl Pts',(-2.93883629113328,-0.428328241075983,
15.2008577530249));
#256905=CARTESIAN_POINT('Ctrl Pts',(-2.8517098208156,-0.855115911932468,
15.2238916231395));
#256906=CARTESIAN_POINT('Ctrl Pts',(-2.67341529622153,-1.23963006790708,
15.246925493254));
#256907=CARTESIAN_POINT('Ctrl Pts',(-2.26362574277417,-2.12339183585687,
15.2998662067723));
#256908=CARTESIAN_POINT('Ctrl Pts',(-1.37223401438344,-2.78384054890816,
15.3528069202905));
#256909=CARTESIAN_POINT('Ctrl Pts',(-0.407443424386039,-2.91853077888232,
15.4057476338088));
#256910=CARTESIAN_POINT('Ctrl Pts',(0.557347165611373,-3.05322100885648,
15.458688347327));
#256911=CARTESIAN_POINT('Ctrl Pts',(1.59553661721545,-2.6621527557535,15.5116290608453));
#256912=CARTESIAN_POINT('Ctrl Pts',(2.23169716897106,-1.92441154572027,
15.5645697743635));
#256913=CARTESIAN_POINT('Ctrl Pts',(2.86785772072666,-1.18667033568704,
15.6175104878818));
#256914=CARTESIAN_POINT('Ctrl Pts',(3.1019893726338,-0.102256168723561,
15.6704512014));
#256915=CARTESIAN_POINT('Ctrl Pts',(2.82687403748138,0.832235079492427,
15.7233919149182));
#256916=CARTESIAN_POINT('Ctrl Pts',(2.55175870232897,1.76672632770841,15.7763326284365));
#256917=CARTESIAN_POINT('Ctrl Pts',(1.767396380117,2.55129465717691,15.8292733419547));
#256918=CARTESIAN_POINT('Ctrl Pts',(0.832977411748055,2.82665538808933,
15.882214055473));
#256919=CARTESIAN_POINT('Ctrl Pts',(-0.10144155662088,3.10201611900175,
15.9351547689912));
#256920=CARTESIAN_POINT('Ctrl Pts',(-1.18591717114679,2.8681692513581,15.9880954825095));
#256921=CARTESIAN_POINT('Ctrl Pts',(-1.92382541687975,2.23220245864934,
16.0410361960277));
#256922=CARTESIAN_POINT('Ctrl Pts',(-2.55935873555268,1.68446757606307,
16.0866320916553));
#256923=CARTESIAN_POINT('Ctrl Pts',(-2.93781720471667,0.838450372262618,
16.1322279872828));
#256924=CARTESIAN_POINT('Ctrl Pts',(-2.94470991062246,-0.00214590136519504,
16.1778238829104));
#256925=CARTESIAN_POINT('Origin',(0.,0.,0.));
#256926=CARTESIAN_POINT('',(-2.94469029704704,0.00215372812720598,17.3221761170896));
#256927=CARTESIAN_POINT('',(-2.94420089479508,0.00232782532028453,17.1778238829104));
#256928=CARTESIAN_POINT('',(-2.942,-3.60291088309151E-16,0.));
#256929=CARTESIAN_POINT('Ctrl Pts',(-2.94469029704704,0.00215372812720598,
17.3221761170896));
#256930=CARTESIAN_POINT('Ctrl Pts',(-2.94580943424373,0.138289047385046,
17.3147919482496));
#256931=CARTESIAN_POINT('Ctrl Pts',(-2.93718614082346,0.274281837578631,
17.3074077794096));
#256932=CARTESIAN_POINT('Ctrl Pts',(-2.91833507980263,0.408841775241091,
17.3000236105696));
#256933=CARTESIAN_POINT('Ctrl Pts',(-2.78318261475982,1.37356769973914,
17.2470828970514));
#256934=CARTESIAN_POINT('Ctrl Pts',(-2.12230688623147,2.26464276139239,
17.1941421835331));
#256935=CARTESIAN_POINT('Ctrl Pts',(-1.23834891424648,2.67400878423888,
17.1412014700149));
#256936=CARTESIAN_POINT('Ctrl Pts',(-0.354390942261467,3.08337480708537,
17.0882607564966));
#256937=CARTESIAN_POINT('Ctrl Pts',(0.752649273180203,3.01103179112507,
17.0353200429784));
#256938=CARTESIAN_POINT('Ctrl Pts',(1.57581452271761,2.49010838265651,16.9823793294601));
#256939=CARTESIAN_POINT('Ctrl Pts',(2.398979772255,1.96918497418795,16.9294386159419));
#256940=CARTESIAN_POINT('Ctrl Pts',(2.93827005588813,0.999681173211149,
16.8764979024236));
#256941=CARTESIAN_POINT('Ctrl Pts',(2.94672314080267,0.0255709155095142,
16.8235571889054));
#256942=CARTESIAN_POINT('Ctrl Pts',(2.95517622571722,-0.948539342192135,
16.7706164753872));
#256943=CARTESIAN_POINT('Ctrl Pts',(2.43279211191319,-1.92725605661859,
16.7176757618689));
#256944=CARTESIAN_POINT('Ctrl Pts',(1.61879102661444,-2.46238638825894,
16.6647350483507));
#256945=CARTESIAN_POINT('Ctrl Pts',(0.804789941315737,-2.99751671989926,
16.6117943348324));
#256946=CARTESIAN_POINT('Ctrl Pts',(-0.300828115477698,-3.08906066875349,
16.5588536213142));
#256947=CARTESIAN_POINT('Ctrl Pts',(-1.19175717671114,-2.69509665274667,
16.5059129077959));
#256948=CARTESIAN_POINT('Ctrl Pts',(-2.08268623794463,-2.30113263673982,
16.4529721942777));
#256949=CARTESIAN_POINT('Ctrl Pts',(-2.75892630361815,-1.42166065587188,
16.4000314807595));
#256950=CARTESIAN_POINT('Ctrl Pts',(-2.91080046267782,-0.459425507372839,
16.3470907672412));
#256951=CARTESIAN_POINT('Ctrl Pts',(-2.93462517330586,-0.30847834090911,
16.3387858838573));
#256952=CARTESIAN_POINT('Ctrl Pts',(-2.94554595557286,-0.155494485994484,
16.3304810004735));
#256953=CARTESIAN_POINT('Ctrl Pts',(-2.94422130955314,-0.00232131633852328,
16.3221761170896));
#256954=CARTESIAN_POINT('Ctrl Pts',(-2.94470991062246,-0.00214590136519504,
16.1778238829104));
#256955=CARTESIAN_POINT('Ctrl Pts',(-2.94582022261338,-0.137553408211996,
16.1851687008011));
#256956=CARTESIAN_POINT('Ctrl Pts',(-2.93728899802496,-0.272820250601191,
16.1925135186917));
#256957=CARTESIAN_POINT('Ctrl Pts',(-2.91863767633933,-0.40667697945158,
16.1998583365824));
#256958=CARTESIAN_POINT('Ctrl Pts',(-2.78420081312597,-1.3715029070699,
16.2527990501007));
#256959=CARTESIAN_POINT('Ctrl Pts',(-2.12398620975921,-2.26306804453264,
16.3057397636189));
#256960=CARTESIAN_POINT('Ctrl Pts',(-1.24033208650932,-2.67308966694861,
16.3586804771372));
#256961=CARTESIAN_POINT('Ctrl Pts',(-0.356677963259429,-3.08311128936457,
16.4116211906554));
#256962=CARTESIAN_POINT('Ctrl Pts',(0.75041567987361,-3.01158939673377,
16.4645619041736));
#256963=CARTESIAN_POINT('Ctrl Pts',(1.57396714373767,-2.49127667662831,
16.5175026176919));
#256964=CARTESIAN_POINT('Ctrl Pts',(2.39751860760173,-1.97096395652286,
16.5704433312101));
#256965=CARTESIAN_POINT('Ctrl Pts',(2.9375278921968,-1.00186040894278,16.6233840447284));
#256966=CARTESIAN_POINT('Ctrl Pts',(2.94670351767431,-0.0277566414570051,
16.6763247582466));
#256967=CARTESIAN_POINT('Ctrl Pts',(2.95587914315182,0.946347126028773,
16.7292654717649));
#256968=CARTESIAN_POINT('Ctrl Pts',(2.43422110951174,1.92545111342022,16.7822061852831));
#256969=CARTESIAN_POINT('Ctrl Pts',(1.62061713784133,2.46118511093008,16.8351468988013));
#256970=CARTESIAN_POINT('Ctrl Pts',(0.807013166170923,2.99691910843993,
16.8880876123196));
#256971=CARTESIAN_POINT('Ctrl Pts',(-0.298536743529821,3.0892831160682,
16.9410283258378));
#256972=CARTESIAN_POINT('Ctrl Pts',(-1.18975782985886,2.6959800335232,16.9939690393561));
#256973=CARTESIAN_POINT('Ctrl Pts',(-2.08097891618788,2.30267695097821,
17.0469097528743));
#256974=CARTESIAN_POINT('Ctrl Pts',(-2.75787117914521,1.42370677825997,
17.0998504663926));
#256975=CARTESIAN_POINT('Ctrl Pts',(-2.91045903925934,0.461584491615014,
17.1527911799108));
#256976=CARTESIAN_POINT('Ctrl Pts',(-2.93450912805829,0.309939882325946,
17.161135414244));
#256977=CARTESIAN_POINT('Ctrl Pts',(-2.94553424156564,0.156229575660569,
17.1694796485772));
#256978=CARTESIAN_POINT('Ctrl Pts',(-2.94420089479508,0.00232782532028453,
17.1778238829104));
#256979=CARTESIAN_POINT('Origin',(0.,0.,0.));
#256980=CARTESIAN_POINT('',(-2.93749488437707,0.00100976365607033,18.3221761170896));
#256981=CARTESIAN_POINT('',(-2.93733769429065,0.000733981079946969,18.1778238829104));
#256982=CARTESIAN_POINT('',(-2.942,-3.60291088309151E-16,0.));
#256983=CARTESIAN_POINT('Ctrl Pts',(-2.93749488437707,0.00100976365607033,
18.3221761170896));
#256984=CARTESIAN_POINT('Ctrl Pts',(-2.93881592843739,0.429049291744892,
18.2991028960257));
#256985=CARTESIAN_POINT('Ctrl Pts',(-2.85138007834119,0.856575277742226,
18.2760296749618));
#256986=CARTESIAN_POINT('Ctrl Pts',(-2.6724955590887,1.24161440663228,18.252956453898));
#256987=CARTESIAN_POINT('Ctrl Pts',(-2.26205117161561,2.12507346765581,
18.2000157403797));
#256988=CARTESIAN_POINT('Ctrl Pts',(-1.37016861804769,2.7848573811066,18.1470750268615));
#256989=CARTESIAN_POINT('Ctrl Pts',(-0.405278145270705,2.91883112712434,
18.0941343133433));
#256990=CARTESIAN_POINT('Ctrl Pts',(0.559612327506269,3.05280487314207,
18.041193599825));
#256991=CARTESIAN_POINT('Ctrl Pts',(1.59751071949234,2.66096845172673,17.9882528863068));
#256992=CARTESIAN_POINT('Ctrl Pts',(2.23312369097767,1.92275603651289,17.9353121727885));
#256993=CARTESIAN_POINT('Ctrl Pts',(2.868736662463,1.18454362129903,17.8823714592703));
#256994=CARTESIAN_POINT('Ctrl Pts',(3.10206421344762,0.0999552122866541,
17.829430745752));
#256995=CARTESIAN_POINT('Ctrl Pts',(2.82625589217435,-0.834331884800715,
17.7764900322338));
#256996=CARTESIAN_POINT('Ctrl Pts',(2.55044757090108,-1.76861898188808,
17.7235493187155));
#256997=CARTESIAN_POINT('Ctrl Pts',(1.76550337736993,-2.55260476705042,
17.6706086051973));
#256998=CARTESIAN_POINT('Ctrl Pts',(0.830880425304543,-2.82727218825324,
17.6176678916791));
#256999=CARTESIAN_POINT('Ctrl Pts',(-0.103742526760801,-3.10193960945605,
17.5647271781608));
#257000=CARTESIAN_POINT('Ctrl Pts',(-1.18804423736035,-2.86728866669937,
17.5117864646426));
#257001=CARTESIAN_POINT('Ctrl Pts',(-1.9254804918815,-2.23077480164964,
17.4588457511243));
#257002=CARTESIAN_POINT('Ctrl Pts',(-2.5600591638307,-1.68304186787519,
17.4132892064461));
#257003=CARTESIAN_POINT('Ctrl Pts',(-2.93778579299154,-0.837731557330954,
17.3677326617678));
#257004=CARTESIAN_POINT('Ctrl Pts',(-2.94469029704704,0.00215372812720598,
17.3221761170896));
#257005=CARTESIAN_POINT('Ctrl Pts',(-2.94420089479508,0.00232782532028453,
17.1778238829104));
#257006=CARTESIAN_POINT('Ctrl Pts',(-2.93707470812229,-0.820213336819081,
17.2224203620954));
#257007=CARTESIAN_POINT('Ctrl Pts',(-2.57693403423976,-1.64822301115232,
17.2670168412805));
#257008=CARTESIAN_POINT('Ctrl Pts',(-1.96553303478957,-2.19556643676288,
17.3116133204655));
#257009=CARTESIAN_POINT('Ctrl Pts',(-1.23973571293473,-2.84532067792415,
17.3645540339838));
#257010=CARTESIAN_POINT('Ctrl Pts',(-0.159857611954115,-3.09955475967498,
17.417494747502));
#257011=CARTESIAN_POINT('Ctrl Pts',(0.779582647763551,-2.84184496923932,
17.4704354610203));
#257012=CARTESIAN_POINT('Ctrl Pts',(1.71902290748122,-2.58413517880367,
17.5233761745385));
#257013=CARTESIAN_POINT('Ctrl Pts',(2.51802532593593,-1.81448151618153,
17.5763168880567));
#257014=CARTESIAN_POINT('Ctrl Pts',(2.81069526295745,-0.88533852033729,
17.629257601575));
#257015=CARTESIAN_POINT('Ctrl Pts',(3.10336519997896,0.04380447550691,17.6821983150932));
#257016=CARTESIAN_POINT('Ctrl Pts',(2.88970265556732,1.13243680457316,17.7351390286115));
#257017=CARTESIAN_POINT('Ctrl Pts',(2.26755215323326,1.88203068350848,17.7880797421297));
#257018=CARTESIAN_POINT('Ctrl Pts',(1.64540165089919,2.63162456244383,17.841020455648));
#257019=CARTESIAN_POINT('Ctrl Pts',(0.614763190642608,3.0421799912482,17.8939611691662));
#257020=CARTESIAN_POINT('Ctrl Pts',(-0.352393448315245,2.92568796859441,
17.9469018826845));
#257021=CARTESIAN_POINT('Ctrl Pts',(-1.3195500872731,2.80919594594063,17.9998425962027));
#257022=CARTESIAN_POINT('Ctrl Pts',(-2.22322490493229,2.16565647182868,
18.052783309721));
#257023=CARTESIAN_POINT('Ctrl Pts',(-2.6495895134013,1.2897706743402,18.1057240232392));
#257024=CARTESIAN_POINT('Ctrl Pts',(-2.84314457022158,0.892148259314461,
18.1297573097963));
#257025=CARTESIAN_POINT('Ctrl Pts',(-2.93833306961704,0.446642711850341,
18.1537905963533));
#257026=CARTESIAN_POINT('Ctrl Pts',(-2.93733769429065,0.000733981079946969,
18.1778238829104));
#257027=CARTESIAN_POINT('Origin',(0.,0.,0.));
#257028=CARTESIAN_POINT('',(-2.94091171156293,-0.00284992947760021,19.3221761170896));
#257029=CARTESIAN_POINT('',(-2.94150036975487,-0.00272063203504856,19.1778238829104));
#257030=CARTESIAN_POINT('',(-2.942,-3.60291088309151E-16,0.));
#257031=CARTESIAN_POINT('Ctrl Pts',(-2.94091171156293,-0.00284992947760021,
19.3221761170896));
#257032=CARTESIAN_POINT('Ctrl Pts',(-2.9346113934442,0.714133551483545,
19.2834138438019));
#257033=CARTESIAN_POINT('Ctrl Pts',(-2.67062843555962,1.43542617849289,
19.2446515705141));
#257034=CARTESIAN_POINT('Ctrl Pts',(-2.19465495964654,1.96666920693444,
19.2058892972264));
#257035=CARTESIAN_POINT('Ctrl Pts',(-1.54458020155545,2.69222998012506,
19.1529485837081));
#257036=CARTESIAN_POINT('Ctrl Pts',(-0.499068228844468,3.06328110544936,
19.1000078701899));
#257037=CARTESIAN_POINT('Ctrl Pts',(0.462994989182175,2.91019309689085,
19.0470671566716));
#257038=CARTESIAN_POINT('Ctrl Pts',(1.42505820720882,2.75710508833233,18.9941264431534));
#257039=CARTESIAN_POINT('Ctrl Pts',(2.3036726705511,2.07987794589101,18.9411857296351));
#257040=CARTESIAN_POINT('Ctrl Pts',(2.69654122955538,1.18848907915869,18.8882450161169));
#257041=CARTESIAN_POINT('Ctrl Pts',(3.08940978855965,0.297100212426381,
18.8353043025987));
#257042=CARTESIAN_POINT('Ctrl Pts',(2.99653244322591,-0.808450378596954,
18.7823635890804));
#257043=CARTESIAN_POINT('Ctrl Pts',(2.46041260156092,-1.62180826741871,
18.7294228755622));
#257044=CARTESIAN_POINT('Ctrl Pts',(1.92429275989593,-2.43516615624046,
18.6764821620439));
#257045=CARTESIAN_POINT('Ctrl Pts',(0.944930421899721,-2.95633134286067,
18.6235414485257));
#257046=CARTESIAN_POINT('Ctrl Pts',(-0.0291708259686788,-2.9466833598546,
18.5706007350074));
#257047=CARTESIAN_POINT('Ctrl Pts',(-1.00327207383711,-2.93703537684853,
18.5176600214892));
#257048=CARTESIAN_POINT('Ctrl Pts',(-1.97211223157771,-2.39657422421615,
18.464719307971));
#257049=CARTESIAN_POINT('Ctrl Pts',(-2.49202919975888,-1.57277654360183,
18.4117785944527));
#257050=CARTESIAN_POINT('Ctrl Pts',(-2.78535006931415,-1.10801569369011,
18.3819111019984));
#257051=CARTESIAN_POINT('Ctrl Pts',(-2.93578483819868,-0.553072708833093,
18.352043609544));
#257052=CARTESIAN_POINT('Ctrl Pts',(-2.93749488437707,0.00100976365607033,
18.3221761170896));
#257053=CARTESIAN_POINT('Ctrl Pts',(-2.93733769429065,0.000733981079946969,
18.1778238829104));
#257054=CARTESIAN_POINT('Ctrl Pts',(-2.93614044898348,-0.535608563477325,
18.2067313098716));
#257055=CARTESIAN_POINT('Ctrl Pts',(-2.79578948618625,-1.07253441221167,
18.2356387368327));
#257056=CARTESIAN_POINT('Ctrl Pts',(-2.52008301984148,-1.52742092622991,
18.2645461637939));
#257057=CARTESIAN_POINT('Ctrl Pts',(-2.01515751853378,-2.36049460844656,
18.3174868773121));
#257058=CARTESIAN_POINT('Ctrl Pts',(-1.05625211663952,-2.91840985201485,
18.3704275908304));
#257059=CARTESIAN_POINT('Ctrl Pts',(-0.0824866903648528,-2.94567859855282,
18.4233683043486));
#257060=CARTESIAN_POINT('Ctrl Pts',(0.891278735909814,-2.97294734509078,
18.4763090178669));
#257061=CARTESIAN_POINT('Ctrl Pts',(1.87990418656487,-2.46956959459843,
18.5292497313851));
#257062=CARTESIAN_POINT('Ctrl Pts',(2.43065805451983,-1.66605557474753,
18.5821904449034));
#257063=CARTESIAN_POINT('Ctrl Pts',(2.9814119224748,-0.862541554896619,
18.6351311584216));
#257064=CARTESIAN_POINT('Ctrl Pts',(3.09429420772964,0.24110873431293,18.6880718719398));
#257065=CARTESIAN_POINT('Ctrl Pts',(2.71761387062628,1.13947853899825,18.7410125854581));
#257066=CARTESIAN_POINT('Ctrl Pts',(2.34093353352292,2.03784834368356,18.7939532989763));
#257067=CARTESIAN_POINT('Ctrl Pts',(1.47469057406145,2.73093766384468,18.8468940124946));
#257068=CARTESIAN_POINT('Ctrl Pts',(0.515567501623733,2.90137638253994,
18.8998347260128));
#257069=CARTESIAN_POINT('Ctrl Pts',(-0.443555570813993,3.0718151012352,
18.9527754395311));
#257070=CARTESIAN_POINT('Ctrl Pts',(-1.49555875622791,2.71960321846454,
19.0057161530493));
#257071=CARTESIAN_POINT('Ctrl Pts',(-2.15868043210128,2.00598899678199,
19.0586568665676));
#257072=CARTESIAN_POINT('Ctrl Pts',(-2.65623216708033,1.47055182586423,
19.0983792053485));
#257073=CARTESIAN_POINT('Ctrl Pts',(-2.93485286441541,0.731653736584941,
19.1381015441295));
#257074=CARTESIAN_POINT('Ctrl Pts',(-2.94150036975487,-0.00272063203504856,
19.1778238829104));
#257075=CARTESIAN_POINT('Origin',(0.,0.,-1.84858989190501));
#257076=CARTESIAN_POINT('',(-2.3708726553023,-0.00229752557382901,19.651410108095));
#257077=CARTESIAN_POINT('',(-2.37527958827657,0.000195494738070845,19.848589891905));
#257078=CARTESIAN_POINT('',(-2.37175,-1.78696459712734E-13,-1.84858989190501));
#257079=CARTESIAN_POINT('',(1.37999437319995,-1.9337199838065,20.));
#257080=CARTESIAN_POINT('Ctrl Pts',(-2.3708726553023,-0.00229752557382881,
19.651410108095));
#257081=CARTESIAN_POINT('Ctrl Pts',(-2.37273049371058,-0.21372168288164,
19.6655885483255));
#257082=CARTESIAN_POINT('Ctrl Pts',(-2.24995196766579,-1.21237978931051,
19.7327077020742));
#257083=CARTESIAN_POINT('Ctrl Pts',(-0.889177232511419,-2.62573507798409,
19.8489043327092));
#257084=CARTESIAN_POINT('Ctrl Pts',(0.784688072628902,-2.35371694544778,
19.9509225231137));
#257085=CARTESIAN_POINT('Ctrl Pts',(1.38000112159638,-1.93372602389037,
20.));
#257086=CARTESIAN_POINT('',(-1.37702479013097,-1.93106208855768,20.));
#257087=CARTESIAN_POINT('Origin',(0.,0.,20.));
#257088=CARTESIAN_POINT('Ctrl Pts',(-2.37527958827657,0.000195494738070906,
19.848589891905));
#257089=CARTESIAN_POINT('Ctrl Pts',(-2.372659361562,-0.7471422980956,19.8990599279367));
#257090=CARTESIAN_POINT('Ctrl Pts',(-1.98938888825762,-1.49439019245293,
19.9495299639683));
#257091=CARTESIAN_POINT('Ctrl Pts',(-1.37702479013087,-1.93106208855776,
20.));
#257092=CARTESIAN_POINT('Origin',(0.,0.,-1.84858989190501));
#257093=CARTESIAN_POINT('',(-2.36811811421527,0.0008140404320815,18.651410108095));
#257094=CARTESIAN_POINT('',(-2.37134721344871,-0.00219328994902151,18.848589891905));
#257095=CARTESIAN_POINT('',(-2.37175,-1.78696459712734E-13,-1.84858989190501));
#257096=CARTESIAN_POINT('Ctrl Pts',(-2.36811811421527,0.00081404043208156,
18.651410108095));
#257097=CARTESIAN_POINT('Ctrl Pts',(-2.36673952753151,-0.44587022337695,
18.6812776005494));
#257098=CARTESIAN_POINT('Ctrl Pts',(-2.03049975964963,-1.68623441444512,
18.764085806522));
#257099=CARTESIAN_POINT('Ctrl Pts',(-0.0277579527538448,-2.80345084765341,
18.8998347260128));
#257100=CARTESIAN_POINT('Ctrl Pts',(2.3408375181597,-1.54300876944143,19.0586568665676));
#257101=CARTESIAN_POINT('Ctrl Pts',(2.56546210394684,1.13077397793403,19.2174790071223));
#257102=CARTESIAN_POINT('Ctrl Pts',(0.440526155511663,2.76865311636215,
19.376301147677));
#257103=CARTESIAN_POINT('Ctrl Pts',(-1.86232031433183,1.95137526934819,
19.5209448480012));
#257104=CARTESIAN_POINT('Ctrl Pts',(-2.36579353242733,0.57571252574142,
19.6126478348072));
#257105=CARTESIAN_POINT('Ctrl Pts',(-2.3708726553023,-0.00229752557382881,
19.651410108095));
#257106=CARTESIAN_POINT('Ctrl Pts',(-2.37134721344871,-0.00219328994902172,
18.848589891905));
#257107=CARTESIAN_POINT('Ctrl Pts',(-2.37313052894926,-0.199202713470517,
18.8618082666423));
#257108=CARTESIAN_POINT('Ctrl Pts',(-2.26053546724123,-1.1832303613783,
18.9279673548978));
#257109=CARTESIAN_POINT('Ctrl Pts',(-0.891859856974616,-2.65783582951041,
19.0470671566717));
#257110=CARTESIAN_POINT('Ctrl Pts',(1.75022653268834,-2.19050141850195,
19.2058892972263));
#257111=CARTESIAN_POINT('Ctrl Pts',(2.78914078757823,0.284026632862494,
19.3647114377811));
#257112=CARTESIAN_POINT('Ctrl Pts',(1.2738787066253,2.49658300563447,19.5235335783358));
#257113=CARTESIAN_POINT('Ctrl Pts',(-1.4087466563893,2.42611756744335,19.6823557188906));
#257114=CARTESIAN_POINT('Ctrl Pts',(-2.35782611185151,0.857292191480967,
19.7907078234136));
#257115=CARTESIAN_POINT('Ctrl Pts',(-2.37540785715971,0.0367801854735495,
19.8461192144184));
#257116=CARTESIAN_POINT('Ctrl Pts',(-2.37527958827657,0.000195494738070906,
19.848589891905));
#257117=CARTESIAN_POINT('Origin',(0.,0.,-1.84858989190501));
#257118=CARTESIAN_POINT('',(-2.3739188348135,0.00173626943759396,17.651410108095));
#257119=CARTESIAN_POINT('',(-2.36799139239764,0.000591712993054244,17.848589891905));
#257120=CARTESIAN_POINT('',(-2.37175,-1.78696459712734E-13,-1.84858989190501));
#257121=CARTESIAN_POINT('Ctrl Pts',(-2.3739188348135,0.00173626943759402,
17.651410108095));
#257122=CARTESIAN_POINT('Ctrl Pts',(-2.36835263580136,-0.675353440210703,
17.6969666527732));
#257123=CARTESIAN_POINT('Ctrl Pts',(-1.70997175802821,-2.14873683783659,
17.7954639109697));
#257124=CARTESIAN_POINT('Ctrl Pts',(0.790496683980206,-2.68985677845362,
17.9469018826844));
#257125=CARTESIAN_POINT('Ctrl Pts',(2.68889035258062,-0.793781027985773,
18.1057240232392));
#257126=CARTESIAN_POINT('Ctrl Pts',(2.1245858464136,1.82930451831788,18.2645461637939));
#257127=CARTESIAN_POINT('Ctrl Pts',(-0.385579528698175,2.7769639668139,
18.4233683043486));
#257128=CARTESIAN_POINT('Ctrl Pts',(-2.13696248834435,1.48135133436157,
18.552322952449));
#257129=CARTESIAN_POINT('Ctrl Pts',(-2.36918309934445,0.345886355437064,
18.6283368870311));
#257130=CARTESIAN_POINT('Ctrl Pts',(-2.36811811421527,0.00081404043208156,
18.651410108095));
#257131=CARTESIAN_POINT('Ctrl Pts',(-2.36799139239764,0.000591712993054314,
17.848589891905));
#257132=CARTESIAN_POINT('Ctrl Pts',(-2.36702621001918,-0.431791166019004,
17.8774973188662));
#257133=CARTESIAN_POINT('Ctrl Pts',(-2.04666419464228,-1.65736627843879,
17.9593454593456));
#257134=CARTESIAN_POINT('Ctrl Pts',(-0.0784779302164847,-2.80250647364015,
18.0941343133432));
#257135=CARTESIAN_POINT('Ctrl Pts',(2.31252045107973,-1.58508344876221,
18.252956453898));
#257136=CARTESIAN_POINT('Ctrl Pts',(2.58552714046087,1.08410340382027,18.4117785944527));
#257137=CARTESIAN_POINT('Ctrl Pts',(0.490511770879417,2.76034534307135,
18.5706007350074));
#257138=CARTESIAN_POINT('Ctrl Pts',(-1.84201218548248,1.97941362568811,
18.7162045008249));
#257139=CARTESIAN_POINT('Ctrl Pts',(-2.36598819890465,0.589836760620223,
18.8088675531241));
#257140=CARTESIAN_POINT('Ctrl Pts',(-2.37134721344871,-0.00219328994902172,
18.848589891905));
#257141=CARTESIAN_POINT('Origin',(0.,0.,-1.84858989190501));
#257142=CARTESIAN_POINT('',(-2.37354075150668,-0.00187137390417786,16.651410108095));
#257143=CARTESIAN_POINT('',(-2.37352429375602,0.00187662124489854,16.848589891905));
#257144=CARTESIAN_POINT('',(-2.37175,-1.78696459712734E-13,-1.84858989190501));
#257145=CARTESIAN_POINT('Ctrl Pts',(-2.37354075150668,-0.0018713739041778,
16.651410108095));
#257146=CARTESIAN_POINT('Ctrl Pts',(-2.37460864042485,-0.125354876668123,
16.6597149914789));
#257147=CARTESIAN_POINT('Ctrl Pts',(-2.30968224051476,-1.03487680478001,
16.720960588381));
#257148=CARTESIAN_POINT('Ctrl Pts',(-1.13383368765599,-2.56410571101671,
16.8351468988013));
#257149=CARTESIAN_POINT('Ctrl Pts',(1.54011222621193,-2.34270595503943,
16.9939690393561));
#257150=CARTESIAN_POINT('Ctrl Pts',(2.80350228934723,0.0243280702232952,
17.1527911799108));
#257151=CARTESIAN_POINT('Ctrl Pts',(1.49922452231095,2.36908059228316,17.3116133204655));
#257152=CARTESIAN_POINT('Ctrl Pts',(-1.17816089336587,2.54404274194716,
17.4704354610202));
#257153=CARTESIAN_POINT('Ctrl Pts',(-2.31802811947121,1.00713161791457,
17.5837010568967));
#257154=CARTESIAN_POINT('Ctrl Pts',(-2.37482104883331,0.111484380739378,
17.644025939255));
#257155=CARTESIAN_POINT('Ctrl Pts',(-2.3739188348135,0.00173626943759402,
17.651410108095));
#257156=CARTESIAN_POINT('Ctrl Pts',(-2.37352429375602,0.00187662124489858,
16.848589891905));
#257157=CARTESIAN_POINT('Ctrl Pts',(-2.3677793810295,-0.661230789123494,
16.8931863710901));
#257158=CARTESIAN_POINT('Ctrl Pts',(-1.73278761746912,-2.12115842707006,
16.9907235637934));
#257159=CARTESIAN_POINT('Ctrl Pts',(0.741692248419004,-2.70372151075853,
17.1412014700149));
#257160=CARTESIAN_POINT('Ctrl Pts',(2.67408584390158,-0.842308110700031,
17.3000236105696));
#257161=CARTESIAN_POINT('Ctrl Pts',(2.15734130986859,1.79055768786866,17.4588457511243));
#257162=CARTESIAN_POINT('Ctrl Pts',(-0.33526586359856,2.78348920207669,
17.6176678916791));
#257163=CARTESIAN_POINT('Ctrl Pts',(-2.12301662194415,1.51036732196377,
17.7475826052726));
#257164=CARTESIAN_POINT('Ctrl Pts',(-2.36879383340052,0.360069630125928,
17.8245566053479));
#257165=CARTESIAN_POINT('Ctrl Pts',(-2.36799139239764,0.000591712993054314,
17.848589891905));
#257166=CARTESIAN_POINT('Origin',(0.,0.,-1.84858989190501));
#257167=CARTESIAN_POINT('',(-2.36799572804382,-0.000601279016031824,15.651410108095));
#257168=CARTESIAN_POINT('',(-2.37393464667533,-0.00172995974292794,15.848589891905));
#257169=CARTESIAN_POINT('',(-2.37175,-1.78696459712734E-13,-1.84858989190501));
#257170=CARTESIAN_POINT('Ctrl Pts',(-2.36799572804382,-0.000601279016032089,
15.651410108095));
#257171=CARTESIAN_POINT('Ctrl Pts',(-2.36880951727872,-0.359488747151558,
15.6754040437027));
#257172=CARTESIAN_POINT('Ctrl Pts',(-2.12359490831044,-1.5091775280786,
15.7523386928287));
#257173=CARTESIAN_POINT('Ctrl Pts',(-0.33733047892205,-2.7832400288392,
15.882214055473));
#257174=CARTESIAN_POINT('Ctrl Pts',(2.15601250060359,-1.79215708184668,
16.0410361960277));
#257175=CARTESIAN_POINT('Ctrl Pts',(2.67470972516702,0.840324220669528,
16.1998583365824));
#257176=CARTESIAN_POINT('Ctrl Pts',(0.743697495552939,2.70317053621002,
16.3586804771371));
#257177=CARTESIAN_POINT('Ctrl Pts',(-1.7318608941197,2.12229113032217,16.509197734308));
#257178=CARTESIAN_POINT('Ctrl Pts',(-2.3678012237914,0.66180906554338,16.6067742779606));
#257179=CARTESIAN_POINT('Ctrl Pts',(-2.37354075150668,-0.0018713739041778,
16.651410108095));
#257180=CARTESIAN_POINT('Ctrl Pts',(-2.37393464667533,-0.00172995974292791,
15.848589891905));
#257181=CARTESIAN_POINT('Ctrl Pts',(-2.3748297460854,-0.110891331042623,
15.8559347097957));
#257182=CARTESIAN_POINT('Ctrl Pts',(-2.31837900116332,-1.00594618946061,
15.9162202412046));
#257183=CARTESIAN_POINT('Ctrl Pts',(-1.18004769118328,-2.54316833766063,
16.0294464861318));
#257184=CARTESIAN_POINT('Ctrl Pts',(1.49746693978282,-2.37019208118836,
16.1882686266865));
#257185=CARTESIAN_POINT('Ctrl Pts',(2.80348361626654,-0.0264075750974751,
16.3470907672412));
#257186=CARTESIAN_POINT('Ctrl Pts',(1.54184958368406,2.34156307285865,16.5059129077959));
#257187=CARTESIAN_POINT('Ctrl Pts',(-1.13193151590743,2.56494614739192,
16.6647350483507));
#257188=CARTESIAN_POINT('Ctrl Pts',(-2.30931972403911,1.03606308387966,
16.7789607097204));
#257189=CARTESIAN_POINT('Ctrl Pts',(-2.37459919695219,0.125947483369248,
16.8402456575718));
#257190=CARTESIAN_POINT('Ctrl Pts',(-2.37352429375602,0.00187662124489858,
16.848589891905));
#257191=CARTESIAN_POINT('Origin',(0.,0.,-1.84858989190501));
#257192=CARTESIAN_POINT('',(-2.37133388400261,0.00216928756102642,14.651410108095));
#257193=CARTESIAN_POINT('',(-2.36812488029342,-0.000824552762472563,14.848589891905));
#257194=CARTESIAN_POINT('',(-2.37175,-1.78696459712734E-13,-1.84858989190501));
#257195=CARTESIAN_POINT('Ctrl Pts',(-2.37133388400261,0.0021692875610264,
14.651410108095));
#257196=CARTESIAN_POINT('Ctrl Pts',(-2.36598423552219,-0.589281582877131,
14.6910930959266));
#257197=CARTESIAN_POINT('Ctrl Pts',(-1.84284323965632,-1.97822400345055,
14.7837167972765));
#257198=CARTESIAN_POINT('Ctrl Pts',(0.488460329284891,-2.7607287835619,
14.9292812121446));
#257199=CARTESIAN_POINT('Ctrl Pts',(2.58472415074527,-1.08601011698834,
15.0881033526993));
#257200=CARTESIAN_POINT('Ctrl Pts',(2.31369438223421,1.5833619975448,15.246925493254));
#257201=CARTESIAN_POINT('Ctrl Pts',(-0.0763986057193116,2.80256670978213,
15.4057476338088));
#257202=CARTESIAN_POINT('Ctrl Pts',(-2.04600918548686,1.65854908717202,
15.5405758387557));
#257203=CARTESIAN_POINT('Ctrl Pts',(-2.36701395595634,0.432367951410106,
15.6224633301845));
#257204=CARTESIAN_POINT('Ctrl Pts',(-2.36799572804382,-0.000601279016032089,
15.651410108095));
#257205=CARTESIAN_POINT('Ctrl Pts',(-2.36812488029342,-0.000824552762472806,
14.848589891905));
#257206=CARTESIAN_POINT('Ctrl Pts',(-2.36919951512415,-0.345305066544026,
14.8716237620196));
#257207=CARTESIAN_POINT('Ctrl Pts',(-2.13752525958051,-1.48015783356563,
14.9475983456523));
#257208=CARTESIAN_POINT('Ctrl Pts',(-0.387640275935778,-2.7766801689505,
15.0765136428034));
#257209=CARTESIAN_POINT('Ctrl Pts',(2.1232290291376,-1.8308785415232,15.2353357833581));
#257210=CARTESIAN_POINT('Ctrl Pts',(2.68947825967196,0.791785599022987,
15.3941579239129));
#257211=CARTESIAN_POINT('Ctrl Pts',(0.792491851405913,2.68927023744945,
15.5529800644676));
#257212=CARTESIAN_POINT('Ctrl Pts',(-1.70902747157913,2.14986441753538,
15.7044573871316));
#257213=CARTESIAN_POINT('Ctrl Pts',(-2.36837795896906,0.67593292672104,
15.8029939962775));
#257214=CARTESIAN_POINT('Ctrl Pts',(-2.37393464667533,-0.00172995974292791,
15.848589891905));
#257215=CARTESIAN_POINT('Origin',(0.,0.,-1.84858989190501));
#257216=CARTESIAN_POINT('',(-2.37542200031537,-0.00066209981418288,13.651410108095));
#257217=CARTESIAN_POINT('',(-2.37091162809913,0.0021416612107103,13.848589891905));
#257218=CARTESIAN_POINT('',(-2.37175,-1.78696459712734E-13,-1.84858989190501));
#257219=CARTESIAN_POINT('Ctrl Pts',(-2.37542200031537,-0.00066209981418278,
13.651410108095));
#257220=CARTESIAN_POINT('Ctrl Pts',(-2.37555567299943,-0.0367377846925378,
13.6538414346322));
#257221=CARTESIAN_POINT('Ctrl Pts',(-2.3584601828308,-0.858210955027421,
13.7092134746877));
#257222=CARTESIAN_POINT('Ctrl Pts',(-1.41019440296941,-2.42313199299893,
13.8175262282615));
#257223=CARTESIAN_POINT('Ctrl Pts',(1.27184219249669,-2.49852643513066,
13.9763483688162));
#257224=CARTESIAN_POINT('Ctrl Pts',(2.78902571499932,-0.285573932167581,
14.1351705093709));
#257225=CARTESIAN_POINT('Ctrl Pts',(1.75180021265799,2.18892962988587,14.2939926499257));
#257226=CARTESIAN_POINT('Ctrl Pts',(-0.889861652127881,2.65863934179406,
14.4528147904804));
#257227=CARTESIAN_POINT('Ctrl Pts',(-2.26011342652525,1.18439942316799,
14.5719539432035));
#257228=CARTESIAN_POINT('Ctrl Pts',(-2.37312115295459,0.199767649626288,
14.6381523824084));
#257229=CARTESIAN_POINT('Ctrl Pts',(-2.37133388400261,0.0021692875610264,
14.651410108095));
#257230=CARTESIAN_POINT('Ctrl Pts',(-2.37091162809913,0.0021416612107103,
13.848589891905));
#257231=CARTESIAN_POINT('Ctrl Pts',(-2.36583346352739,-0.575261783852008,
13.8873128142435));
#257232=CARTESIAN_POINT('Ctrl Pts',(-1.86305904372481,-1.94999080919174,
13.9789764501001));
#257233=CARTESIAN_POINT('Ctrl Pts',(0.438422718329072,-2.76911597159671,
14.123580799475));
#257234=CARTESIAN_POINT('Ctrl Pts',(2.56464881291346,-1.1326050549584,14.2824029400298));
#257235=CARTESIAN_POINT('Ctrl Pts',(2.34196789024492,1.54123461716797,14.4412250805845));
#257236=CARTESIAN_POINT('Ctrl Pts',(-0.0256713533761431,2.80349045400981,
14.6000472211392));
#257237=CARTESIAN_POINT('Ctrl Pts',(-2.02983150517857,1.68741078469057,
14.7358354915794));
#257238=CARTESIAN_POINT('Ctrl Pts',(-2.36672958999097,0.44644395791586,
14.8186830485013));
#257239=CARTESIAN_POINT('Ctrl Pts',(-2.36812488029342,-0.000824552762472806,
14.848589891905));
#257240=CARTESIAN_POINT('Origin',(0.,0.,-1.84858989190501));
#257241=CARTESIAN_POINT('',(-2.36937452646423,-0.00176685267772711,12.651410108095));
#257242=CARTESIAN_POINT('',(-2.37556206679244,-0.000405523443091083,12.848589891905));
#257243=CARTESIAN_POINT('',(-2.37175,-1.78696459712734E-13,-1.84858989190501));
#257244=CARTESIAN_POINT('Ctrl Pts',(-2.36937452646423,-0.00176685267772737,
12.651410108095));
#257245=CARTESIAN_POINT('Ctrl Pts',(-2.37124528291158,-0.272405989378181,
12.6695304868561));
#257246=CARTESIAN_POINT('Ctrl Pts',(-2.20341674148091,-1.33149770622952,
12.7405915791355));
#257247=CARTESIAN_POINT('Ctrl Pts',(-0.642779497905573,-2.7289286225062,
12.8645933849331));
#257248=CARTESIAN_POINT('Ctrl Pts',(1.94480058344235,-2.01939783111293,
13.0234155254878));
#257249=CARTESIAN_POINT('Ctrl Pts',(2.7511793889647,0.539656260407611,13.1822376660426));
#257250=CARTESIAN_POINT('Ctrl Pts',(1.03781181052871,2.60445072051449,13.3410598065973));
#257251=CARTESIAN_POINT('Ctrl Pts',(-1.58528548982049,2.28879183148743,
13.4974506206148));
#257252=CARTESIAN_POINT('Ctrl Pts',(-2.37264502847528,0.748789156612332,
13.600900721114));
#257253=CARTESIAN_POINT('Ctrl Pts',(-2.37542200031537,-0.00066209981418278,
13.651410108095));
#257254=CARTESIAN_POINT('Ctrl Pts',(-2.37556206679244,-0.000405523443090844,
12.848589891905));
#257255=CARTESIAN_POINT('Ctrl Pts',(-2.37561368933657,-0.0222324491625394,
12.8500611529491));
#257256=CARTESIAN_POINT('Ctrl Pts',(-2.36545128211817,-0.829413219156352,
12.9044731275114));
#257257=CARTESIAN_POINT('Ctrl Pts',(-1.45381213248182,-2.39721672519321,
13.0118258155919));
#257258=CARTESIAN_POINT('Ctrl Pts',(1.22642111687513,-2.52113248128301,
13.1706479561466));
#257259=CARTESIAN_POINT('Ctrl Pts',(2.7834014853579,-0.335996897909497,
13.3294700967014));
#257260=CARTESIAN_POINT('Ctrl Pts',(1.79112394068293,2.15687106086799,13.4882922372561));
#257261=CARTESIAN_POINT('Ctrl Pts',(-0.841605728219187,2.6743069274723,
13.6471143778108));
#257262=CARTESIAN_POINT('Ctrl Pts',(-2.24956593291735,1.21342596888521,
13.7672135960271));
#257263=CARTESIAN_POINT('Ctrl Pts',(-2.37277616411804,0.214145330165912,
13.8343721007252));
#257264=CARTESIAN_POINT('Ctrl Pts',(-2.37091162809913,0.0021416612107103,
13.848589891905));
#257265=CARTESIAN_POINT('Origin',(0.,0.,-1.84858989190501));
#257266=CARTESIAN_POINT('',(-2.3690442531058,0.00160878581760178,11.651410108095));
#257267=CARTESIAN_POINT('',(-2.36971778769283,-0.00189546110360289,11.848589891905));
#257268=CARTESIAN_POINT('',(-2.37175,-1.78696459712734E-13,-1.84858989190501));
#257269=CARTESIAN_POINT('Ctrl Pts',(-2.3690442531058,0.00160878581760195,
11.651410108095));
#257270=CARTESIAN_POINT('Ctrl Pts',(-2.36589429483149,-0.503533084642829,
11.68521953908));
#257271=CARTESIAN_POINT('Ctrl Pts',(-1.96012607113578,-1.80427476842366,
11.7719696835832));
#257272=CARTESIAN_POINT('Ctrl Pts',(0.180442601226353,-2.79779509209019,
11.9116605416047));
#257273=CARTESIAN_POINT('Ctrl Pts',(2.44890812594382,-1.36494172049492,
12.0704826821594));
#257274=CARTESIAN_POINT('Ctrl Pts',(2.47447105414424,1.31803259135108,12.2293048227142));
#257275=CARTESIAN_POINT('Ctrl Pts',(0.233718846407313,2.79384903144306,
12.3881269632689));
#257276=CARTESIAN_POINT('Ctrl Pts',(-1.94101657279419,1.83440196303656,
12.5288287250625));
#257277=CARTESIAN_POINT('Ctrl Pts',(-2.36577965868557,0.518296522515291,
12.6165897733379));
#257278=CARTESIAN_POINT('Ctrl Pts',(-2.36937452646423,-0.00176685267772737,
12.651410108095));
#257279=CARTESIAN_POINT('Ctrl Pts',(-2.36971778769283,-0.00189546110360261,
11.848589891905));
#257280=CARTESIAN_POINT('Ctrl Pts',(-2.37163683174812,-0.258101966923812,
11.8657502051729));
#257281=CARTESIAN_POINT('Ctrl Pts',(-2.21526537220026,-1.30244339925312,
11.9358512319591));
#257282=CARTESIAN_POINT('Ctrl Pts',(-0.692056486524632,-2.71685030201456,
12.0588929722635));
#257283=CARTESIAN_POINT('Ctrl Pts',(1.90793957711943,-2.05426004053984,
12.2177151128183));
#257284=CARTESIAN_POINT('Ctrl Pts',(2.7604945725652,0.489783073345279,12.376537253373));
#257285=CARTESIAN_POINT('Ctrl Pts',(1.08477160654539,2.58524434159141,12.5353593939277));
#257286=CARTESIAN_POINT('Ctrl Pts',(-1.55974375400603,2.31545814114733,
12.6927102734384));
#257287=CARTESIAN_POINT('Ctrl Pts',(-2.37375614384427,0.763170675708133,
12.7971204394308));
#257288=CARTESIAN_POINT('Ctrl Pts',(-2.37556206679244,-0.000405523443090844,
12.848589891905));
#257289=CARTESIAN_POINT('Origin',(0.,0.,-1.84858989190501));
#257290=CARTESIAN_POINT('',(-2.37521155387067,0.000920058411076374,10.651410108095));
#257291=CARTESIAN_POINT('',(-2.36876326363149,0.00143919393907455,10.848589891905));
#257292=CARTESIAN_POINT('',(-2.37175,-1.78696459712734E-13,-1.84858989190501));
#257293=CARTESIAN_POINT('Ctrl Pts',(-2.37521155387066,0.00092005841107628,
10.651410108095));
#257294=CARTESIAN_POINT('Ctrl Pts',(-2.37157703832641,-0.733704863043044,
10.7009085913039));
#257295=CARTESIAN_POINT('Ctrl Pts',(-1.6116945446461,-2.26053349925102,
10.803347788031));
#257296=CARTESIAN_POINT('Ctrl Pts',(0.987998371084236,-2.62375229935987,
10.9587276982763));
#257297=CARTESIAN_POINT('Ctrl Pts',(2.74039735767968,-0.591979080444202,
11.1175498388311));
#257298=CARTESIAN_POINT('Ctrl Pts',(1.98292499225804,1.98197512212938,11.2763719793858));
#257299=CARTESIAN_POINT('Ctrl Pts',(-0.590665979948808,2.74068068366097,
11.4351941199405));
#257300=CARTESIAN_POINT('Ctrl Pts',(-2.19058404802704,1.36209190860851,
11.5602068295102));
#257301=CARTESIAN_POINT('Ctrl Pts',(-2.37082667712059,0.287446540597829,
11.6322788255617));
#257302=CARTESIAN_POINT('Ctrl Pts',(-2.3690442531058,0.00160878581760195,
11.651410108095));
#257303=CARTESIAN_POINT('Ctrl Pts',(-2.36876326363149,0.00143919393907441,
10.848589891905));
#257304=CARTESIAN_POINT('Ctrl Pts',(-2.36604542551571,-0.489504653257154,
10.8814392573968));
#257305=CARTESIAN_POINT('Ctrl Pts',(-1.97786935145004,-1.7756026914142,
10.9672293364069));
#257306=CARTESIAN_POINT('Ctrl Pts',(0.129784664299144,-2.80060237895531,
11.1059601289351));
#257307=CARTESIAN_POINT('Ctrl Pts',(2.42380752331122,-1.40903329770356,
11.2647822694899));
#257308=CARTESIAN_POINT('Ctrl Pts',(2.49791689112318,1.27303925671557,11.4236044100446));
#257309=CARTESIAN_POINT('Ctrl Pts',(0.28423758216529,2.78916237264563,11.5824265505993));
#257310=CARTESIAN_POINT('Ctrl Pts',(-1.92245898347911,1.86294887847699,
11.7240883778862));
#257311=CARTESIAN_POINT('Ctrl Pts',(-2.36571645255842,0.532312229738396,
11.8128094916547));
#257312=CARTESIAN_POINT('Ctrl Pts',(-2.36971778769283,-0.00189546110360261,
11.848589891905));
#257313=CARTESIAN_POINT('Origin',(0.,0.,-1.84858989190501));
#257314=CARTESIAN_POINT('',(-2.37178798974141,-0.00216870721807306,9.65141010809499));
#257315=CARTESIAN_POINT('',(-2.37495901083281,0.00114971299769069,9.84858989190502));
#257316=CARTESIAN_POINT('',(-2.37175,-1.78696459712734E-13,-1.84858989190501));
#257317=CARTESIAN_POINT('Ctrl Pts',(-2.37178798974141,-0.00216870721807308,
9.65141010809499));
#257318=CARTESIAN_POINT('Ctrl Pts',(-2.37346696852305,-0.184610939429616,
9.66365693000949));
#257319=CARTESIAN_POINT('Ctrl Pts',(-2.27088436585652,-1.15384864042565,
9.72884446544225));
#257320=CARTESIAN_POINT('Ctrl Pts',(-0.940357642981567,-2.64120132003364,
9.84697271439322));
#257321=CARTESIAN_POINT('Ctrl Pts',(1.70977446530886,-2.22191093148198,
10.005794854948));
#257322=CARTESIAN_POINT('Ctrl Pts',(2.79396069466933,0.232380176228921,
10.1646169955027));
#257323=CARTESIAN_POINT('Ctrl Pts',(1.3192180568126,2.47383924866609,10.3234391360574));
#257324=CARTESIAN_POINT('Ctrl Pts',(-1.36376819526984,2.44956184229582,
10.4822612766122));
#257325=CARTESIAN_POINT('Ctrl Pts',(-2.35080676320134,0.88855867422785,
10.591584933958));
#257326=CARTESIAN_POINT('Ctrl Pts',(-2.37546430584922,0.0520074454725471,
10.6479678777856));
#257327=CARTESIAN_POINT('Ctrl Pts',(-2.37521155387066,0.00092005841107628,
10.651410108095));
#257328=CARTESIAN_POINT('Ctrl Pts',(-2.37495901083282,0.0011497129976905,
9.84858989190502));
#257329=CARTESIAN_POINT('Ctrl Pts',(-2.37065689581574,-0.719429682383803,
9.89712830962069));
#257330=CARTESIAN_POINT('Ctrl Pts',(-1.6363171272997,-2.23353310922339,
9.99860744085461));
#257331=CARTESIAN_POINT('Ctrl Pts',(0.940357692895628,-2.6412014602278,
10.1530272856068));
#257332=CARTESIAN_POINT('Ctrl Pts',(2.7292364351563,-0.6414719207516,10.3118494261615));
#257333=CARTESIAN_POINT('Ctrl Pts',(2.01846587572594,1.94576803669588,10.4706715667162));
#257334=CARTESIAN_POINT('Ctrl Pts',(-0.540974425817324,2.75092064856641,
10.6294937072709));
#257335=CARTESIAN_POINT('Ctrl Pts',(-2.17805383277753,1.3911462339404,10.7554664823339));
#257336=CARTESIAN_POINT('Ctrl Pts',(-2.37042554936049,0.301710555281621,
10.8284985438786));
#257337=CARTESIAN_POINT('Ctrl Pts',(-2.36876326363149,0.00143919393907441,
10.848589891905));
#257338=CARTESIAN_POINT('Origin',(0.,0.,-1.84858989190501));
#257339=CARTESIAN_POINT('',(-2.3679044556045,0.000358786198520854,8.65141010809499));
#257340=CARTESIAN_POINT('',(-2.37222321442519,-0.00213950769743509,8.84858989190502));
#257341=CARTESIAN_POINT('',(-2.37175,-1.78696459712734E-13,-1.84858989190501));
#257342=CARTESIAN_POINT('Ctrl Pts',(-2.3679044556045,0.000358786198520929,
8.65141010809499));
#257343=CARTESIAN_POINT('Ctrl Pts',(-2.3673403064869,-0.417530117617411,
8.67934598223336));
#257344=CARTESIAN_POINT('Ctrl Pts',(-2.06263816549048,-1.62812080978298,
8.76022256988998));
#257345=CARTESIAN_POINT('Ctrl Pts',(-0.129784657410042,-2.80060223030017,
8.89403987106487));
#257346=CARTESIAN_POINT('Ctrl Pts',(2.28310507284784,-1.62715952997786,
9.05286201161958));
#257347=CARTESIAN_POINT('Ctrl Pts',(2.60494767815974,1.03656379625737,9.21168415217432));
#257348=CARTESIAN_POINT('Ctrl Pts',(0.540974397102402,2.75092050254836,
9.37050629272904));
#257349=CARTESIAN_POINT('Ctrl Pts',(-1.82110658553714,2.00785348454621,
9.51708161136926));
#257350=CARTESIAN_POINT('Ctrl Pts',(-2.36620905824215,0.604052602554313,
9.61071621649125));
#257351=CARTESIAN_POINT('Ctrl Pts',(-2.37178798974141,-0.00216870721807308,
9.65141010809499));
#257352=CARTESIAN_POINT('Ctrl Pts',(-2.37222321442519,-0.00213950769743516,
8.84858989190502));
#257353=CARTESIAN_POINT('Ctrl Pts',(-2.37377707132607,-0.170200548119919,
8.85987664832633));
#257354=CARTESIAN_POINT('Ctrl Pts',(-2.28079939028199,-1.12484813559341,
8.92410411826587));
#257355=CARTESIAN_POINT('Ctrl Pts',(-0.987998423526767,-2.62375243862793,
9.04127230172366));
#257356=CARTESIAN_POINT('Ctrl Pts',(1.66928728944139,-2.2524870009407,9.2000944422784));
#257357=CARTESIAN_POINT('Ctrl Pts',(2.79770846226761,0.181783124226867,
9.35891658283312));
#257358=CARTESIAN_POINT('Ctrl Pts',(1.36376826765814,2.44956197231794,9.51773872338785));
#257359=CARTESIAN_POINT('Ctrl Pts',(-1.31921812683648,2.4738393799767,9.67656086394259));
#257360=CARTESIAN_POINT('Ctrl Pts',(-2.34325744778466,0.917403587350583,
9.78684458678164));
#257361=CARTESIAN_POINT('Ctrl Pts',(-2.37534920037284,0.066504205315249,
9.84418759610245));
#257362=CARTESIAN_POINT('Ctrl Pts',(-2.37495901083282,0.0011497129976905,
9.84858989190502));
#257363=CARTESIAN_POINT('Origin',(0.,0.,-1.84858989190501));
#257364=CARTESIAN_POINT('',(-2.37310580416009,0.00199191559344375,7.65141010809498));
#257365=CARTESIAN_POINT('',(-2.36786103774315,0.000124229582373903,7.84858989190502));
#257366=CARTESIAN_POINT('',(-2.37175,-1.78696459712734E-13,-1.84858989190501));
#257367=CARTESIAN_POINT('Ctrl Pts',(-2.37310580416009,0.00199191559344367,
7.65141010809498));
#257368=CARTESIAN_POINT('Ctrl Pts',(-2.36727740979178,-0.64696574170308,
7.69503503445724));
#257369=CARTESIAN_POINT('Ctrl Pts',(-1.75543549519818,-2.09312447203823,
7.79160067433773));
#257370=CARTESIAN_POINT('Ctrl Pts',(0.692056449790645,-2.71685015780489,
7.94110702773648));
#257371=CARTESIAN_POINT('Ctrl Pts',(2.65821266877332,-0.891135409034062,
8.0999291682912));
#257372=CARTESIAN_POINT('Ctrl Pts',(2.18976873525401,1.75075120898583,8.25875130884594));
#257373=CARTESIAN_POINT('Ctrl Pts',(-0.284237567078199,2.78916222459769,
8.41757344940066));
#257374=CARTESIAN_POINT('Ctrl Pts',(-2.10854369594215,1.53971625412154,
8.54845971581703));
#257375=CARTESIAN_POINT('Ctrl Pts',(-2.36840941413925,0.37440274368431,
8.62640526871512));
#257376=CARTESIAN_POINT('Ctrl Pts',(-2.3679044556045,0.000358786198520929,
8.65141010809499));
#257377=CARTESIAN_POINT('Ctrl Pts',(-2.36786103774315,0.000124229582374076,
7.84858989190502));
#257378=CARTESIAN_POINT('Ctrl Pts',(-2.36767260749056,-0.403421717141786,
7.8755657005502));
#257379=CARTESIAN_POINT('Ctrl Pts',(-2.07805004637786,-1.59919064096749,
7.95548222271362));
#257380=CARTESIAN_POINT('Ctrl Pts',(-0.180442610804054,-2.79779524059636,
8.08833945839529));
#257381=CARTESIAN_POINT('Ctrl Pts',(2.25328656381482,-1.66820784239526,
8.24716159895002));
#257382=CARTESIAN_POINT('Ctrl Pts',(2.62327874841108,0.989255453476115,
8.40598373950475));
#257383=CARTESIAN_POINT('Ctrl Pts',(0.59066601130102,2.74068082913556,8.56480588005947));
#257384=CARTESIAN_POINT('Ctrl Pts',(-1.80003185686014,2.03589293233909,
8.71234126419291));
#257385=CARTESIAN_POINT('Ctrl Pts',(-2.36648868040425,0.618092479785756,
8.80693593480808));
#257386=CARTESIAN_POINT('Ctrl Pts',(-2.37222321442519,-0.00213950769743516,
8.84858989190502));
#257387=CARTESIAN_POINT('Origin',(0.,0.,-1.84858989190501));
#257388=CARTESIAN_POINT('',(-2.37430755786411,-0.00156154949053819,6.65141010809498));
#257389=CARTESIAN_POINT('',(-2.37267966097722,0.00207845467076861,6.84858989190502));
#257390=CARTESIAN_POINT('',(-2.37175,-1.78696459712734E-13,-1.84858989190501));
#257391=CARTESIAN_POINT('Ctrl Pts',(-2.37430755786411,-0.00156154949053798,
6.65141010809498));
#257392=CARTESIAN_POINT('Ctrl Pts',(-2.37502807860986,-0.0962444547289554,
6.65778337316287));
#257393=CARTESIAN_POINT('Ctrl Pts',(-2.3268869061531,-0.97668956233699,
6.717097351749));
#257394=CARTESIAN_POINT('Ctrl Pts',(-1.2264210517769,-2.5211323474621,6.82935204385337));
#257395=CARTESIAN_POINT('Ctrl Pts',(1.45381205531404,-2.39721659794956,
6.9881741844081));
#257396=CARTESIAN_POINT('Ctrl Pts',(2.80252978248238,-0.0777414172792658,
7.14699632496283));
#257397=CARTESIAN_POINT('Ctrl Pts',(1.58447039810697,2.31293546541706,7.30581846551756));
#257398=CARTESIAN_POINT('Ctrl Pts',(-1.08477154896619,2.58524420436732,
7.46464060607229));
#257399=CARTESIAN_POINT('Ctrl Pts',(-2.30021044509958,1.06535984256429,
7.57983782026477));
#257400=CARTESIAN_POINT('Ctrl Pts',(-2.37435041557663,0.140572124495619,
7.642094320939));
#257401=CARTESIAN_POINT('Ctrl Pts',(-2.37310580416009,0.00199191559344367,
7.65141010809498));
#257402=CARTESIAN_POINT('Ctrl Pts',(-2.37267966097722,0.00207845467076865,
6.84858989190502));
#257403=CARTESIAN_POINT('Ctrl Pts',(-2.36685601691948,-0.632891799205702,
6.89125475277407));
#257404=CARTESIAN_POINT('Ctrl Pts',(-1.77738326645305,-2.06530485168304,
6.98686032716137));
#257405=CARTESIAN_POINT('Ctrl Pts',(0.64277953202424,-2.72892876735691,
7.13540661506691));
#257406=CARTESIAN_POINT('Ctrl Pts',(2.64165171954015,-0.939092081080438,
7.29422875562163));
#257407=CARTESIAN_POINT('Ctrl Pts',(2.2210915738946,1.71083896509047,7.45305089617638));
#257408=CARTESIAN_POINT('Ctrl Pts',(-0.233718858813212,2.79384917973975,
7.61187303673109));
#257409=CARTESIAN_POINT('Ctrl Pts',(-2.09388126411793,1.56869887105715,
7.74371936864065));
#257410=CARTESIAN_POINT('Ctrl Pts',(-2.36804240667441,0.388547511213119,
7.82262498703196));
#257411=CARTESIAN_POINT('Ctrl Pts',(-2.36786103774315,0.000124229582374076,
7.84858989190502));
#257412=CARTESIAN_POINT('Origin',(0.,0.,-1.84858989190501));
#257413=CARTESIAN_POINT('',(-2.36829614019373,-0.00104083913653463,5.65141010809498));
#257414=CARTESIAN_POINT('',(-2.37464485901916,-0.00137191232029432,5.84858989190501));
#257415=CARTESIAN_POINT('',(-2.37175,-1.78696459712734E-13,-1.84858989190501));
#257416=CARTESIAN_POINT('Ctrl Pts',(-2.36829614019373,-0.00104083913653439,
5.65141010809498));
#257417=CARTESIAN_POINT('Ctrl Pts',(-2.3696008644205,-0.330931720072927,
5.67347242538674));
#257418=CARTESIAN_POINT('Ctrl Pts',(-2.15126520202627,-1.45077744645276,
5.74847545619674));
#257419=CARTESIAN_POINT('Ctrl Pts',(-0.438422695057549,-2.76911582461286,
5.876419200525));
#257420=CARTESIAN_POINT('Ctrl Pts',(2.08934525988381,-1.86945267248516,
6.03524134107972));
#257421=CARTESIAN_POINT('Ctrl Pts',(2.7035265601163,0.742402214710351,6.19406348163445));
#257422=CARTESIAN_POINT('Ctrl Pts',(0.841605683546825,2.67430678552092,
6.35288562218919));
#257423=CARTESIAN_POINT('Ctrl Pts',(-1.68547684272582,2.17763477532239,
6.50533449767602));
#257424=CARTESIAN_POINT('Ctrl Pts',(-2.36904293881439,0.690256735463098,
6.60484265964462));
#257425=CARTESIAN_POINT('Ctrl Pts',(-2.37430755786411,-0.00156154949053798,
6.65141010809498));
#257426=CARTESIAN_POINT('Ctrl Pts',(-2.37464485901916,-0.00137191232029429,
5.84858989190501));
#257427=CARTESIAN_POINT('Ctrl Pts',(-2.37519850445556,-0.0817618654996098,
5.8540030914797));
#257428=CARTESIAN_POINT('Ctrl Pts',(-2.33500878081015,-0.94779985711636,
5.91235700457263));
#257429=CARTESIAN_POINT('Ctrl Pts',(-1.2718422600056,-2.49852656775178,
6.02365163118381));
#257430=CARTESIAN_POINT('Ctrl Pts',(1.41019447782222,-2.42313212161802,
6.18247377173853));
#257431=CARTESIAN_POINT('Ctrl Pts',(2.80066424243723,-0.128442770255383,
6.34129591229326));
#257432=CARTESIAN_POINT('Ctrl Pts',(1.62606550375187,2.28388456836278,6.50011805284799));
#257433=CARTESIAN_POINT('Ctrl Pts',(-1.0378118656156,2.60445085875792,6.65894019340272));
#257434=CARTESIAN_POINT('Ctrl Pts',(-2.29091251569842,1.09432815490155,
6.7750974730884));
#257435=CARTESIAN_POINT('Ctrl Pts',(-2.37408228850253,0.155011351498428,
6.83831403925583));
#257436=CARTESIAN_POINT('Ctrl Pts',(-2.37267966097722,0.00207845467076865,
6.84858989190502));
#257437=CARTESIAN_POINT('Origin',(0.,0.,-1.84858989190501));
#257438=CARTESIAN_POINT('',(-2.37049761817908,0.00208654043934857,4.65141010809498));
#257439=CARTESIAN_POINT('',(-2.36850443708147,-0.00124249154027839,4.84858989190502));
#257440=CARTESIAN_POINT('',(-2.37175,-1.78696459712734E-13,-1.84858989190501));
#257441=CARTESIAN_POINT('Ctrl Pts',(-2.37049761817908,0.00208654043934844,
4.65141010809498));
#257442=CARTESIAN_POINT('Ctrl Pts',(-2.3657393662343,-0.561079367483094,
4.68916147761062));
#257443=CARTESIAN_POINT('Ctrl Pts',(-1.88309579984035,-1.9213324922744,
4.7798535606445));
#257444=CARTESIAN_POINT('Ctrl Pts',(0.387640255360107,-2.77668002156518,
4.92348635719661));
#257445=CARTESIAN_POINT('Ctrl Pts',(2.54347800477387,-1.17937973057141,
5.08230849775135));
#257446=CARTESIAN_POINT('Ctrl Pts',(2.36979862748696,1.49808924126962,5.24113063830607));
#257447=CARTESIAN_POINT('Ctrl Pts',(0.0256713520133373,2.80349030520137,
5.3999527788608));
#257448=CARTESIAN_POINT('Ctrl Pts',(-2.01307404072613,1.71657713684027,
5.53671260212377));
#257449=CARTESIAN_POINT('Ctrl Pts',(-2.36647004952937,0.460674093086885,
5.6205317118685));
#257450=CARTESIAN_POINT('Ctrl Pts',(-2.36829614019373,-0.00104083913653439,
5.65141010809498));
#257451=CARTESIAN_POINT('Ctrl Pts',(-2.36850443708147,-0.00124249154027849,
4.84858989190502));
#257452=CARTESIAN_POINT('Ctrl Pts',(-2.37000186470862,-0.316708460084333,
4.86969214370357));
#257453=CARTESIAN_POINT('Ctrl Pts',(-2.16449434554539,-1.42173458182854,
4.94373510902037));
#257454=CARTESIAN_POINT('Ctrl Pts',(-0.488460355212123,-2.76072893010059,
5.07071878785543));
#257455=CARTESIAN_POINT('Ctrl Pts',(2.05517397389945,-1.90695508103928,
5.22954092841014));
#257456=CARTESIAN_POINT('Ctrl Pts',(2.7165183985746,0.693358157305003,5.3883630689649));
#257457=CARTESIAN_POINT('Ctrl Pts',(0.889861699361338,2.65863948291391,
5.5471852095196));
#257458=CARTESIAN_POINT('Ctrl Pts',(-1.66176346574157,2.20493905396228,
5.70059415049967));
#257459=CARTESIAN_POINT('Ctrl Pts',(-2.36978389078125,0.704446258234449,
5.80106237796146));
#257460=CARTESIAN_POINT('Ctrl Pts',(-2.37464485901916,-0.00137191232029429,
5.84858989190501));
#257461=CARTESIAN_POINT('Origin',(0.,0.,-1.84858989190501));
#257462=CARTESIAN_POINT('',(-2.37563694907561,-0.000138612772022241,3.65141010809498));
#257463=CARTESIAN_POINT('',(-2.37010644407789,0.0020062719553457,3.84858989190501));
#257464=CARTESIAN_POINT('',(-2.37175,-1.78696459712734E-13,-1.84858989190501));
#257465=CARTESIAN_POINT('Ctrl Pts',(-2.37563694907561,-0.00013861277202187,
3.65141010809498));
#257466=CARTESIAN_POINT('Ctrl Pts',(-2.37564322066674,-0.0075514150958584,
3.65190981631625));
#257467=CARTESIAN_POINT('Ctrl Pts',(-2.37225376878547,-0.800294695141046,
3.70535023805575));
#257468=CARTESIAN_POINT('Ctrl Pts',(-1.49746686029714,-2.37019195537365,
3.81173137331351));
#257469=CARTESIAN_POINT('Ctrl Pts',(1.18004762854664,-2.54316820267302,
3.97055351386824));
#257470=CARTESIAN_POINT('Ctrl Pts',(2.77678172346816,-0.3869110620803,4.12937565442297));
#257471=CARTESIAN_POINT('Ctrl Pts',(1.83032080339732,2.12370964715592,4.2881977949777));
#257472=CARTESIAN_POINT('Ctrl Pts',(-0.792491809340816,2.68927009470421,
4.44701993553242));
#257473=CARTESIAN_POINT('Ctrl Pts',(-2.23857227461137,1.24280982655239,
4.56809070657152));
#257474=CARTESIAN_POINT('Ctrl Pts',(-2.37241211099266,0.2286775440434,4.63622076409237));
#257475=CARTESIAN_POINT('Ctrl Pts',(-2.37049761817908,0.00208654043934844,
4.65141010809498));
#257476=CARTESIAN_POINT('Ctrl Pts',(-2.37010644407789,0.00200627195534563,
3.84858989190501));
#257477=CARTESIAN_POINT('Ctrl Pts',(-2.36570137679432,-0.547067010809973,
3.88538119592745));
#257478=CARTESIAN_POINT('Ctrl Pts',(-1.90248361218273,-1.89293283173512,
3.97511321346813));
#257479=CARTESIAN_POINT('Ctrl Pts',(0.337330496827683,-2.7832401765723,
4.11778594452705));
#257480=CARTESIAN_POINT('Ctrl Pts',(2.5217198186729,-1.22521300196359,4.27660808508177));
#257481=CARTESIAN_POINT('Ctrl Pts',(2.39651987123609,1.45496056673479,4.43543022563651));
#257482=CARTESIAN_POINT('Ctrl Pts',(0.0763986097743705,2.80256685854148,
4.59425236619123));
#257483=CARTESIAN_POINT('Ctrl Pts',(-1.99612954492781,1.74535439643512,
4.73197225494741));
#257484=CARTESIAN_POINT('Ctrl Pts',(-2.36624516197471,0.474723356049453,
4.81675143018533));
#257485=CARTESIAN_POINT('Ctrl Pts',(-2.36850443708147,-0.00124249154027849,
4.84858989190502));
#257486=CARTESIAN_POINT('Origin',(0.,0.,-1.84858989190501));
#257487=CARTESIAN_POINT('',(-2.37009071158309,-0.00200244152909902,2.65141010809498));
#257488=CARTESIAN_POINT('',(-2.37563860010749,0.000127708837501365,2.84858989190502));
#257489=CARTESIAN_POINT('',(-2.37175,-1.78696459712734E-13,-1.84858989190501));
#257490=CARTESIAN_POINT('Ctrl Pts',(-2.37009071158308,-0.00200244152909895,
2.65141010809498));
#257491=CARTESIAN_POINT('Ctrl Pts',(-2.37202441399179,-0.243607466556911,
2.66759886854012));
#257492=CARTESIAN_POINT('Ctrl Pts',(-2.22692364558065,-1.27304507845961,
2.7367283425035));
#257493=CARTESIAN_POINT('Ctrl Pts',(-0.741692209042783,-2.70372136703395,
2.85879852998513));
#257494=CARTESIAN_POINT('Ctrl Pts',(1.87000128182168,-2.08885428573093,
3.01762067053986));
#257495=CARTESIAN_POINT('Ctrl Pts',(2.76900059871079,0.439149889804403,
3.17644281109459));
#257496=CARTESIAN_POINT('Ctrl Pts',(1.13193145582276,2.56494601121031,3.33526495164932));
#257497=CARTESIAN_POINT('Ctrl Pts',(-1.53343688177706,2.34226578732656,
3.49358738398278));
#257498=CARTESIAN_POINT('Ctrl Pts',(-2.37497878791394,0.77778496219778,
3.598969102798));
#257499=CARTESIAN_POINT('Ctrl Pts',(-2.37563694907561,-0.00013861277202187,
3.65141010809498));
#257500=CARTESIAN_POINT('Ctrl Pts',(-2.37563860010749,0.000127708837501165,
2.84858989190502));
#257501=CARTESIAN_POINT('Ctrl Pts',(-2.37503056579596,-0.778378305301327,
2.90107024815132));
#257502=CARTESIAN_POINT('Ctrl Pts',(-1.53236168511894,-2.34334782239945,
3.00649131791588));
#257503=CARTESIAN_POINT('Ctrl Pts',(1.13383374784398,-2.56410584709992,
3.16485310119866));
#257504=CARTESIAN_POINT('Ctrl Pts',(2.76932572019706,-0.437095872952947,
3.3236752417534));
#257505=CARTESIAN_POINT('Ctrl Pts',(1.86845146885275,2.09024085837316,3.48249738230812));
#257506=CARTESIAN_POINT('Ctrl Pts',(-0.743697535029044,2.70317067969047,
3.64131952286286));
#257507=CARTESIAN_POINT('Ctrl Pts',(-2.22738897388365,1.27185445710156,
3.76335035939515));
#257508=CARTESIAN_POINT('Ctrl Pts',(-2.37204003238928,0.243019998491892,
3.8324404824092));
#257509=CARTESIAN_POINT('Ctrl Pts',(-2.37010644407789,0.00200627195534563,
3.84858989190501));
#257510=CARTESIAN_POINT('Origin',(0.,0.,-1.84858989190501));
#257511=CARTESIAN_POINT('',(-2.36851313222558,0.00125322961359671,1.65141010809498));
#257512=CARTESIAN_POINT('',(-2.37048131180486,-0.00208369211671167,1.84858989190502));
#257513=CARTESIAN_POINT('',(-2.37175,-1.78696459712734E-13,-1.84858989190501));
#257514=CARTESIAN_POINT('Ctrl Pts',(-2.36851313222558,0.0012532296135967,
1.65141010809498));
#257515=CARTESIAN_POINT('Ctrl Pts',(-2.36623622912522,-0.475297325567596,
1.68328792076399));
#257516=CARTESIAN_POINT('Ctrl Pts',(-1.99542751577998,-1.74653730674971,
1.76810644695125));
#257517=CARTESIAN_POINT('Ctrl Pts',(0.078477925820518,-2.80250631776144,
1.90586568665675));
#257518=CARTESIAN_POINT('Ctrl Pts',(2.39759801404543,-1.4531840222644,2.06468782721148));
#257519=CARTESIAN_POINT('Ctrl Pts',(2.520810341052,1.22708388997517,2.22350996776621));
#257520=CARTESIAN_POINT('Ctrl Pts',(0.335265845793994,2.78348905308081,
2.38233210832094));
#257521=CARTESIAN_POINT('Ctrl Pts',(-1.90326945111716,1.89176722009415,
2.52496548843053));
#257522=CARTESIAN_POINT('Ctrl Pts',(-2.36570079300822,0.546492705590905,
2.61465815502187));
#257523=CARTESIAN_POINT('Ctrl Pts',(-2.37009071158308,-0.00200244152909895,
2.65141010809498));
#257524=CARTESIAN_POINT('Ctrl Pts',(-2.37048131180486,-0.00208369211671135,
1.84858989190502));
#257525=CARTESIAN_POINT('Ctrl Pts',(-2.37239723210793,-0.229265828060701,
1.86381858685695));
#257526=CARTESIAN_POINT('Ctrl Pts',(-2.23812046499434,-1.24400071348261,
1.93198799532714));
#257527=CARTESIAN_POINT('Ctrl Pts',(-0.79049672615424,-2.68985692246101,
2.05309811731556));
#257528=CARTESIAN_POINT('Ctrl Pts',(1.83189557733352,-2.12235175091147,
2.21192025787029));
#257529=CARTESIAN_POINT('Ctrl Pts',(2.77649415671547,0.388970759351873,
2.37074239842502));
#257530=CARTESIAN_POINT('Ctrl Pts',(1.17816095594432,2.54404287719204,2.52956453897975));
#257531=CARTESIAN_POINT('Ctrl Pts',(-1.49922460191346,2.36908071791899,
2.68838667953448));
#257532=CARTESIAN_POINT('Ctrl Pts',(-2.37252370148548,0.799115854689114,
2.7947284638429));
#257533=CARTESIAN_POINT('Ctrl Pts',(-2.37564393377968,0.00695675746614235,
2.84812953463308));
#257534=CARTESIAN_POINT('Ctrl Pts',(-2.37563860010749,0.000127708837501165,
2.84858989190502));
#257535=CARTESIAN_POINT('Origin',(0.,0.,-1.84858989190501));
#257536=CARTESIAN_POINT('',(-2.37462805812147,0.00152502885334134,0.651410108094979));
#257537=CARTESIAN_POINT('',(-2.36829764012707,0.00106700769158252,0.848589891905016));
#257538=CARTESIAN_POINT('',(-2.37175,-1.78696459712734E-13,-1.84858989190501));
#257539=CARTESIAN_POINT('Ctrl Pts',(-2.37462805812147,0.00152502885334119,
0.651410108094978));
#257540=CARTESIAN_POINT('Ctrl Pts',(-2.36977823922653,-0.704823399369114,
0.698976972987868));
#257541=CARTESIAN_POINT('Ctrl Pts',(-1.66082968322975,-2.20631416213666,
0.799484551399001));
#257542=CARTESIAN_POINT('Ctrl Pts',(0.891859770330893,-2.65783549575534,
0.952932843328373));
#257543=CARTESIAN_POINT('Ctrl Pts',(2.71701801755088,-0.691417882516756,
1.11175498388311));
#257544=CARTESIAN_POINT('Ctrl Pts',(2.05376604018409,1.90851811654588,1.27057712443783));
#257545=CARTESIAN_POINT('Ctrl Pts',(-0.490511741217893,2.76034515792448,
1.42939926499256));
#257546=CARTESIAN_POINT('Ctrl Pts',(-2.16502830177281,1.42054841044669,
1.55634359287828));
#257547=CARTESIAN_POINT('Ctrl Pts',(-2.37001756995926,0.316128569325436,
1.63034720724575));
#257548=CARTESIAN_POINT('Ctrl Pts',(-2.36851313222558,0.0012532296135967,
1.65141010809498));
#257549=CARTESIAN_POINT('Ctrl Pts',(-2.36829764012707,0.00106700769158283,
0.848589891905016));
#257550=CARTESIAN_POINT('Ctrl Pts',(-2.36645677222522,-0.461240440100845,
0.879507639080828));
#257551=CARTESIAN_POINT('Ctrl Pts',(-2.01239790937726,-1.71778716938983,
0.963366099774883));
#257552=CARTESIAN_POINT('Ctrl Pts',(0.0277579514215299,-2.80345103515647,
1.10016527398718));
#257553=CARTESIAN_POINT('Ctrl Pts',(2.37090557643909,-1.49634138211991,
1.25898741454191));
#257554=CARTESIAN_POINT('Ctrl Pts',(2.54260459056719,1.18127146424035,1.41780955509664));
#257555=CARTESIAN_POINT('Ctrl Pts',(0.385579550113745,2.77696412127707,
1.57663169565137));
#257556=CARTESIAN_POINT('Ctrl Pts',(-1.88389820241982,1.92017114645465,
1.72022514125416));
#257557=CARTESIAN_POINT('Ctrl Pts',(-2.36573676722839,0.560505351507294,
1.81087787333871));
#257558=CARTESIAN_POINT('Ctrl Pts',(-2.37048131180486,-0.00208369211671135,
1.84858989190502));
#257559=CARTESIAN_POINT('Ctrl Pts',(-1.03908919352509,2.13201587949044,
-0.329233991005384));
#257560=CARTESIAN_POINT('Ctrl Pts',(-1.74827509563859,1.7863770809358,-0.276293277487141));
#257561=CARTESIAN_POINT('Ctrl Pts',(-2.78233718465057,0.337749170168978,
-0.170411850450654));
#257562=CARTESIAN_POINT('Ctrl Pts',(-1.79018921372264,-2.16005466875641,
-0.0115897098959247));
#257563=CARTESIAN_POINT('Ctrl Pts',(0.843935273622217,-2.67272649501447,
0.147232430658805));
#257564=CARTESIAN_POINT('Ctrl Pts',(2.70389566823784,-0.740895185834261,
0.306054571213535));
#257565=CARTESIAN_POINT('Ctrl Pts',(2.08805286496322,1.8712628391822,0.464876711768264));
#257566=CARTESIAN_POINT('Ctrl Pts',(-0.440526185828228,2.76865345984501,
0.623698852322994));
#257567=CARTESIAN_POINT('Ctrl Pts',(-2.56546224110779,1.13077392232151,
0.782520992877724));
#257568=CARTESIAN_POINT('Ctrl Pts',(-2.34083763947357,-1.54300878412073,
0.941343133432452));
#257569=CARTESIAN_POINT('Ctrl Pts',(0.0277579514215299,-2.80345103515647,
1.10016527398718));
#257570=CARTESIAN_POINT('Ctrl Pts',(2.37090557643909,-1.49634138211991,
1.25898741454191));
#257571=CARTESIAN_POINT('Ctrl Pts',(2.54260459056719,1.18127146424035,1.41780955509664));
#257572=CARTESIAN_POINT('Ctrl Pts',(0.385579550113745,2.77696412127707,
1.57663169565137));
#257573=CARTESIAN_POINT('Ctrl Pts',(-2.12458595977851,1.82930461145536,
1.7354538362061));
#257574=CARTESIAN_POINT('Ctrl Pts',(-2.68889049494592,-0.793781067907386,
1.89427597676083));
#257575=CARTESIAN_POINT('Ctrl Pts',(-0.79049672615424,-2.68985692246101,
2.05309811731556));
#257576=CARTESIAN_POINT('Ctrl Pts',(1.83189557733352,-2.12235175091147,
2.21192025787029));
#257577=CARTESIAN_POINT('Ctrl Pts',(2.77649415671547,0.388970759351873,
2.37074239842502));
#257578=CARTESIAN_POINT('Ctrl Pts',(1.17816095594432,2.54404287719204,2.52956453897975));
#257579=CARTESIAN_POINT('Ctrl Pts',(-1.49922460191346,2.36908071791899,
2.68838667953448));
#257580=CARTESIAN_POINT('Ctrl Pts',(-2.80350243814271,0.024328071577183,
2.84720882008921));
#257581=CARTESIAN_POINT('Ctrl Pts',(-1.54011230796823,-2.34270607942395,
3.00603096064394));
#257582=CARTESIAN_POINT('Ctrl Pts',(1.13383374784398,-2.56410584709992,
3.16485310119866));
#257583=CARTESIAN_POINT('Ctrl Pts',(2.76932572019706,-0.437095872952947,
3.3236752417534));
#257584=CARTESIAN_POINT('Ctrl Pts',(1.86845146885275,2.09024085837316,3.48249738230812));
#257585=CARTESIAN_POINT('Ctrl Pts',(-0.743697535029044,2.70317067969047,
3.64131952286286));
#257586=CARTESIAN_POINT('Ctrl Pts',(-2.67470986713947,0.840324265275232,
3.80014166341758));
#257587=CARTESIAN_POINT('Ctrl Pts',(-2.15601261504427,-1.79215717697482,
3.95896380397232));
#257588=CARTESIAN_POINT('Ctrl Pts',(0.337330496827683,-2.7832401765723,
4.11778594452705));
#257589=CARTESIAN_POINT('Ctrl Pts',(2.5217198186729,-1.22521300196359,4.27660808508177));
#257590=CARTESIAN_POINT('Ctrl Pts',(2.39651987123609,1.45496056673479,4.43543022563651));
#257591=CARTESIAN_POINT('Ctrl Pts',(0.0763986097743705,2.80256685854148,
4.59425236619123));
#257592=CARTESIAN_POINT('Ctrl Pts',(-2.31369450504449,1.58336208158914,
4.75307450674597));
#257593=CARTESIAN_POINT('Ctrl Pts',(-2.58472428794165,-1.08601017463356,
4.91189664730069));
#257594=CARTESIAN_POINT('Ctrl Pts',(-0.488460355212123,-2.76072893010059,
5.07071878785543));
#257595=CARTESIAN_POINT('Ctrl Pts',(2.05517397389945,-1.90695508103928,
5.22954092841014));
#257596=CARTESIAN_POINT('Ctrl Pts',(2.7165183985746,0.693358157305003,5.3883630689649));
#257597=CARTESIAN_POINT('Ctrl Pts',(0.889861699361338,2.65863948291391,
5.5471852095196));
#257598=CARTESIAN_POINT('Ctrl Pts',(-1.75180030564315,2.18892974607354,
5.70600735007435));
#257599=CARTESIAN_POINT('Ctrl Pts',(-2.78902586303999,-0.285573947325892,
5.86482949062906));
#257600=CARTESIAN_POINT('Ctrl Pts',(-1.2718422600056,-2.49852656775178,
6.02365163118381));
#257601=CARTESIAN_POINT('Ctrl Pts',(1.41019447782222,-2.42313212161802,
6.18247377173853));
#257602=CARTESIAN_POINT('Ctrl Pts',(2.80066424243723,-0.128442770255383,
6.34129591229326));
#257603=CARTESIAN_POINT('Ctrl Pts',(1.62606550375187,2.28388456836278,6.50011805284799));
#257604=CARTESIAN_POINT('Ctrl Pts',(-1.0378118656156,2.60445085875792,6.65894019340272));
#257605=CARTESIAN_POINT('Ctrl Pts',(-2.75117953499654,0.539656289052272,
6.81776233395745));
#257606=CARTESIAN_POINT('Ctrl Pts',(-1.94480068667171,-2.01939793830208,
6.97658447451218));
#257607=CARTESIAN_POINT('Ctrl Pts',(0.64277953202424,-2.72892876735691,
7.13540661506691));
#257608=CARTESIAN_POINT('Ctrl Pts',(2.64165171954015,-0.939092081080438,
7.29422875562163));
#257609=CARTESIAN_POINT('Ctrl Pts',(2.2210915738946,1.71083896509047,7.45305089617638));
#257610=CARTESIAN_POINT('Ctrl Pts',(-0.233718858813212,2.79384917973975,
7.61187303673109));
#257611=CARTESIAN_POINT('Ctrl Pts',(-2.47447118548852,1.31803266131172,
7.77069517728583));
#257612=CARTESIAN_POINT('Ctrl Pts',(-2.44890825593109,-1.36494179294576,
7.92951731784055));
#257613=CARTESIAN_POINT('Ctrl Pts',(-0.180442610804054,-2.79779524059636,
8.08833945839529));
#257614=CARTESIAN_POINT('Ctrl Pts',(2.25328656381482,-1.66820784239526,
8.24716159895002));
#257615=CARTESIAN_POINT('Ctrl Pts',(2.62327874841108,0.989255453476115,
8.40598373950475));
#257616=CARTESIAN_POINT('Ctrl Pts',(0.59066601130102,2.74068082913556,8.56480588005947));
#257617=CARTESIAN_POINT('Ctrl Pts',(-1.98292509751125,1.98197522733192,
8.72362802061421));
#257618=CARTESIAN_POINT('Ctrl Pts',(-2.74039750313914,-0.591979111866446,
8.88245016116893));
#257619=CARTESIAN_POINT('Ctrl Pts',(-0.987998423526767,-2.62375243862793,
9.04127230172366));
#257620=CARTESIAN_POINT('Ctrl Pts',(1.66928728944139,-2.2524870009407,9.2000944422784));
#257621=CARTESIAN_POINT('Ctrl Pts',(2.79770846226761,0.181783124226867,
9.35891658283312));
#257622=CARTESIAN_POINT('Ctrl Pts',(1.36376826765814,2.44956197231794,9.51773872338785));
#257623=CARTESIAN_POINT('Ctrl Pts',(-1.31921812683648,2.4738393799767,9.67656086394259));
#257624=CARTESIAN_POINT('Ctrl Pts',(-2.79396084297197,0.23238018856341,
9.83538300449731));
#257625=CARTESIAN_POINT('Ctrl Pts',(-1.70977455606306,-2.22191104942047,
9.99420514505205));
#257626=CARTESIAN_POINT('Ctrl Pts',(0.940357692895628,-2.6412014602278,
10.1530272856068));
#257627=CARTESIAN_POINT('Ctrl Pts',(2.7292364351563,-0.6414719207516,10.3118494261615));
#257628=CARTESIAN_POINT('Ctrl Pts',(2.01846587572594,1.94576803669588,10.4706715667162));
#257629=CARTESIAN_POINT('Ctrl Pts',(-0.540974425817324,2.75092064856641,
10.6294937072709));
#257630=CARTESIAN_POINT('Ctrl Pts',(-2.60494781642969,1.0365638512777,10.7883158478257));
#257631=CARTESIAN_POINT('Ctrl Pts',(-2.28310519403429,-1.62715961634717,
10.9471379883804));
#257632=CARTESIAN_POINT('Ctrl Pts',(0.129784664299144,-2.80060237895531,
11.1059601289351));
#257633=CARTESIAN_POINT('Ctrl Pts',(2.42380752331122,-1.40903329770356,
11.2647822694899));
#257634=CARTESIAN_POINT('Ctrl Pts',(2.49791689112318,1.27303925671557,11.4236044100446));
#257635=CARTESIAN_POINT('Ctrl Pts',(0.28423758216529,2.78916237264563,11.5824265505993));
#257636=CARTESIAN_POINT('Ctrl Pts',(-2.18976885148641,1.75075130191508,
11.7412486911541));
#257637=CARTESIAN_POINT('Ctrl Pts',(-2.65821280987044,-0.891135456335437,
11.9000708317088));
#257638=CARTESIAN_POINT('Ctrl Pts',(-0.692056486524632,-2.71685030201456,
12.0588929722635));
#257639=CARTESIAN_POINT('Ctrl Pts',(1.90793957711943,-2.05426004053984,
12.2177151128183));
#257640=CARTESIAN_POINT('Ctrl Pts',(2.7604945725652,0.489783073345279,12.376537253373));
#257641=CARTESIAN_POINT('Ctrl Pts',(1.08477160654539,2.58524434159141,12.5353593939277));
#257642=CARTESIAN_POINT('Ctrl Pts',(-1.58447048221035,2.31293558818691,
12.6941815344825));
#257643=CARTESIAN_POINT('Ctrl Pts',(-2.80252993123984,-0.0777414214059339,
12.8530036750372));
#257644=CARTESIAN_POINT('Ctrl Pts',(-1.45381213248182,-2.39721672519321,
13.0118258155919));
#257645=CARTESIAN_POINT('Ctrl Pts',(1.22642111687513,-2.52113248128301,
13.1706479561466));
#257646=CARTESIAN_POINT('Ctrl Pts',(2.7834014853579,-0.335996897909497,
13.3294700967014));
#257647=CARTESIAN_POINT('Ctrl Pts',(1.79112394068293,2.15687106086799,13.4882922372561));
#257648=CARTESIAN_POINT('Ctrl Pts',(-0.841605728219187,2.6743069274723,
13.6471143778108));
#257649=CARTESIAN_POINT('Ctrl Pts',(-2.70352670361876,0.742402254116675,
13.8059365183655));
#257650=CARTESIAN_POINT('Ctrl Pts',(-2.08934537078553,-1.8694527717153,
13.9647586589203));
#257651=CARTESIAN_POINT('Ctrl Pts',(0.438422718329072,-2.76911597159671,
14.123580799475));
#257652=CARTESIAN_POINT('Ctrl Pts',(2.56464881291346,-1.1326050549584,14.2824029400298));
#257653=CARTESIAN_POINT('Ctrl Pts',(2.34196789024492,1.54123461716797,14.4412250805845));
#257654=CARTESIAN_POINT('Ctrl Pts',(-0.0256713533761431,2.80349045400981,
14.6000472211392));
#257655=CARTESIAN_POINT('Ctrl Pts',(-2.3697987532753,1.49808932078764,14.7588693616939));
#257656=CARTESIAN_POINT('Ctrl Pts',(-2.54347813978087,-1.17937979317275,
14.9176915022486));
#257657=CARTESIAN_POINT('Ctrl Pts',(-0.387640275935778,-2.7766801689505,
15.0765136428034));
#257658=CARTESIAN_POINT('Ctrl Pts',(2.1232290291376,-1.8308785415232,15.2353357833581));
#257659=CARTESIAN_POINT('Ctrl Pts',(2.68947825967196,0.791785599022987,
15.3941579239129));
#257660=CARTESIAN_POINT('Ctrl Pts',(0.792491851405913,2.68927023744945,
15.5529800644676));
#257661=CARTESIAN_POINT('Ctrl Pts',(-1.83032090055044,2.12370975988261,
15.7118022050223));
#257662=CARTESIAN_POINT('Ctrl Pts',(-2.77678187085878,-0.386911082619306,
15.870624345577));
#257663=CARTESIAN_POINT('Ctrl Pts',(-1.18004769118328,-2.54316833766063,
16.0294464861318));
#257664=CARTESIAN_POINT('Ctrl Pts',(1.49746693978282,-2.37019208118836,
16.1882686266865));
#257665=CARTESIAN_POINT('Ctrl Pts',(2.80348361626654,-0.0264075750974751,
16.3470907672412));
#257666=CARTESIAN_POINT('Ctrl Pts',(1.54184958368406,2.34156307285865,16.5059129077959));
#257667=CARTESIAN_POINT('Ctrl Pts',(-1.13193151590743,2.56494614739192,
16.6647350483507));
#257668=CARTESIAN_POINT('Ctrl Pts',(-2.7690007456855,0.439149913050121,
16.8235571889054));
#257669=CARTESIAN_POINT('Ctrl Pts',(-1.87000138108549,-2.08885439649021,
16.9823793294602));
#257670=CARTESIAN_POINT('Ctrl Pts',(0.741692248419004,-2.70372151075853,
17.1412014700149));
#257671=CARTESIAN_POINT('Ctrl Pts',(2.67408584390158,-0.842308110700031,
17.3000236105696));
#257672=CARTESIAN_POINT('Ctrl Pts',(2.15734130986859,1.79055768786866,17.4588457511243));
#257673=CARTESIAN_POINT('Ctrl Pts',(-0.33526586359856,2.78348920207669,
17.6176678916791));
#257674=CARTESIAN_POINT('Ctrl Pts',(-2.52081047486617,1.22708395286699,
17.7764900322338));
#257675=CARTESIAN_POINT('Ctrl Pts',(-2.39759814123902,-1.45318409539433,
17.9353121727885));
#257676=CARTESIAN_POINT('Ctrl Pts',(-0.0784779302164847,-2.80250647364015,
18.0941343133432));
#257677=CARTESIAN_POINT('Ctrl Pts',(2.31252045107973,-1.58508344876221,
18.252956453898));
#257678=CARTESIAN_POINT('Ctrl Pts',(2.58552714046087,1.08410340382027,18.4117785944527));
#257679=CARTESIAN_POINT('Ctrl Pts',(0.490511770879417,2.76034534307135,
18.5706007350074));
#257680=CARTESIAN_POINT('Ctrl Pts',(-2.05376615740623,1.90851815106454,
18.7294228755622));
#257681=CARTESIAN_POINT('Ctrl Pts',(-2.71701814363985,-0.691417805009407,
18.8882450161169));
#257682=CARTESIAN_POINT('Ctrl Pts',(-0.891859856974616,-2.65783582951041,
19.0470671566717));
#257683=CARTESIAN_POINT('Ctrl Pts',(1.75022653268834,-2.19050141850195,
19.2058892972263));
#257684=CARTESIAN_POINT('Ctrl Pts',(2.78914078757823,0.284026632862494,
19.3647114377811));
#257685=CARTESIAN_POINT('Ctrl Pts',(1.2738787066253,2.49658300563447,19.5235335783358));
#257686=CARTESIAN_POINT('Ctrl Pts',(-1.4087466563893,2.42611756744335,19.6823557188906));
#257687=CARTESIAN_POINT('Ctrl Pts',(-2.79990404402391,0.126538750182127,
19.8411778594453));
#257688=CARTESIAN_POINT('Ctrl Pts',(-2.01936616407895,-1.47301363900539,
19.9470592864818));
#257689=CARTESIAN_POINT('Ctrl Pts',(-1.37702479013087,-1.93106208855776,
20.));
#257690=CARTESIAN_POINT('Ctrl Pts',(-1.12236674703447,2.30288577939268,
-0.219489327336923));
#257691=CARTESIAN_POINT('Ctrl Pts',(-1.88839018271042,1.92954584245559,
-0.16654861381868));
#257692=CARTESIAN_POINT('Ctrl Pts',(-3.00532692914963,0.364817996181975,
-0.060667186782193));
#257693=CARTESIAN_POINT('Ctrl Pts',(-1.9336634977078,-2.33317173068091,
0.0981549537725366));
#257694=CARTESIAN_POINT('Ctrl Pts',(0.911572263156383,-2.88693151715453,
0.256977094327266));
#257695=CARTESIAN_POINT('Ctrl Pts',(2.92059873626954,-0.800274052314299,
0.415799234881996));
#257696=CARTESIAN_POINT('Ctrl Pts',(2.2553993596395,2.02123474938121,0.574621375436725));
#257697=CARTESIAN_POINT('Ctrl Pts',(-0.475832051042864,2.99054652551054,
0.733443515991456));
#257698=CARTESIAN_POINT('Ctrl Pts',(-2.77107059541602,1.2213995263697,0.892265656546184));
#257699=CARTESIAN_POINT('Ctrl Pts',(-2.52844350910708,-1.66667285202344,
1.05108779710092));
#257700=CARTESIAN_POINT('Ctrl Pts',(0.0299826057622768,-3.02813294412635,
1.20990993765564));
#257701=CARTESIAN_POINT('Ctrl Pts',(2.56092123364921,-1.61626530231301,
1.36873207821037));
#257702=CARTESIAN_POINT('Ctrl Pts',(2.74638102397023,1.27594418164071,1.5275542187651));
#257703=CARTESIAN_POINT('Ctrl Pts',(0.416481730423991,2.99952324290431,
1.68637635931983));
#257704=CARTESIAN_POINT('Ctrl Pts',(-2.29486039055236,1.97591378958438,
1.84519849987456));
#257705=CARTESIAN_POINT('Ctrl Pts',(-2.90439097697297,-0.857398460686849,
2.00402064042929));
#257706=CARTESIAN_POINT('Ctrl Pts',(-0.853850896153828,-2.90543485858881,
2.16284278098402));
#257707=CARTESIAN_POINT('Ctrl Pts',(1.97871240779968,-2.29244712155302,
2.32166492153875));
#257708=CARTESIAN_POINT('Ctrl Pts',(2.99901561314596,0.420144727310875,
2.48048706209348));
#257709=CARTESIAN_POINT('Ctrl Pts',(1.27258438240543,2.7479345817307,2.63930920264821));
#257710=CARTESIAN_POINT('Ctrl Pts',(-1.61937959706346,2.55895012228193,
2.79813134320294));
#257711=CARTESIAN_POINT('Ctrl Pts',(-3.02818846679257,0.0262778390227437,
2.95695348375767));
#257712=CARTESIAN_POINT('Ctrl Pts',(-1.66354423848634,-2.53046169472791,
3.1157756243124));
#257713=CARTESIAN_POINT('Ctrl Pts',(1.22470458087275,-2.76960549353663,
3.27459776486713));
#257714=CARTESIAN_POINT('Ctrl Pts',(2.99127266400681,-0.472126816567234,
3.43341990542186));
#257715=CARTESIAN_POINT('Ctrl Pts',(2.01819806245289,2.25776270925503,3.59224204597659));
#257716=CARTESIAN_POINT('Ctrl Pts',(-0.803300995111289,2.91981564368942,
3.75106418653132));
#257717=CARTESIAN_POINT('Ctrl Pts',(-2.88907384616146,0.907671851413923,
3.90988632708605));
#257718=CARTESIAN_POINT('Ctrl Pts',(-2.32880572754616,-1.9357891829015,
4.06870846764077));
#257719=CARTESIAN_POINT('Ctrl Pts',(0.364365768366402,-3.00630229114176,
4.22753060819551));
#257720=CARTESIAN_POINT('Ctrl Pts',(2.72382244705534,-1.32340740333668,
4.38635274875023));
#257721=CARTESIAN_POINT('Ctrl Pts',(2.58858837994239,1.5715680314311,4.54517488930497));
#257722=CARTESIAN_POINT('Ctrl Pts',(0.0825215579805379,3.02717790538921,
4.70399702985969));
#257723=CARTESIAN_POINT('Ctrl Pts',(-2.49912499469722,1.71026025481233,
4.86281917041443));
#257724=CARTESIAN_POINT('Ctrl Pts',(-2.79187639436079,-1.17304819888917,
5.02164131096916));
#257725=CARTESIAN_POINT('Ctrl Pts',(-0.527607892903676,-2.98198688623563,
5.18046345152388));
#257726=CARTESIAN_POINT('Ctrl Pts',(2.21988539775892,-2.05978753737781,
5.33928559207862));
#257727=CARTESIAN_POINT('Ctrl Pts',(2.93423311229333,0.748927180066403,
5.49810773263335));
#257728=CARTESIAN_POINT('Ctrl Pts',(0.96117945124088,2.87171550485715,5.65692987318806));
#257729=CARTESIAN_POINT('Ctrl Pts',(-1.89219791982296,2.36436099412505,
5.81575201374282));
#257730=CARTESIAN_POINT('Ctrl Pts',(-3.01255167005992,-0.308461202652475,
5.97457415429752));
#257731=CARTESIAN_POINT('Ctrl Pts',(-1.37377375204991,-2.69877037861723,
6.13339629485228));
#257732=CARTESIAN_POINT('Ctrl Pts',(1.52321417508908,-2.6173334627308,6.29221843540698));
#257733=CARTESIAN_POINT('Ctrl Pts',(3.02512280457487,-0.138736785186446,
6.45104057596173));
#257734=CARTESIAN_POINT('Ctrl Pts',(1.75638613247392,2.46692594780958,6.60986271651646));
#257735=CARTESIAN_POINT('Ctrl Pts',(-1.12098704798687,2.8131839464508,6.76868485707117));
#257736=CARTESIAN_POINT('Ctrl Pts',(-2.97167215715763,0.582906912548589,
6.92750699762592));
#257737=CARTESIAN_POINT('Ctrl Pts',(-2.10066626997162,-2.18124210039289,
7.08632913818064));
#257738=CARTESIAN_POINT('Ctrl Pts',(0.694294943026906,-2.94763810709695,
7.24515127873538));
#257739=CARTESIAN_POINT('Ctrl Pts',(2.85336626127343,-1.01435539006273,
7.40397341929009));
#257740=CARTESIAN_POINT('Ctrl Pts',(2.39910042390177,1.84795374248307,7.56279555984483));
#257741=CARTESIAN_POINT('Ctrl Pts',(-0.25245020054233,3.01776155031655,
7.72161770039956));
#257742=CARTESIAN_POINT('Ctrl Pts',(-2.67278708352791,1.42366607195971,
7.8804398409543));
#257743=CARTESIAN_POINT('Ctrl Pts',(-2.64517541912911,-1.47433472466667,
8.03926198150901));
#257744=CARTESIAN_POINT('Ctrl Pts',(-0.194904140449694,-3.02202386727147,
8.19808412206375));
#257745=CARTESIAN_POINT('Ctrl Pts',(2.43387567354607,-1.80190595871246,
8.35690626261848));
#257746=CARTESIAN_POINT('Ctrl Pts',(2.83352079279202,1.0685390938745,8.5157284031732));
#257747=CARTESIAN_POINT('Ctrl Pts',(0.638004796718893,2.96033203504042,
8.67455054372795));
#257748=CARTESIAN_POINT('Ctrl Pts',(-2.14184615254877,2.14082015525238,
8.83337268428265));
#257749=CARTESIAN_POINT('Ctrl Pts',(-2.96002600195016,-0.639423135413294,
8.99219482483741));
#257750=CARTESIAN_POINT('Ctrl Pts',(-1.06718131956222,-2.83403244679736,
9.15101696539212));
#257751=CARTESIAN_POINT('Ctrl Pts',(1.80307191778247,-2.43301202989773,
9.30983910594686));
#257752=CARTESIAN_POINT('Ctrl Pts',(3.02193013411443,0.196352088998341,
9.46866124650158));
#257753=CARTESIAN_POINT('Ctrl Pts',(1.47306714747715,2.64588152745855,9.62748338705632));
#257754=CARTESIAN_POINT('Ctrl Pts',(-1.42494654633381,2.67210464211531,
9.78630552761105));
#257755=CARTESIAN_POINT('Ctrl Pts',(-3.01788216277166,0.251004242887347,
9.94512766816578));
#257756=CARTESIAN_POINT('Ctrl Pts',(-1.84680402665019,-2.39998557609655,
10.1039498087205));
#257757=CARTESIAN_POINT('Ctrl Pts',(1.01572243403243,-2.85287991603679,
10.2627719492752));
#257758=CARTESIAN_POINT('Ctrl Pts',(2.94797043285812,-0.692882533563333,
10.42159408983));
#257759=CARTESIAN_POINT('Ctrl Pts',(2.18023533788578,2.10171114803079,10.5804162303847));
#257760=CARTESIAN_POINT('Ctrl Pts',(-0.584330691067625,2.97139252233684,
10.7392383709394));
#257761=CARTESIAN_POINT('Ctrl Pts',(-2.81372073267564,1.11963901184004,
10.8980605114941));
#257762=CARTESIAN_POINT('Ctrl Pts',(-2.46608411071298,-1.75756793246,11.0568826520489));
#257763=CARTESIAN_POINT('Ctrl Pts',(0.140186225005578,-3.02505598305908,
11.2157047926036));
#257764=CARTESIAN_POINT('Ctrl Pts',(2.61806299433025,-1.5219599324691,11.3745269331583));
#257765=CARTESIAN_POINT('Ctrl Pts',(2.69811183960188,1.37506668177329,11.5333490737131));
#257766=CARTESIAN_POINT('Ctrl Pts',(0.307017734827514,3.01269912019508,
11.6921712142678));
#257767=CARTESIAN_POINT('Ctrl Pts',(-2.36526734943941,1.89106484394342,
11.8509933548225));
#257768=CARTESIAN_POINT('Ctrl Pts',(-2.87125463620523,-0.962555293161294,
12.0098154953773));
#257769=CARTESIAN_POINT('Ctrl Pts',(-0.747521187194434,-2.93459161605465,
12.168637635932));
#257770=CARTESIAN_POINT('Ctrl Pts',(2.06085093565951,-2.21889821743003,
12.3274597764867));
#257771=CARTESIAN_POINT('Ctrl Pts',(2.98173374617193,0.529036619963464,
12.4862819170415));
#257772=CARTESIAN_POINT('Ctrl Pts',(1.17171036605948,2.79243812758522,12.6451040575962));
#257773=CARTESIAN_POINT('Ctrl Pts',(-1.71145748793473,2.49830525463062,
12.8039261981509));
#257774=CARTESIAN_POINT('Ctrl Pts',(-3.02713801855786,-0.0839719889273276,
12.9627483387056));
#257775=CARTESIAN_POINT('Ctrl Pts',(-1.57032755619116,-2.58934108309229,
13.1215704792604));
#257776=CARTESIAN_POINT('Ctrl Pts',(1.32471234232721,-2.7231880376516,13.2803926198151));
#257777=CARTESIAN_POINT('Ctrl Pts',(3.00647652798119,-0.36292528848369,
13.4392147603698));
#257778=CARTESIAN_POINT('Ctrl Pts',(1.93467313813552,2.32973297330394,13.5980369009245));
#257779=CARTESIAN_POINT('Ctrl Pts',(-0.909056016897293,2.88863861299158,
13.7568590414793));
#257780=CARTESIAN_POINT('Ctrl Pts',(-2.9202002010698,0.801901904221753,
13.915681182034));
#257781=CARTESIAN_POINT('Ctrl Pts',(-2.25679545303008,-2.01927961449252,
14.0745033225888));
#257782=CARTESIAN_POINT('Ctrl Pts',(0.473560001646884,-2.99104610515534,
14.2333254631435));
#257783=CARTESIAN_POINT('Ctrl Pts',(2.77019197521469,-1.22337741469139,
14.3921476036982));
#257784=CARTESIAN_POINT('Ctrl Pts',(2.52966434355467,1.66475649488695,14.5509697442529));
#257785=CARTESIAN_POINT('Ctrl Pts',(-0.0277287778183823,3.02817552219422,
14.7097918848077));
#257786=CARTESIAN_POINT('Ctrl Pts',(-2.55972570440915,1.61815332910488,
14.8686140253624));
#257787=CARTESIAN_POINT('Ctrl Pts',(-2.74732458357555,-1.27390090305035,
15.0274361659171));
#257788=CARTESIAN_POINT('Ctrl Pts',(-0.418707612621415,-2.99921653328682,
15.1862583064718));
#257789=CARTESIAN_POINT('Ctrl Pts',(2.29339470903158,-1.97761386189897,
15.3450804470266));
#257790=CARTESIAN_POINT('Ctrl Pts',(2.90502584796162,0.855243065428628,
15.5039025875813));
#257791=CARTESIAN_POINT('Ctrl Pts',(0.856005920238958,2.9048011538481,15.6627247281361));
#257792=CARTESIAN_POINT('Ctrl Pts',(-1.97701152892453,2.29391396782655,
15.8215468686908));
#257793=CARTESIAN_POINT('Ctrl Pts',(-2.99932638607008,-0.417919978281937,
15.9803690092455));
#257794=CARTESIAN_POINT('Ctrl Pts',(-1.27462232958634,-2.74698995243888,
16.1391911498002));
#257795=CARTESIAN_POINT('Ctrl Pts',(1.61748106752409,-2.56015055549323,
16.298013290355));
#257796=CARTESIAN_POINT('Ctrl Pts',(3.02816813644166,-0.0285240038525372,
16.4568354309097));
#257797=CARTESIAN_POINT('Ctrl Pts',(1.66542074774659,2.52922708217632,16.6156575714644));
#257798=CARTESIAN_POINT('Ctrl Pts',(-1.22264989501513,2.77051313949344,
16.7744797120191));
#257799=CARTESIAN_POINT('Ctrl Pts',(-2.99092164449118,0.474345477213988,
16.9333018525739));
#257800=CARTESIAN_POINT('Ctrl Pts',(-2.01987219202877,-2.25626512971792,
17.0921239931286));
#257801=CARTESIAN_POINT('Ctrl Pts',(0.801134995288171,-2.92041062098095,
17.2509461336833));
#257802=CARTESIAN_POINT('Ctrl Pts',(2.88839981073126,-0.909814691653167,
17.4097682742381));
#257803=CARTESIAN_POINT('Ctrl Pts',(2.33024091029762,1.93406150312561,17.5685904147928));
#257804=CARTESIAN_POINT('Ctrl Pts',(-0.362135665603684,3.00657127473531,
17.7274125553475));
#257805=CARTESIAN_POINT('Ctrl Pts',(-2.72284022410792,1.32542830115026,
17.8862346959023));
#257806=CARTESIAN_POINT('Ctrl Pts',(-2.58975306763537,-1.56964918522231,
18.045056836457));
#257807=CARTESIAN_POINT('Ctrl Pts',(-0.0847675250594005,-3.02711268095448,
18.2038789770117));
#257808=CARTESIAN_POINT('Ctrl Pts',(2.49785684645981,-1.71211958054349,
18.3627011175664));
#257809=CARTESIAN_POINT('Ctrl Pts',(2.79274359130207,1.17098861038763,18.5215232581212));
#257810=CARTESIAN_POINT('Ctrl Pts',(0.529823718786248,2.98157255671619,
18.6803453986759));
#257811=CARTESIAN_POINT('Ctrl Pts',(-2.21836475215143,2.06147587927432,
18.8391675392306));
#257812=CARTESIAN_POINT('Ctrl Pts',(-2.93477290930665,-0.746831318702741,
18.9979896797854));
#257813=CARTESIAN_POINT('Ctrl Pts',(-0.963337750715509,-2.87084744284491,
19.1568118203401));
#257814=CARTESIAN_POINT('Ctrl Pts',(1.89049801721319,-2.36605862786224,
19.3156339608948));
#257815=CARTESIAN_POINT('Ctrl Pts',(3.01267580519764,0.306789879043543,
19.4744561014495));
#257816=CARTESIAN_POINT('Ctrl Pts',(1.37597340919417,2.69667105018146,19.6332782420043));
#257817=CARTESIAN_POINT('Ctrl Pts',(-1.52165031835563,2.62055817639379,
19.792100382559));
#257818=CARTESIAN_POINT('Ctrl Pts',(-3.02430168024254,0.136680167882348,
19.9509225231137));
#257819=CARTESIAN_POINT('Ctrl Pts',(-2.18120777963231,-1.59106796283699,
20.0568039501502));
#257820=CARTESIAN_POINT('Ctrl Pts',(-1.48738611075519,-2.08582659521599,
20.1097446636685));
#257821=CARTESIAN_POINT('Ctrl Pts',(-1.20564430054384,2.47375567929493,
-0.109744663668461));
#257822=CARTESIAN_POINT('Ctrl Pts',(-2.02850526978225,2.07271460397539,
-0.056803950150218));
#257823=CARTESIAN_POINT('Ctrl Pts',(-3.2283166736487,0.391886822194973,
0.0490774768862683));
#257824=CARTESIAN_POINT('Ctrl Pts',(-2.07713778169297,-2.5062887926054,
0.207899617440998));
#257825=CARTESIAN_POINT('Ctrl Pts',(0.979209252690544,-3.10113653929458,
0.366721757995727));
#257826=CARTESIAN_POINT('Ctrl Pts',(3.13730180430125,-0.85965291879434,
0.525543898550458));
#257827=CARTESIAN_POINT('Ctrl Pts',(2.42274585431577,2.17120665958024,0.684366039105187));
#257828=CARTESIAN_POINT('Ctrl Pts',(-0.511137916257496,3.21243959117606,
0.843188179659916));
#257829=CARTESIAN_POINT('Ctrl Pts',(-2.97667894972426,1.3120251304179,1.00201032021465));
#257830=CARTESIAN_POINT('Ctrl Pts',(-2.71604937874059,-1.79033691992615,
1.16083246076937));
#257831=CARTESIAN_POINT('Ctrl Pts',(0.0322072601030219,-3.25281485309624,
1.31965460132411));
#257832=CARTESIAN_POINT('Ctrl Pts',(2.75093689085934,-1.73618922250611,
1.47847674187883));
#257833=CARTESIAN_POINT('Ctrl Pts',(2.95015745737327,1.37061689904108,1.63729888243357));
#257834=CARTESIAN_POINT('Ctrl Pts',(0.44738391073424,3.22208236453155,1.79612102298829));
#257835=CARTESIAN_POINT('Ctrl Pts',(-2.46513482132621,2.1225229677134,1.95494316354302));
#257836=CARTESIAN_POINT('Ctrl Pts',(-3.11989145900001,-0.921015853466312,
2.11376530409775));
#257837=CARTESIAN_POINT('Ctrl Pts',(-0.91720506615342,-3.12101279471662,
2.27258744465248));
#257838=CARTESIAN_POINT('Ctrl Pts',(2.12552923826585,-2.46254249219458,
2.43140958520721));
#257839=CARTESIAN_POINT('Ctrl Pts',(3.22153706957644,0.451318695269874,
2.59023172576194));
#257840=CARTESIAN_POINT('Ctrl Pts',(1.36700780886653,2.95182628626936,2.74905386631667));
#257841=CARTESIAN_POINT('Ctrl Pts',(-1.73953459221347,2.74881952664486,
2.9078760068714));
#257842=CARTESIAN_POINT('Ctrl Pts',(-3.25287449544242,0.0282276064683039,
3.06669814742613));
#257843=CARTESIAN_POINT('Ctrl Pts',(-1.78697616900445,-2.71821731003186,
3.22552028798086));
#257844=CARTESIAN_POINT('Ctrl Pts',(1.31557541390151,-2.97510513997333,
3.38434242853558));
#257845=CARTESIAN_POINT('Ctrl Pts',(3.21321960781657,-0.507157760181518,
3.54316456909033));
#257846=CARTESIAN_POINT('Ctrl Pts',(2.16794465605303,2.4252845601369,3.70198670964504));
#257847=CARTESIAN_POINT('Ctrl Pts',(-0.862904455193533,3.13646060768837,
3.86080885019978));
#257848=CARTESIAN_POINT('Ctrl Pts',(-3.10343782518346,0.975019437552611,
4.01963099075451));
#257849=CARTESIAN_POINT('Ctrl Pts',(-2.50159884004805,-2.07942118882818,
4.17845313130924));
#257850=CARTESIAN_POINT('Ctrl Pts',(0.391401039905119,-3.22936440571122,
4.33727527186397));
#257851=CARTESIAN_POINT('Ctrl Pts',(2.92592507543778,-1.42160180470976,
4.4960974124187));
#257852=CARTESIAN_POINT('Ctrl Pts',(2.78065688864868,1.6881754961274,4.65491955297343));
#257853=CARTESIAN_POINT('Ctrl Pts',(0.0886445061867101,3.25178895223693,
4.81374169352816));
#257854=CARTESIAN_POINT('Ctrl Pts',(-2.68455548434994,1.83715842803552,
4.97256383408289));
#257855=CARTESIAN_POINT('Ctrl Pts',(-2.99902850077992,-1.26008622314477,
5.13138597463762));
#257856=CARTESIAN_POINT('Ctrl Pts',(-0.566755430595232,-3.20324484237067,
5.29020811519235));
#257857=CARTESIAN_POINT('Ctrl Pts',(2.38459682161839,-2.21261999371634,
5.44903025574707));
#257858=CARTESIAN_POINT('Ctrl Pts',(3.15194782601206,0.804496202827806,
5.60785239630181));
#257859=CARTESIAN_POINT('Ctrl Pts',(1.03249720312042,3.08479152680039,5.76667453685653));
#257860=CARTESIAN_POINT('Ctrl Pts',(-2.03259553400278,2.53979224217656,
5.92549667741127));
#257861=CARTESIAN_POINT('Ctrl Pts',(-3.23607747707985,-0.331348457979058,
6.08431881796598));
#257862=CARTESIAN_POINT('Ctrl Pts',(-1.47570524409423,-2.89901418948268,
6.24314095852073));
#257863=CARTESIAN_POINT('Ctrl Pts',(1.63623387235594,-2.81153480384359,
6.40196309907545));
#257864=CARTESIAN_POINT('Ctrl Pts',(3.24958136671251,-0.149030800117508,
6.56078523963019));
#257865=CARTESIAN_POINT('Ctrl Pts',(1.88670676119597,2.64996732725637,6.71960738018491));
#257866=CARTESIAN_POINT('Ctrl Pts',(-1.20416223035814,3.02191703414368,
6.87842952073964));
#257867=CARTESIAN_POINT('Ctrl Pts',(-3.19216477931873,0.626157536044905,
7.03725166129438));
#257868=CARTESIAN_POINT('Ctrl Pts',(-2.25653185327151,-2.3430862624837,
7.1960738018491));
#257869=CARTESIAN_POINT('Ctrl Pts',(0.745810354029566,-3.16634744683699,
7.35489594240383));
#257870=CARTESIAN_POINT('Ctrl Pts',(3.06508080300672,-1.08961869904501,
7.51371808295856));
#257871=CARTESIAN_POINT('Ctrl Pts',(2.57710927390893,1.98506851987568,7.67254022351329));
#257872=CARTESIAN_POINT('Ctrl Pts',(-0.271181542271447,3.24167392089336,
7.83136236406802));
#257873=CARTESIAN_POINT('Ctrl Pts',(-2.8711029815673,1.5292994826077,7.99018450462276));
#257874=CARTESIAN_POINT('Ctrl Pts',(-2.84144258232714,-1.58372765638758,
8.14900664517747));
#257875=CARTESIAN_POINT('Ctrl Pts',(-0.209365670095335,-3.24625249394657,
8.30782878573222));
#257876=CARTESIAN_POINT('Ctrl Pts',(2.61446478327733,-1.93560407502967,
8.46665092628693));
#257877=CARTESIAN_POINT('Ctrl Pts',(3.04376283717295,1.14782273427289,8.62547306684167));
#257878=CARTESIAN_POINT('Ctrl Pts',(0.685343582136768,3.17998324094527,
8.7842952073964));
#257879=CARTESIAN_POINT('Ctrl Pts',(-2.30076720758629,2.29966508317285,
8.94311734795113));
#257880=CARTESIAN_POINT('Ctrl Pts',(-3.17965450076118,-0.686867158960146,
9.10193948850586));
#257881=CARTESIAN_POINT('Ctrl Pts',(-1.14636421559767,-3.04431245496679,
9.2607616290606));
#257882=CARTESIAN_POINT('Ctrl Pts',(1.93685654612355,-2.61353705885476,
9.4195837696153));
#257883=CARTESIAN_POINT('Ctrl Pts',(3.24615180596125,0.210921053769822,
9.57840591017007));
#257884=CARTESIAN_POINT('Ctrl Pts',(1.58236602729615,2.84220108259916,9.73722805072475));
#257885=CARTESIAN_POINT('Ctrl Pts',(-1.53067496583115,2.87036990425393,
9.89605019127954));
#257886=CARTESIAN_POINT('Ctrl Pts',(-3.24180348257135,0.269628297211287,
10.0548723318342));
#257887=CARTESIAN_POINT('Ctrl Pts',(-1.98383349723732,-2.57806010277262,
10.213694472389));
#257888=CARTESIAN_POINT('Ctrl Pts',(1.09108717516923,-3.06455837184578,
10.3725166129437));
#257889=CARTESIAN_POINT('Ctrl Pts',(3.16670443055993,-0.744293146375072,
10.5313387534984));
#257890=CARTESIAN_POINT('Ctrl Pts',(2.34200480004562,2.2576542593657,10.6901608940532));
#257891=CARTESIAN_POINT('Ctrl Pts',(-0.62768695631793,3.19186439610727,
10.8489830346079));
#257892=CARTESIAN_POINT('Ctrl Pts',(-3.02249364892158,1.20271417240239,
11.0078051751626));
#257893=CARTESIAN_POINT('Ctrl Pts',(-2.64906302739169,-1.88797624857284,
11.1666273157173));
#257894=CARTESIAN_POINT('Ctrl Pts',(0.150587785712017,-3.24950958716283,
11.3254494562721));
#257895=CARTESIAN_POINT('Ctrl Pts',(2.81231846534928,-1.63488656723465,
11.4842715968268));
#257896=CARTESIAN_POINT('Ctrl Pts',(2.89830678808057,1.47709410683101,11.6430937373815));
#257897=CARTESIAN_POINT('Ctrl Pts',(0.329797887489733,3.23623586774451,
11.8019158779363));
#257898=CARTESIAN_POINT('Ctrl Pts',(-2.5407658473924,2.03137838597176,11.960738018491));
#257899=CARTESIAN_POINT('Ctrl Pts',(-3.08429646254003,-1.03397512998715,
12.1195601590457));
#257900=CARTESIAN_POINT('Ctrl Pts',(-0.802985887864231,-3.15233293009474,
12.2783822996005));
#257901=CARTESIAN_POINT('Ctrl Pts',(2.21376229419958,-2.38353639432022,
12.4372044401552));
#257902=CARTESIAN_POINT('Ctrl Pts',(3.20297291977867,0.568290166581644,
12.5960265807099));
#257903=CARTESIAN_POINT('Ctrl Pts',(1.25864912557356,2.99963191357903,12.7548487212647));
#257904=CARTESIAN_POINT('Ctrl Pts',(-1.8384444936591,2.68367492107434,12.9136708618194));
#257905=CARTESIAN_POINT('Ctrl Pts',(-3.25174610587588,-0.0902025564487242,
13.0724930023741));
#257906=CARTESIAN_POINT('Ctrl Pts',(-1.6868429799005,-2.78146544099136,
13.2313151429288));
#257907=CARTESIAN_POINT('Ctrl Pts',(1.42300356777929,-2.92524359402021,
13.3901372834835));
#257908=CARTESIAN_POINT('Ctrl Pts',(3.22955157060447,-0.389853679057881,
13.5489594240383));
#257909=CARTESIAN_POINT('Ctrl Pts',(2.07822233558811,2.50259488573989,13.707781564593));
#257910=CARTESIAN_POINT('Ctrl Pts',(-0.976506305575396,3.10297029851087,
13.8666037051478));
#257911=CARTESIAN_POINT('Ctrl Pts',(-3.13687369852085,0.86140155432683,
14.0254258457025));
#257912=CARTESIAN_POINT('Ctrl Pts',(-2.42424553527463,-2.16910645726973,
14.1842479862572));
#257913=CARTESIAN_POINT('Ctrl Pts',(0.508697284964691,-3.21297623871397,
14.3430701268119));
#257914=CARTESIAN_POINT('Ctrl Pts',(2.97573513751593,-1.31414977442438,
14.5018922673667));
#257915=CARTESIAN_POINT('Ctrl Pts',(2.71736079686443,1.78827837260592,14.6607144079214));
#257916=CARTESIAN_POINT('Ctrl Pts',(-0.0297862022606204,3.25286059037863,
14.8195365484761));
#257917=CARTESIAN_POINT('Ctrl Pts',(-2.749652655543,1.73821733742212,14.9783586890308));
#257918=CARTESIAN_POINT('Ctrl Pts',(-2.95117102737023,-1.36842201292796,
15.1371808295856));
#257919=CARTESIAN_POINT('Ctrl Pts',(-0.449774949307054,-3.22175289762314,
15.2960029701403));
#257920=CARTESIAN_POINT('Ctrl Pts',(2.46356038892555,-2.12434918227474,
15.4548251106951));
#257921=CARTESIAN_POINT('Ctrl Pts',(3.12057343625127,0.918700531834268,
15.6136472512498));
#257922=CARTESIAN_POINT('Ctrl Pts',(0.919519989072005,3.12033207024676,
15.7724693918045));
#257923=CARTESIAN_POINT('Ctrl Pts',(-2.12370215729863,2.46411817577049,
15.9312915323592));
#257924=CARTESIAN_POINT('Ctrl Pts',(-3.22187090128139,-0.448928873944568,
16.090113672914));
#257925=CARTESIAN_POINT('Ctrl Pts',(-1.3691969679894,-2.95081156721713,
16.2489358134687));
#257926=CARTESIAN_POINT('Ctrl Pts',(1.73749519526536,-2.7501090297981,16.4077579540234));
#257927=CARTESIAN_POINT('Ctrl Pts',(3.25285265661678,-0.0306404326076004,
16.5665800945781));
#257928=CARTESIAN_POINT('Ctrl Pts',(1.78899191180913,2.716891091494,16.7254022351329));
#257929=CARTESIAN_POINT('Ctrl Pts',(-1.31336827412284,2.97608013159495,
16.8842243756876));
#257930=CARTESIAN_POINT('Ctrl Pts',(-3.21284254329687,0.509541041377854,
17.0430465162423));
#257931=CARTESIAN_POINT('Ctrl Pts',(-2.16974300297203,-2.42367586294563,
17.2018686567971));
#257932=CARTESIAN_POINT('Ctrl Pts',(0.860577742157333,-3.13709973120337,
17.3606907973518));
#257933=CARTESIAN_POINT('Ctrl Pts',(3.10271377756093,-0.977321272606305,
17.5195129379065));
#257934=CARTESIAN_POINT('Ctrl Pts',(2.50314051072665,2.07756531838256,17.6783350784613));
#257935=CARTESIAN_POINT('Ctrl Pts',(-0.389005467608808,3.22965334739393,
17.837157219016));
#257936=CARTESIAN_POINT('Ctrl Pts',(-2.92486997334968,1.42377264943353,
17.9959793595707));
#257937=CARTESIAN_POINT('Ctrl Pts',(-2.78190799403171,-1.68611427505029,
18.1548015001254));
#257938=CARTESIAN_POINT('Ctrl Pts',(-0.091057119902321,-3.25171888826882,
18.3136236406802));
#257939=CARTESIAN_POINT('Ctrl Pts',(2.6831932418399,-1.83915571232477,18.4724457812349));
#257940=CARTESIAN_POINT('Ctrl Pts',(2.99996004214327,1.25787381695499,18.6312679217897));
#257941=CARTESIAN_POINT('Ctrl Pts',(0.569135666693086,3.20279977036102,
18.7900900623443));
#257942=CARTESIAN_POINT('Ctrl Pts',(-2.38296334689664,2.2144336074841,18.9489122028991));
#257943=CARTESIAN_POINT('Ctrl Pts',(-3.15252767497344,-0.802244832396076,
19.1077343434538));
#257944=CARTESIAN_POINT('Ctrl Pts',(-1.0348156444564,-3.0838590561794,19.2665564840085));
#257945=CARTESIAN_POINT('Ctrl Pts',(2.03076950173803,-2.54161583722253,
19.4253786245633));
#257946=CARTESIAN_POINT('Ctrl Pts',(3.23621082281705,0.329553125224593,
19.584200765118));
#257947=CARTESIAN_POINT('Ctrl Pts',(1.47806811176305,2.89675909472846,19.7430229056727));
#257948=CARTESIAN_POINT('Ctrl Pts',(-1.63455398032195,2.81499878534423,
19.9018450462275));
#257949=CARTESIAN_POINT('Ctrl Pts',(-3.24869931646117,0.146821585582566,
20.0606671867822));
#257950=CARTESIAN_POINT('Ctrl Pts',(-2.34304939518568,-1.70912228666858,
20.1665486138187));
#257951=CARTESIAN_POINT('Ctrl Pts',(-1.59774743137951,-2.24059110187423,
20.2194893273369));
#257952=CARTESIAN_POINT('Ctrl Pts',(-1.28892185405322,2.64462557919718,
0.));
#257953=CARTESIAN_POINT('Ctrl Pts',(-2.16862035685408,2.21588336549518,
0.0529407135182432));
#257954=CARTESIAN_POINT('Ctrl Pts',(-3.45130641814776,0.41895564820797,
0.15882214055473));
#257955=CARTESIAN_POINT('Ctrl Pts',(-2.22061206567813,-2.6794058545299,
0.317644281109459));
#257956=CARTESIAN_POINT('Ctrl Pts',(1.04684624222471,-3.31534156143464,
0.476466421664189));
#257957=CARTESIAN_POINT('Ctrl Pts',(3.35400487233295,-0.91903178527438,
0.635288562218918));
#257958=CARTESIAN_POINT('Ctrl Pts',(2.59009234899204,2.32117856977925,0.794110702773649));
#257959=CARTESIAN_POINT('Ctrl Pts',(-0.54644378147213,3.43433265684159,
0.952932843328378));
#257960=CARTESIAN_POINT('Ctrl Pts',(-3.1822873040325,1.4026507344661,1.11175498388311));
#257961=CARTESIAN_POINT('Ctrl Pts',(-2.9036552483741,-1.91400098782886,
1.27057712443784));
#257962=CARTESIAN_POINT('Ctrl Pts',(0.0344319144437711,-3.47749676206612,
1.42939926499257));
#257963=CARTESIAN_POINT('Ctrl Pts',(2.94095254806946,-1.85611314269922,
1.5882214055473));
#257964=CARTESIAN_POINT('Ctrl Pts',(3.15393389077631,1.46528961644145,1.74704354610203));
#257965=CARTESIAN_POINT('Ctrl Pts',(0.478286091044485,3.44464148615879,
1.90586568665676));
#257966=CARTESIAN_POINT('Ctrl Pts',(-2.63540925210006,2.26913214584243,
2.06468782721148));
#257967=CARTESIAN_POINT('Ctrl Pts',(-3.33539194102706,-0.984633246245777,
2.22350996776621));
#257968=CARTESIAN_POINT('Ctrl Pts',(-0.980559236153007,-3.33659073084442,
2.38233210832095));
#257969=CARTESIAN_POINT('Ctrl Pts',(2.272346068732,-2.63263786283614,2.54115424887567));
#257970=CARTESIAN_POINT('Ctrl Pts',(3.44405852600693,0.482492663228878,
2.6999763894304));
#257971=CARTESIAN_POINT('Ctrl Pts',(1.46143123532763,3.15571799080802,2.85879852998513));
#257972=CARTESIAN_POINT('Ctrl Pts',(-1.85968958736347,2.93868893100779,
3.01762067053986));
#257973=CARTESIAN_POINT('Ctrl Pts',(-3.47756052409227,0.0301773739138614,
3.17644281109459));
#257974=CARTESIAN_POINT('Ctrl Pts',(-1.91040809952256,-2.90597292533581,
3.33526495164932));
#257975=CARTESIAN_POINT('Ctrl Pts',(1.40644624693028,-3.18060478641004,
3.49408709220405));
#257976=CARTESIAN_POINT('Ctrl Pts',(3.43516655162632,-0.542188703795803,
3.65290923275879));
#257977=CARTESIAN_POINT('Ctrl Pts',(2.31769124965316,2.59280641101876,3.81173137331351));
#257978=CARTESIAN_POINT('Ctrl Pts',(-0.922507915275779,3.35310557168732,
3.97055351386824));
#257979=CARTESIAN_POINT('Ctrl Pts',(-3.31780180420545,1.0423670236913,4.12937565442297));
#257980=CARTESIAN_POINT('Ctrl Pts',(-2.67439195254995,-2.22305319475486,
4.2881977949777));
#257981=CARTESIAN_POINT('Ctrl Pts',(0.418436311443839,-3.45242652028068,
4.44701993553243));
#257982=CARTESIAN_POINT('Ctrl Pts',(3.12802770382022,-1.51979620608285,
4.60584207608716));
#257983=CARTESIAN_POINT('Ctrl Pts',(2.97272539735497,1.80478296082371,4.76466421664189));
#257984=CARTESIAN_POINT('Ctrl Pts',(0.0947674543928817,3.47639999908466,
4.92348635719661));
#257985=CARTESIAN_POINT('Ctrl Pts',(-2.86998597400267,1.96405660125871,
5.08230849775136));
#257986=CARTESIAN_POINT('Ctrl Pts',(-3.20618060719906,-1.34712424740037,
5.24113063830607));
#257987=CARTESIAN_POINT('Ctrl Pts',(-0.605902968286784,-3.42450279850571,
5.39995277886081));
#257988=CARTESIAN_POINT('Ctrl Pts',(2.54930824547785,-2.36545245005487,
5.55877491941554));
#257989=CARTESIAN_POINT('Ctrl Pts',(3.3696625397308,0.860065225589209,5.71759705997026));
#257990=CARTESIAN_POINT('Ctrl Pts',(1.10381495499996,3.29786754874362,5.87641920052501));
#257991=CARTESIAN_POINT('Ctrl Pts',(-2.17299314818259,2.71522349022807,
6.03524134107972));
#257992=CARTESIAN_POINT('Ctrl Pts',(-3.45960328409978,-0.354235713305642,
6.19406348163447));
#257993=CARTESIAN_POINT('Ctrl Pts',(-1.57763673613854,-3.09925800034814,
6.35288562218917));
#257994=CARTESIAN_POINT('Ctrl Pts',(1.7492535696228,-3.00573614495637,6.51170776274393));
#257995=CARTESIAN_POINT('Ctrl Pts',(3.47403992885015,-0.159324815048575,
6.67052990329863));
#257996=CARTESIAN_POINT('Ctrl Pts',(2.01702738991803,2.83300870670317,6.82935204385339));
#257997=CARTESIAN_POINT('Ctrl Pts',(-1.28733741272941,3.23065012183655,
6.98817418440809));
#257998=CARTESIAN_POINT('Ctrl Pts',(-3.41265740147983,0.669408159541225,
7.14699632496285));
#257999=CARTESIAN_POINT('Ctrl Pts',(-2.41239743657142,-2.50493042457452,
7.30581846551755));
#258000=CARTESIAN_POINT('Ctrl Pts',(0.797325765032234,-3.38505678657703,
7.4646406060723));
#258001=CARTESIAN_POINT('Ctrl Pts',(3.27679534473999,-1.16488200802731,
7.62346274662702));
#258002=CARTESIAN_POINT('Ctrl Pts',(2.75511812391609,2.12218329726829,7.78228488718175));
#258003=CARTESIAN_POINT('Ctrl Pts',(-0.289912884000569,3.46558629147016,
7.94110702773649));
#258004=CARTESIAN_POINT('Ctrl Pts',(-3.06941887960669,1.6349328932557,8.09992916829121));
#258005=CARTESIAN_POINT('Ctrl Pts',(-3.03770974552517,-1.6931205881085,
8.25875130884594));
#258006=CARTESIAN_POINT('Ctrl Pts',(-0.223827199740972,-3.47048112062168,
8.41757344940067));
#258007=CARTESIAN_POINT('Ctrl Pts',(2.79505389300859,-2.06930219134687,
8.5763955899554));
#258008=CARTESIAN_POINT('Ctrl Pts',(3.25400488155389,1.22710637467128,8.73521773051013));
#258009=CARTESIAN_POINT('Ctrl Pts',(0.73268236755464,3.39963444685013,8.89403987106487));
#258010=CARTESIAN_POINT('Ctrl Pts',(-2.45968826262381,2.45851001109332,
9.05286201161959));
#258011=CARTESIAN_POINT('Ctrl Pts',(-3.3992829995722,-0.734311182506995,
9.21168415217432));
#258012=CARTESIAN_POINT('Ctrl Pts',(-1.22554711163312,-3.25459246313622,
9.37050629272904));
#258013=CARTESIAN_POINT('Ctrl Pts',(2.07064117446462,-2.79406208781179,
9.52932843328378));
#258014=CARTESIAN_POINT('Ctrl Pts',(3.47037347780808,0.225490018541298,
9.68815057383851));
#258015=CARTESIAN_POINT('Ctrl Pts',(1.69166490711515,3.03852063773977,9.84697271439324));
#258016=CARTESIAN_POINT('Ctrl Pts',(-1.63640338532848,3.06863516639254,
10.005794854948));
#258017=CARTESIAN_POINT('Ctrl Pts',(-3.46572480237104,0.288252351535223,
10.1646169955027));
#258018=CARTESIAN_POINT('Ctrl Pts',(-2.12086296782444,-2.7561346294487,
10.3234391360574));
#258019=CARTESIAN_POINT('Ctrl Pts',(1.16645191630603,-3.27623682765478,
10.4822612766121));
#258020=CARTESIAN_POINT('Ctrl Pts',(3.38543842826175,-0.795703759186809,
10.6410834171669));
#258021=CARTESIAN_POINT('Ctrl Pts',(2.50377426220545,2.41359737070061,10.7999055577216));
#258022=CARTESIAN_POINT('Ctrl Pts',(-0.671043221568228,3.41233626987769,
10.9587276982764));
#258023=CARTESIAN_POINT('Ctrl Pts',(-3.23126656516753,1.28578933296473,
11.1175498388311));
#258024=CARTESIAN_POINT('Ctrl Pts',(-2.83204194407039,-2.01838456468568,
11.2763719793858));
#258025=CARTESIAN_POINT('Ctrl Pts',(0.160989346418449,-3.47396319126659,
11.4351941199405));
#258026=CARTESIAN_POINT('Ctrl Pts',(3.00657393636832,-1.7478132020002,11.5940162604952));
#258027=CARTESIAN_POINT('Ctrl Pts',(3.09850173655927,1.57912153188873,11.75283840105));
#258028=CARTESIAN_POINT('Ctrl Pts',(0.352578040151959,3.45977261529396,
11.9116605416047));
#258029=CARTESIAN_POINT('Ctrl Pts',(-2.7162643453454,2.1716919280001,12.0704826821594));
#258030=CARTESIAN_POINT('Ctrl Pts',(-3.29733828887482,-1.105394966813,12.2293048227142));
#258031=CARTESIAN_POINT('Ctrl Pts',(-0.858450588534032,-3.37007424413483,
12.3881269632689));
#258032=CARTESIAN_POINT('Ctrl Pts',(2.36667365273965,-2.54817457121041,
12.5469491038237));
#258033=CARTESIAN_POINT('Ctrl Pts',(3.4242120933854,0.607543713199829,12.7057712443784));
#258034=CARTESIAN_POINT('Ctrl Pts',(1.34558788508765,3.20682569957283,12.8645933849331));
#258035=CARTESIAN_POINT('Ctrl Pts',(-1.96543149938347,2.86904458751805,
13.0234155254878));
#258036=CARTESIAN_POINT('Ctrl Pts',(-3.4763541931939,-0.0964331239701206,
13.1822376660426));
#258037=CARTESIAN_POINT('Ctrl Pts',(-1.80335840360983,-2.97358979889043,
13.3410598065973));
#258038=CARTESIAN_POINT('Ctrl Pts',(1.52129479323137,-3.12729915038881,
13.499881947152));
#258039=CARTESIAN_POINT('Ctrl Pts',(3.45262661322776,-0.41678206963207,
13.6587040877068));
#258040=CARTESIAN_POINT('Ctrl Pts',(2.2217715330407,2.67545679817584,13.8175262282615));
#258041=CARTESIAN_POINT('Ctrl Pts',(-1.0439565942535,3.31730198403016,13.9763483688162));
#258042=CARTESIAN_POINT('Ctrl Pts',(-3.3535471959719,0.920901204431906,
14.1351705093709));
#258043=CARTESIAN_POINT('Ctrl Pts',(-2.59169561751918,-2.31893330004694,
14.2939926499257));
#258044=CARTESIAN_POINT('Ctrl Pts',(0.543834568282501,-3.4349063722726,
14.4528147904804));
#258045=CARTESIAN_POINT('Ctrl Pts',(3.18127829981716,-1.40492213415736,
14.6116369310352));
#258046=CARTESIAN_POINT('Ctrl Pts',(2.90505725017418,1.9118002503249,14.7704590715898));
#258047=CARTESIAN_POINT('Ctrl Pts',(-0.0318436267028579,3.47754565856303,
14.9292812121446));
#258048=CARTESIAN_POINT('Ctrl Pts',(-2.93957960667686,1.85828134573937,
15.0881033526993));
#258049=CARTESIAN_POINT('Ctrl Pts',(-3.15501747116491,-1.46294312280557,
15.2469254932541));
#258050=CARTESIAN_POINT('Ctrl Pts',(-0.480842285992692,-3.44428926195945,
15.4057476338088));
#258051=CARTESIAN_POINT('Ctrl Pts',(2.63372606881953,-2.27108450265052,
15.5645697743635));
#258052=CARTESIAN_POINT('Ctrl Pts',(3.33612102454093,0.982157998239916,
15.7233919149182));
#258053=CARTESIAN_POINT('Ctrl Pts',(0.98303405790505,3.3358629866454,15.882214055473));
#258054=CARTESIAN_POINT('Ctrl Pts',(-2.27039278567272,2.63432238371444,
16.0410361960277));
#258055=CARTESIAN_POINT('Ctrl Pts',(-3.44441541649269,-0.479937769607203,
16.1998583365824));
#258056=CARTESIAN_POINT('Ctrl Pts',(-1.46377160639246,-3.15463318199537,
16.3586804771372));
#258057=CARTESIAN_POINT('Ctrl Pts',(1.85750932300663,-2.94006750410297,
16.5175026176919));
#258058=CARTESIAN_POINT('Ctrl Pts',(3.47753717679189,-0.0327568613626608,
16.6763247582466));
#258059=CARTESIAN_POINT('Ctrl Pts',(1.91256307587166,2.90455510081167,16.8351468988013));
#258060=CARTESIAN_POINT('Ctrl Pts',(-1.40408665323054,3.18164712369646,
16.9939690393561));
#258061=CARTESIAN_POINT('Ctrl Pts',(-3.43476344210255,0.544736605541722,
17.1527911799108));
#258062=CARTESIAN_POINT('Ctrl Pts',(-2.3196138139153,-2.59108659617335,
17.3116133204655));
#258063=CARTESIAN_POINT('Ctrl Pts',(0.920020489026498,-3.35378884142579,
17.4704354610203));
#258064=CARTESIAN_POINT('Ctrl Pts',(3.31702774439061,-1.04482785355944,
17.629257601575));
#258065=CARTESIAN_POINT('Ctrl Pts',(2.67604011115567,2.22106913363951,17.7880797421297));
#258066=CARTESIAN_POINT('Ctrl Pts',(-0.415875269613933,3.45273542005255,
17.9469018826845));
#258067=CARTESIAN_POINT('Ctrl Pts',(-3.12689972259143,1.5221169977168,18.1057240232392));
#258068=CARTESIAN_POINT('Ctrl Pts',(-2.97406292042806,-1.80257936487827,
18.2645461637939));
#258069=CARTESIAN_POINT('Ctrl Pts',(-0.0973467147452378,-3.47632509558314,
18.4233683043487));
#258070=CARTESIAN_POINT('Ctrl Pts',(2.86852963721998,-1.96619184410605,
18.5821904449033));
#258071=CARTESIAN_POINT('Ctrl Pts',(3.20717649298447,1.34475902352235,18.7410125854581));
#258072=CARTESIAN_POINT('Ctrl Pts',(0.608447614599921,3.42402698400585,
18.8998347260128));
#258073=CARTESIAN_POINT('Ctrl Pts',(-2.54756194164184,2.36739133569388,
19.0586568665676));
#258074=CARTESIAN_POINT('Ctrl Pts',(-3.37028244064023,-0.85765834608941,
19.2174790071223));
#258075=CARTESIAN_POINT('Ctrl Pts',(-1.10629353819729,-3.2968706695139,
19.376301147677));
#258076=CARTESIAN_POINT('Ctrl Pts',(2.17104098626288,-2.71717304658282,
19.5351232882318));
#258077=CARTESIAN_POINT('Ctrl Pts',(3.45974584043646,0.352316371405642,
19.6939454287865));
#258078=CARTESIAN_POINT('Ctrl Pts',(1.58016281433192,3.09684713927545,19.8527675693412));
#258079=CARTESIAN_POINT('Ctrl Pts',(-1.74745764228828,3.00943939429467,
20.0115897098959));
#258080=CARTESIAN_POINT('Ctrl Pts',(-3.4730969526798,0.156963003282784,
20.1704118504506));
#258081=CARTESIAN_POINT('Ctrl Pts',(-2.50489101073904,-1.82717661050017,
20.2762932774871));
#258082=CARTESIAN_POINT('Ctrl Pts',(-1.70810875200383,-2.39535560853246,
20.3292339910054));
#258083=CARTESIAN_POINT('',(-1.28892185405321,2.64462557919718,20.));
#258084=CARTESIAN_POINT('Ctrl Pts',(-1.29201753387187,2.6484941502042,20.));
#258085=CARTESIAN_POINT('Ctrl Pts',(-1.35308056853875,2.61168945411392,
20.));
#258086=CARTESIAN_POINT('Ctrl Pts',(-1.41257524201938,2.57259309505077,
20.));
#258087=CARTESIAN_POINT('Ctrl Pts',(-1.47035924820557,2.53120495213521,
20.));
#258088=CARTESIAN_POINT('Ctrl Pts',(-1.54864379104185,2.47513317620905,
20.));
#258089=CARTESIAN_POINT('Ctrl Pts',(-1.62379024837904,2.41485613876148,
20.));
#258090=CARTESIAN_POINT('Ctrl Pts',(-1.6956508900262,2.35075252758899,20.));
#258091=CARTESIAN_POINT('Ctrl Pts',(-1.76862788507419,2.28565306830413,
20.));
#258092=CARTESIAN_POINT('Ctrl Pts',(-1.83821666035171,2.21660632168619,
20.));
#258093=CARTESIAN_POINT('Ctrl Pts',(-1.90421889121248,2.14397855279972,
20.));
#258094=CARTESIAN_POINT('Ctrl Pts',(-1.96614898753727,2.0758316937567,20.));
#258095=CARTESIAN_POINT('Ctrl Pts',(-2.02492131194806,2.00453113467257,
20.));
#258096=CARTESIAN_POINT('Ctrl Pts',(-2.08033244291902,1.93036652625872,
20.));
#258097=CARTESIAN_POINT('Ctrl Pts',(-2.08908421298837,1.91865278591904,
20.));
#258098=CARTESIAN_POINT('Ctrl Pts',(-2.09775205259584,1.90686758723073,
20.));
#258099=CARTESIAN_POINT('Ctrl Pts',(-2.10633506565414,1.89501206141369,
20.));
#258100=CARTESIAN_POINT('Ctrl Pts',(-2.1147494360715,1.883389477941,20.));
#258101=CARTESIAN_POINT('Ctrl Pts',(-2.12307703147204,1.87170653313929,
20.));
#258102=CARTESIAN_POINT('Ctrl Pts',(-2.131315873543,1.85996662408695,20.));
#258103=CARTESIAN_POINT('Ctrl Pts',(-2.18649728066684,1.78133607194937,
20.));
#258104=CARTESIAN_POINT('Ctrl Pts',(-2.2377236591346,1.70012099926416,20.));
#258105=CARTESIAN_POINT('Ctrl Pts',(-2.28483930387176,1.61668443511336,
20.));
#258106=CARTESIAN_POINT('Ctrl Pts',(-2.33175427875346,1.53360323494751,
20.));
#258107=CARTESIAN_POINT('Ctrl Pts',(-2.37459374927346,1.44831846308543,
20.));
#258108=CARTESIAN_POINT('Ctrl Pts',(-2.41315551737691,1.3611718656051,20.));
#258109=CARTESIAN_POINT('Ctrl Pts',(-2.45102518317753,1.27558936551363,
20.));
#258110=CARTESIAN_POINT('Ctrl Pts',(-2.48476946641423,1.18821040330778,
20.));
#258111=CARTESIAN_POINT('Ctrl Pts',(-2.51414698808105,1.09935608424961,
20.));
#258112=CARTESIAN_POINT('Ctrl Pts',(-2.52719508595624,1.05989122179956,
20.));
#258113=CARTESIAN_POINT('Ctrl Pts',(-2.53938106790202,1.02013535678853,
20.));
#258114=CARTESIAN_POINT('Ctrl Pts',(-2.55068042718563,0.980117124868435,
20.));
#258115=CARTESIAN_POINT('Ctrl Pts',(-2.55535533199412,0.963560307783975,
20.));
#258116=CARTESIAN_POINT('Ctrl Pts',(-2.55987844483971,0.946958586108546,
20.));
#258117=CARTESIAN_POINT('Ctrl Pts',(-2.56424792226785,0.930314016077816,
20.));
#258118=CARTESIAN_POINT('Ctrl Pts',(-2.56773342049482,0.917036771765441,
20.));
#258119=CARTESIAN_POINT('Ctrl Pts',(-2.57112065866752,0.903733935297233,
20.));
#258120=CARTESIAN_POINT('Ctrl Pts',(-2.574406132533,0.890417896529939,20.));
#258121=CARTESIAN_POINT('Ctrl Pts',(-2.59638017612545,0.801357009628399,
20.));
#258122=CARTESIAN_POINT('Ctrl Pts',(-2.61384334169276,0.711566154968481,
20.));
#258123=CARTESIAN_POINT('Ctrl Pts',(-2.62661790150812,0.621356934352257,
20.));
#258124=CARTESIAN_POINT('Ctrl Pts',(-2.63902788351211,0.5337222275113,20.));
#258125=CARTESIAN_POINT('Ctrl Pts',(-2.64701305177373,0.445691945839366,
20.));
#258126=CARTESIAN_POINT('Ctrl Pts',(-2.65036239442747,0.357554648287183,
20.));
#258127=CARTESIAN_POINT('Ctrl Pts',(-2.65333726456503,0.279271521835412,
20.));
#258128=CARTESIAN_POINT('Ctrl Pts',(-2.65265441549259,0.200903685880382,
20.));
#258129=CARTESIAN_POINT('Ctrl Pts',(-2.64813257022355,0.122662167407797,
20.));
#258130=CARTESIAN_POINT('Ctrl Pts',(-2.64512361303306,0.0705981613229452,
20.));
#258131=CARTESIAN_POINT('Ctrl Pts',(-2.64041394214298,0.018590270709511,
20.));
#258132=CARTESIAN_POINT('Ctrl Pts',(-2.63403298703025,-0.033295129085088,
20.));
#258133=CARTESIAN_POINT('Ctrl Pts',(-2.63152917116831,-0.0536543832584386,
20.));
#258134=CARTESIAN_POINT('Ctrl Pts',(-2.62876798190389,-0.0739947427382281,
20.));
#258135=CARTESIAN_POINT('Ctrl Pts',(-2.62575102113751,-0.09431205197893,
20.));
#258136=CARTESIAN_POINT('Ctrl Pts',(-2.62396534248827,-0.106337460371819,
20.));
#258137=CARTESIAN_POINT('Ctrl Pts',(-2.62209016838413,-0.118353727017597,
20.));
#258138=CARTESIAN_POINT('Ctrl Pts',(-2.62012761849013,-0.130350157446536,
20.));
#258139=CARTESIAN_POINT('Ctrl Pts',(-2.60589970539201,-0.217320771621497,
20.));
#258140=CARTESIAN_POINT('Ctrl Pts',(-2.58706315697293,-0.303391223847671,
20.));
#258141=CARTESIAN_POINT('Ctrl Pts',(-2.56384391335586,-0.38826985486937,
20.));
#258142=CARTESIAN_POINT('Ctrl Pts',(-2.54023125732743,-0.474586616583607,
20.));
#258143=CARTESIAN_POINT('Ctrl Pts',(-2.51208561519729,-0.559671701455797,
20.));
#258144=CARTESIAN_POINT('Ctrl Pts',(-2.47959660063743,-0.643195714463827,
20.));
#258145=CARTESIAN_POINT('Ctrl Pts',(-2.44745273696693,-0.725832400239446,
20.));
#258146=CARTESIAN_POINT('Ctrl Pts',(-2.41105660996257,-0.806941724285991,
20.));
#258147=CARTESIAN_POINT('Ctrl Pts',(-2.37055459062379,-0.886170933862585,
20.));
#258148=CARTESIAN_POINT('Ctrl Pts',(-2.35442910138672,-0.917715281209858,
20.));
#258149=CARTESIAN_POINT('Ctrl Pts',(-2.3376524018868,-0.948961164264044,
20.));
#258150=CARTESIAN_POINT('Ctrl Pts',(-2.32023242312333,-0.979884425452891,
20.));
#258151=CARTESIAN_POINT('Ctrl Pts',(-2.31191361326991,-0.994651649533392,
20.));
#258152=CARTESIAN_POINT('Ctrl Pts',(-2.30344809480684,-1.009345282903,20.));
#258153=CARTESIAN_POINT('Ctrl Pts',(-2.29483668091622,-1.02396259612013,
20.));
#258154=CARTESIAN_POINT('Ctrl Pts',(-2.28734968907845,-1.03667127626685,
20.));
#258155=CARTESIAN_POINT('Ctrl Pts',(-2.27975321692475,-1.04932077027146,
20.));
#258156=CARTESIAN_POINT('Ctrl Pts',(-2.27205422236239,-1.06189926689777,
20.));
#258157=CARTESIAN_POINT('Ctrl Pts',(-2.22635340848745,-1.13656454019917,
20.));
#258158=CARTESIAN_POINT('Ctrl Pts',(-2.17698444175376,-1.20883151645312,
20.));
#258159=CARTESIAN_POINT('Ctrl Pts',(-2.12411390333182,-1.27837441920937,
20.));
#258160=CARTESIAN_POINT('Ctrl Pts',(-2.07364971882218,-1.3447521407302,
20.));
#258161=CARTESIAN_POINT('Ctrl Pts',(-2.01999471848565,-1.4086484336108,
20.));
#258162=CARTESIAN_POINT('Ctrl Pts',(-1.9632684582212,-1.46974240857356,
20.));
#258163=CARTESIAN_POINT('Ctrl Pts',(-1.94362308304001,-1.49090040583722,
20.));
#258164=CARTESIAN_POINT('Ctrl Pts',(-1.92360916867631,-1.51172193809043,
20.));
#258165=CARTESIAN_POINT('Ctrl Pts',(-1.90323115841627,-1.53219245375308,
20.));
#258166=CARTESIAN_POINT('Ctrl Pts',(-1.88918447856243,-1.54630289811379,
20.));
#258167=CARTESIAN_POINT('Ctrl Pts',(-1.87496284084597,-1.56024823878356,
20.));
#258168=CARTESIAN_POINT('Ctrl Pts',(-1.86058497339293,-1.57400746720644,
20.));
#258169=CARTESIAN_POINT('Ctrl Pts',(-1.79998491988447,-1.63200007156065,
20.));
#258170=CARTESIAN_POINT('Ctrl Pts',(-1.73654958268729,-1.68675391438818,
20.));
#258171=CARTESIAN_POINT('Ctrl Pts',(-1.67041279855624,-1.73795012014107,
20.));
#258172=CARTESIAN_POINT('Ctrl Pts',(-1.60614828232035,-1.78769701121008,
20.));
#258173=CARTESIAN_POINT('Ctrl Pts',(-1.53933251541267,-1.83408516483458,
20.));
#258174=CARTESIAN_POINT('Ctrl Pts',(-1.47007091945726,-1.87677627180768,
20.));
#258175=CARTESIAN_POINT('Ctrl Pts',(-1.43952854209994,-1.8956018255794,
20.));
#258176=CARTESIAN_POINT('Ctrl Pts',(-1.40851038026661,-1.91370783080608,
20.));
#258177=CARTESIAN_POINT('Ctrl Pts',(-1.37702479013087,-1.93106208855776,
20.));
#258178=CARTESIAN_POINT('Ctrl Pts',(-2.94150036975487,-0.00272063203504856,
19.1778238829104));
#258179=CARTESIAN_POINT('Ctrl Pts',(-2.94371245543113,-0.247097874156059,
19.1910422576477));
#258180=CARTESIAN_POINT('Ctrl Pts',(-2.91580747959954,-0.490974180238699,
19.204260632385));
#258181=CARTESIAN_POINT('Ctrl Pts',(-2.85583087373334,-0.726685453029614,
19.2174790071223));
#258182=CARTESIAN_POINT('Ctrl Pts',(-2.61561947315925,-1.67072912056425,
19.2704197206405));
#258183=CARTESIAN_POINT('Ctrl Pts',(-1.86095650567826,-2.48379989503908,
19.3233604341588));
#258184=CARTESIAN_POINT('Ctrl Pts',(-0.937402601194396,-2.79371901178798,
19.376301147677));
#258185=CARTESIAN_POINT('Ctrl Pts',(-0.0138486967105547,-3.10363812853687,
19.4292418611953));
#258186=CARTESIAN_POINT('Ctrl Pts',(1.07859614477614,-2.91040558755985,
19.4821825747135));
#258187=CARTESIAN_POINT('Ctrl Pts',(1.83960270788176,-2.30220774740661,
19.5351232882317));
#258188=CARTESIAN_POINT('Ctrl Pts',(2.60060927098739,-1.69400990725336,
19.58806400175));
#258189=CARTESIAN_POINT('Ctrl Pts',(3.03017755571193,-0.670846767923846,
19.6410047152682));
#258190=CARTESIAN_POINT('Ctrl Pts',(2.9316978603901,0.298156596385862,19.6939454287865));
#258191=CARTESIAN_POINT('Ctrl Pts',(2.83321816506828,1.26715996069558,19.7468861423047));
#258192=CARTESIAN_POINT('Ctrl Pts',(2.2066904897001,2.18200354998551,19.7998268558229));
#258193=CARTESIAN_POINT('Ctrl Pts',(1.33882324257931,2.62485738713369,19.8527675693412));
#258194=CARTESIAN_POINT('Ctrl Pts',(0.534286772812256,3.03539490187918,
19.9018450462275));
#258195=CARTESIAN_POINT('Ctrl Pts',(-0.477651922143633,3.04031420760226,
19.9509225231137));
#258196=CARTESIAN_POINT('Ctrl Pts',(-1.29201753387187,2.6484941502042,20.));
#258197=CARTESIAN_POINT('',(-1.37702479013099,-1.93106208855767,0.));
#258198=CARTESIAN_POINT('Ctrl Pts',(-1.38000136014985,-1.93372567510039,
-5.3776427755281E-17));
#258199=CARTESIAN_POINT('Ctrl Pts',(-1.43101535044438,-1.90597970583003,
-6.22176958538883E-17));
#258200=CARTESIAN_POINT('Ctrl Pts',(-1.48084385890449,-1.87629002335049,
-1.38602792231131E-16));
#258201=CARTESIAN_POINT('Ctrl Pts',(-1.52936200486733,-1.84468127109107,
-1.61329283265843E-16));
#258202=CARTESIAN_POINT('Ctrl Pts',(-1.59766408851972,-1.800183617726,-1.92502189234508E-16));
#258203=CARTESIAN_POINT('Ctrl Pts',(-1.66337061633866,-1.75188515356435,
-7.54981138379841E-17));
#258204=CARTESIAN_POINT('Ctrl Pts',(-1.72639642843817,-1.70014539872556,
-3.12250225675825E-16));
#258205=CARTESIAN_POINT('Ctrl Pts',(-1.76317324629481,-1.6699542202819,
-4.50399802875828E-16));
#258206=CARTESIAN_POINT('Ctrl Pts',(-1.79903699951223,-1.63859032242655,
-3.1031875783162E-17));
#258207=CARTESIAN_POINT('Ctrl Pts',(-1.83396765709214,-1.60611776805061,
-1.38777878078145E-16));
#258208=CARTESIAN_POINT('Ctrl Pts',(-1.84847964786871,-1.59262699970429,
-1.83541106137601E-16));
#258209=CARTESIAN_POINT('Ctrl Pts',(-1.86283055532984,-1.57894481768837,
-1.98430142350905E-16));
#258210=CARTESIAN_POINT('Ctrl Pts',(-1.87701880215806,-1.56507557173329,
-1.87350135405495E-16));
#258211=CARTESIAN_POINT('Ctrl Pts',(-1.8884302860734,-1.55392065745456,
-1.78438581880232E-16));
#258212=CARTESIAN_POINT('Ctrl Pts',(-1.89973595998167,-1.54264518151194,
3.57342686513655E-16));
#258213=CARTESIAN_POINT('Ctrl Pts',(-1.91092588736256,-1.53126101376045,
3.12250225675825E-16));
#258214=CARTESIAN_POINT('Ctrl Pts',(-1.97083426275634,-1.47031271874583,
7.08352477809135E-17));
#258215=CARTESIAN_POINT('Ctrl Pts',(-2.02749743984676,-1.40618475518815,
-8.11534412475848E-16));
#258216=CARTESIAN_POINT('Ctrl Pts',(-2.08082093919753,-1.33926925427454,
-5.48172618408671E-16));
#258217=CARTESIAN_POINT('Ctrl Pts',(-2.12725152044828,-1.2810036558061,
-3.1885456301731E-16));
#258218=CARTESIAN_POINT('Ctrl Pts',(-2.17114995783034,-1.2206234746831,
9.75718645724583E-17));
#258219=CARTESIAN_POINT('Ctrl Pts',(-2.21243810966654,-1.15835938453353,
1.66533453693773E-16));
#258220=CARTESIAN_POINT('Ctrl Pts',(-2.23225460122457,-1.12847536788602,
1.99631974404344E-16));
#258221=CARTESIAN_POINT('Ctrl Pts',(-2.25146955036191,-1.09815702694957,
-1.08310280677544E-16));
#258222=CARTESIAN_POINT('Ctrl Pts',(-2.2700728366736,-1.06742810552577,
-9.71445146547012E-17));
#258223=CARTESIAN_POINT('Ctrl Pts',(-2.28179995764522,-1.04805723885056,
-9.01058502651499E-17));
#258224=CARTESIAN_POINT('Ctrl Pts',(-2.29328723219393,-1.02851724410871,
-1.76640528435757E-16));
#258225=CARTESIAN_POINT('Ctrl Pts',(-2.30451408383319,-1.00884594392475,
-1.80411241501588E-16));
#258226=CARTESIAN_POINT('Ctrl Pts',(-2.34846160948551,-0.931842613229072,
-1.95171702805683E-16));
#258227=CARTESIAN_POINT('Ctrl Pts',(-2.38846508399537,-0.852762706837416,
-1.08344740154023E-16));
#258228=CARTESIAN_POINT('Ctrl Pts',(-2.42442591717442,-0.772002953652072,
-1.38777878078145E-17));
#258229=CARTESIAN_POINT('Ctrl Pts',(-2.46263172560052,-0.686201502852074,
8.64865798909936E-17));
#258230=CARTESIAN_POINT('Ctrl Pts',(-2.49627541606281,-0.598503422002609,
-1.68069008667652E-16));
#258231=CARTESIAN_POINT('Ctrl Pts',(-2.52519947762592,-0.509336114470687,
-2.91433543964104E-16));
#258232=CARTESIAN_POINT('Ctrl Pts',(-2.54689252379825,-0.442460633821745,
-3.83956945436442E-16));
#258233=CARTESIAN_POINT('Ctrl Pts',(-2.56593002240835,-0.374757582045608,
2.75043757311674E-16));
#258234=CARTESIAN_POINT('Ctrl Pts',(-2.58222700004388,-0.306394258608983,
3.33066907387547E-16));
#258235=CARTESIAN_POINT('Ctrl Pts',(-2.59444973327053,-0.255121766031515,
3.76584269944452E-16));
#258236=CARTESIAN_POINT('Ctrl Pts',(-2.60513060989885,-0.203477624456378,
-3.29320581511714E-17));
#258237=CARTESIAN_POINT('Ctrl Pts',(-2.61422692989439,-0.151529773561905,
0.));
#258238=CARTESIAN_POINT('Ctrl Pts',(-2.61684954307657,-0.136552385056628,
9.49483415994306E-18));
#258239=CARTESIAN_POINT('Ctrl Pts',(-2.61934039841294,-0.121549739952084,
1.11903402599329E-17));
#258240=CARTESIAN_POINT('Ctrl Pts',(-2.62169837307482,-0.106523444586755,
0.));
#258241=CARTESIAN_POINT('Ctrl Pts',(-2.62406378639396,-0.0914497460567891,
-1.12256422108653E-17));
#258242=CARTESIAN_POINT('Ctrl Pts',(-2.62629415830334,-0.0763603840706239,
2.83678833725852E-16));
#258243=CARTESIAN_POINT('Ctrl Pts',(-2.62838787459448,-0.0612642678389218,
2.77555756156289E-16));
#258244=CARTESIAN_POINT('Ctrl Pts',(-2.64110515406688,0.0304298790130256,
2.40364046366038E-16));
#258245=CARTESIAN_POINT('Ctrl Pts',(-2.64879705700742,0.122452682837918,
1.35678568928957E-16));
#258246=CARTESIAN_POINT('Ctrl Pts',(-2.65132822859212,0.21441013312469,
1.38777878078145E-16));
#258247=CARTESIAN_POINT('Ctrl Pts',(-2.65228737650166,0.249255971606106,
1.39952312837697E-16));
#258248=CARTESIAN_POINT('Ctrl Pts',(-2.65250504989958,0.284092732465562,
-6.80384553331465E-17));
#258249=CARTESIAN_POINT('Ctrl Pts',(-2.65197217923219,0.318899937974375,
-5.55111512312578E-17));
#258250=CARTESIAN_POINT('Ctrl Pts',(-2.65061524597764,0.407535056292549,
-2.36108861841977E-17));
#258251=CARTESIAN_POINT('Ctrl Pts',(-2.64439528531828,0.495977946818749,
-1.03572650581825E-16));
#258252=CARTESIAN_POINT('Ctrl Pts',(-2.63355716179701,0.583967053320013,
-1.94289029309402E-16));
#258253=CARTESIAN_POINT('Ctrl Pts',(-2.62250057345816,0.673729762425441,
-2.868339844591E-16));
#258254=CARTESIAN_POINT('Ctrl Pts',(-2.60663767123318,0.763020939005978,
-7.23771563560485E-17));
#258255=CARTESIAN_POINT('Ctrl Pts',(-2.58617447009765,0.851566464826489,
-1.11022302462516E-16));
#258256=CARTESIAN_POINT('Ctrl Pts',(-2.58109483477611,0.873546358272459,
-1.20615290767153E-16));
#258257=CARTESIAN_POINT('Ctrl Pts',(-2.57573148044371,0.895480291325348,
2.39702298114726E-16));
#258258=CARTESIAN_POINT('Ctrl Pts',(-2.57008706945311,0.917364020427546,
2.4980018054066E-16));
#258259=CARTESIAN_POINT('Ctrl Pts',(-2.56640505109836,0.931639432398567,
2.56387331706348E-16));
#258260=CARTESIAN_POINT('Ctrl Pts',(-2.56260537556786,0.94588580938044,
4.94036337426619E-18));
#258261=CARTESIAN_POINT('Ctrl Pts',(-2.55869076374861,0.960096434692657,
0.));
#258262=CARTESIAN_POINT('Ctrl Pts',(-2.53409586674846,1.04937958254999,
-3.10395344274081E-17));
#258263=CARTESIAN_POINT('Ctrl Pts',(-2.50495054498212,1.13732018527145,
-2.59292046237921E-16));
#258264=CARTESIAN_POINT('Ctrl Pts',(-2.47154363309989,1.22363519951094,
-2.22044604925031E-16));
#258265=CARTESIAN_POINT('Ctrl Pts',(-2.43749715253502,1.31160269752815,
-1.84084068757516E-16));
#258266=CARTESIAN_POINT('Ctrl Pts',(-2.39902417803456,1.39788255512328,
1.18743150656401E-16));
#258267=CARTESIAN_POINT('Ctrl Pts',(-2.35637502831346,1.48217800192524,
1.38777878078145E-16));
#258268=CARTESIAN_POINT('Ctrl Pts',(-2.31337208634223,1.56717271415208,
1.58978801809585E-16));
#258269=CARTESIAN_POINT('Ctrl Pts',(-2.26612310346488,1.65015083103388,
-2.12641302436217E-17));
#258270=CARTESIAN_POINT('Ctrl Pts',(-2.21483250272833,1.73079835854605,
0.));
#258271=CARTESIAN_POINT('Ctrl Pts',(-2.18408162452443,1.77914995241235,
1.27487428465136E-17));
#258272=CARTESIAN_POINT('Ctrl Pts',(-2.15187700314947,1.82666356774367,
-1.93359933520376E-16));
#258273=CARTESIAN_POINT('Ctrl Pts',(-2.11825450271608,1.87326783752673,
-2.22044604925031E-16));
#258274=CARTESIAN_POINT('Ctrl Pts',(-2.10898884344645,1.88611100144236,
-2.29949501588597E-16));
#258275=CARTESIAN_POINT('Ctrl Pts',(-2.09961449121588,1.89888626983332,
-3.51687330639502E-16));
#258276=CARTESIAN_POINT('Ctrl Pts',(-2.09014358815089,1.9115771165726,-3.33066907387547E-16));
#258277=CARTESIAN_POINT('Ctrl Pts',(-2.03133347089822,1.99038165924946,
-2.17442318345972E-16));
#258278=CARTESIAN_POINT('Ctrl Pts',(-1.9687115216203,2.06606315861356,-3.78880423800246E-16));
#258279=CARTESIAN_POINT('Ctrl Pts',(-1.90254904260934,2.13831227552401,
-3.33066907387547E-16));
#258280=CARTESIAN_POINT('Ctrl Pts',(-1.83622830911578,2.21073420558757,
-2.87143809313996E-16));
#258281=CARTESIAN_POINT('Ctrl Pts',(-1.76634968788036,2.27970821505394,
1.19516948523233E-16));
#258282=CARTESIAN_POINT('Ctrl Pts',(-1.69313645008632,2.34490696177326,
1.66533453693773E-16));
#258283=CARTESIAN_POINT('Ctrl Pts',(-1.62134465410955,2.40883986876451,
2.12637129046033E-16));
#258284=CARTESIAN_POINT('Ctrl Pts',(-1.54634593780016,2.46914345344329,
3.88578058618805E-16));
#258285=CARTESIAN_POINT('Ctrl Pts',(-1.4683099737214,2.52548168087978,3.88578058618805E-16));
#258286=CARTESIAN_POINT('Ctrl Pts',(-1.4101809347186,2.56744806213316,3.88578058618805E-16));
#258287=CARTESIAN_POINT('Ctrl Pts',(-1.35036573192052,2.60721367515221,
1.51746623653549E-17));
#258288=CARTESIAN_POINT('Ctrl Pts',(-1.28892185405322,2.64462557919718,
0.));
#258289=CARTESIAN_POINT('Ctrl Pts',(-1.38000136014988,-1.93372567510037,
-2.60100101179273E-15));
#258290=CARTESIAN_POINT('Ctrl Pts',(-0.784688350722177,-2.35371652554116,
0.0490774768862665));
#258291=CARTESIAN_POINT('Ctrl Pts',(0.889177499330816,-2.62573605996334,
0.151095667290779));
#258292=CARTESIAN_POINT('Ctrl Pts',(2.70389566823784,-0.740895185834261,
0.306054571213535));
#258293=CARTESIAN_POINT('Ctrl Pts',(2.08805286496322,1.8712628391822,0.464876711768264));
#258294=CARTESIAN_POINT('Ctrl Pts',(-0.440526185828228,2.76865345984501,
0.623698852322994));
#258295=CARTESIAN_POINT('Ctrl Pts',(-2.15180306555184,1.44961829294084,
0.751603245701911));
#258296=CARTESIAN_POINT('Ctrl Pts',(-2.36960890551819,0.330372416157857,
0.826566925562585));
#258297=CARTESIAN_POINT('Ctrl Pts',(-2.36829764012707,0.00106700769158283,
0.848589891905016));
#258298=CARTESIAN_POINT('Origin',(0.,0.,-1.84858989190501));
#258299=CARTESIAN_POINT('',(1.37702479013102,-1.93106208855765,0.));
#258300=CARTESIAN_POINT('Origin',(0.,0.,0.));
#258301=CARTESIAN_POINT('Ctrl Pts',(1.37702479013101,-1.93106208855765,
-2.4980018054066E-15));
#258302=CARTESIAN_POINT('Ctrl Pts',(2.01936616407906,-1.47301363900524,
0.0529407135182407));
#258303=CARTESIAN_POINT('Ctrl Pts',(2.79990526463056,0.126536631817626,
0.158822140554727));
#258304=CARTESIAN_POINT('Ctrl Pts',(1.40874583290953,2.42611875140058,0.317644281109456));
#258305=CARTESIAN_POINT('Ctrl Pts',(-1.27387826991474,2.49658204560485,
0.476466421664188));
#258306=CARTESIAN_POINT('Ctrl Pts',(-2.33532317779642,0.946682230744997,
0.587721697326026));
#258307=CARTESIAN_POINT('Ctrl Pts',(-2.37517596458242,0.081324476190725,
0.646036259469624));
#258308=CARTESIAN_POINT('Ctrl Pts',(-2.37462805812147,0.00152502885334119,
0.651410108094978));
#258309=CARTESIAN_POINT('Ctrl Pts',(1.70810875200395,-2.39535560853238,
-0.329233991005387));
#258310=CARTESIAN_POINT('Ctrl Pts',(2.50489101073913,-1.82717661050005,
-0.276293277487143));
#258311=CARTESIAN_POINT('Ctrl Pts',(3.47309846676214,0.156960375590738,
-0.170411850450657));
#258312=CARTESIAN_POINT('Ctrl Pts',(1.74745662081582,3.00944086291576,-0.0115897098959277));
#258313=CARTESIAN_POINT('Ctrl Pts',(-1.58016227262108,3.09684594842185,
0.147232430658803));
#258314=CARTESIAN_POINT('Ctrl Pts',(-3.45974587664961,0.352316997116106,
0.306054571213531));
#258315=CARTESIAN_POINT('Ctrl Pts',(-2.17104076685187,-2.71717329882319,
0.464876711768262));
#258316=CARTESIAN_POINT('Ctrl Pts',(1.10629343072135,-3.2968702555127,0.62369885232299));
#258317=CARTESIAN_POINT('Ctrl Pts',(3.37028228423513,-0.857658442232281,
0.782520992877721));
#258318=CARTESIAN_POINT('Ctrl Pts',(2.54756179623556,2.36739129287567,0.941343133432451));
#258319=CARTESIAN_POINT('Ctrl Pts',(-0.608447577806647,3.42402675434335,
1.10016527398718));
#258320=CARTESIAN_POINT('Ctrl Pts',(-3.20717632466629,1.34475897960982,
1.25898741454191));
#258321=CARTESIAN_POINT('Ctrl Pts',(-2.86852948418392,-1.96619175536868,
1.41780955509664));
#258322=CARTESIAN_POINT('Ctrl Pts',(0.097346709292227,-3.47632490222585,
1.57663169565137));
#258323=CARTESIAN_POINT('Ctrl Pts',(2.97406276265272,-1.80257927416548,
1.7354538362061));
#258324=CARTESIAN_POINT('Ctrl Pts',(3.12689955660378,1.52211691970352,1.89427597676083));
#258325=CARTESIAN_POINT('Ctrl Pts',(0.415875247528641,3.45273523523294,
2.05309811731556));
#258326=CARTESIAN_POINT('Ctrl Pts',(-2.67603996909776,2.22106901660608,
2.21192025787029));
#258327=CARTESIAN_POINT('Ctrl Pts',(-3.31702756833606,-1.04482779857665,
2.37074239842501));
#258328=CARTESIAN_POINT('Ctrl Pts',(-0.92002044018298,-3.35378866314487,
2.52956453897975));
#258329=CARTESIAN_POINT('Ctrl Pts',(2.31961369078498,-2.5910864587838,2.68838667953447));
#258330=CARTESIAN_POINT('Ctrl Pts',(3.4347632597901,0.54473657670683,2.84720882008921));
#258331=CARTESIAN_POINT('Ctrl Pts',(1.40408657869956,3.18164695477209,3.00603096064393));
#258332=CARTESIAN_POINT('Ctrl Pts',(-1.91256297435207,2.90455494666245,
3.16485310119866));
#258333=CARTESIAN_POINT('Ctrl Pts',(-3.47753699220607,-0.0327568596370786,
3.3236752417534));
#258334=CARTESIAN_POINT('Ctrl Pts',(-1.85750922440995,-2.94006734803805,
3.48249738230812));
#258335=CARTESIAN_POINT('Ctrl Pts',(1.46377152869574,-3.15463301455215,
3.64131952286286));
#258336=CARTESIAN_POINT('Ctrl Pts',(3.4444152336643,-0.479937744130016,
3.80014166341758));
#258337=CARTESIAN_POINT('Ctrl Pts',(2.27039266516074,2.63432224388432,3.95896380397232));
#258338=CARTESIAN_POINT('Ctrl Pts',(-0.983034005725968,3.33586280957935,
4.11778594452704));
#258339=CARTESIAN_POINT('Ctrl Pts',(-3.33612084746066,0.982157946106786,
4.27660808508178));
#258340=CARTESIAN_POINT('Ctrl Pts',(-2.63372592902202,-2.27108438210191,
4.4354302256365));
#258341=CARTESIAN_POINT('Ctrl Pts',(0.480842260469829,-3.44428907913767,
4.59425236619123));
#258342=CARTESIAN_POINT('Ctrl Pts',(3.15501730369756,-1.46294304515281,
4.75307450674596));
#258343=CARTESIAN_POINT('Ctrl Pts',(2.93957945064476,1.8582812471024,4.9118966473007));
#258344=CARTESIAN_POINT('Ctrl Pts',(0.0318436250124843,3.47754547397594,
5.07071878785541));
#258345=CARTESIAN_POINT('Ctrl Pts',(-2.90505709597467,1.91180014884698,
5.22954092841015));
#258346=CARTESIAN_POINT('Ctrl Pts',(-3.18127813095577,-1.40492205958462,
5.38836306896487));
#258347=CARTESIAN_POINT('Ctrl Pts',(-0.543834539415804,-3.43490618994878,
5.54718520951961));
#258348=CARTESIAN_POINT('Ctrl Pts',(2.59169547995281,-2.31893317695855,
5.70600735007433));
#258349=CARTESIAN_POINT('Ctrl Pts',(3.35354701796656,0.920901155550854,
5.86482949062907));
#258350=CARTESIAN_POINT('Ctrl Pts',(1.04395653884046,3.31730180794877,6.0236516311838));
#258351=CARTESIAN_POINT('Ctrl Pts',(-2.22177141510979,2.6754566561633,6.18247377173853));
#258352=CARTESIAN_POINT('Ctrl Pts',(-3.45262642996333,-0.416782047509506,
6.34129591229325));
#258353=CARTESIAN_POINT('Ctrl Pts',(-1.52129471248139,-3.12729898439273,
6.50011805284799));
#258354=CARTESIAN_POINT('Ctrl Pts',(1.80335830788818,-2.97358964105309,
6.65894019340271));
#258355=CARTESIAN_POINT('Ctrl Pts',(3.47635400867004,-0.0964331188513625,
6.81776233395745));
#258356=CARTESIAN_POINT('Ctrl Pts',(1.96543139505884,2.86904443523007,6.97658447451217));
#258357=CARTESIAN_POINT('Ctrl Pts',(-1.34558781366435,3.20682552935541,
7.13540661506691));
#258358=CARTESIAN_POINT('Ctrl Pts',(-3.42421191162923,0.607543680951476,
7.29422875562163));
#258359=CARTESIAN_POINT('Ctrl Pts',(-2.36667352711723,-2.54817443595411,
7.45305089617636));
#258360=CARTESIAN_POINT('Ctrl Pts',(0.858450542967834,-3.37007406525225,
7.6118730367311));
#258361=CARTESIAN_POINT('Ctrl Pts',(3.29733811385309,-1.10539490813885,
7.77069517728582));
#258362=CARTESIAN_POINT('Ctrl Pts',(2.71626420116681,2.1716918127274,7.92951731784056));
#258363=CARTESIAN_POINT('Ctrl Pts',(-0.352578021437311,3.45977243165023,
8.08833945839528));
#258364=CARTESIAN_POINT('Ctrl Pts',(-3.09850157209174,1.57912144806933,
8.24716159895001));
#258365=CARTESIAN_POINT('Ctrl Pts',(-3.0065737767802,-1.74781310922686,
8.40598373950474));
#258366=CARTESIAN_POINT('Ctrl Pts',(-0.160989337873077,-3.47396300686965,
8.56480588005947));
#258367=CARTESIAN_POINT('Ctrl Pts',(2.83204179374651,-2.01838445755032,
8.72362802061421));
#258368=CARTESIAN_POINT('Ctrl Pts',(3.23126639365278,1.28578926471553,8.88245016116893));
#258369=CARTESIAN_POINT('Ctrl Pts',(0.671043185949358,3.41233608875187,
9.04127230172366));
#258370=CARTESIAN_POINT('Ctrl Pts',(-2.5037741293059,2.41359724258752,9.20009444227838));
#258371=CARTESIAN_POINT('Ctrl Pts',(-3.38543824856365,-0.795703716951166,
9.35891658283312));
#258372=CARTESIAN_POINT('Ctrl Pts',(-1.16645185439101,-3.27623665375311,
9.51773872338784));
#258373=CARTESIAN_POINT('Ctrl Pts',(2.12086285524974,-2.75613448315381,
9.67656086394259));
#258374=CARTESIAN_POINT('Ctrl Pts',(3.46572461841138,0.288252336235001,
9.8353830044973));
#258375=CARTESIAN_POINT('Ctrl Pts',(1.63640329846855,3.06863500351032,9.99420514505204));
#258376=CARTESIAN_POINT('Ctrl Pts',(-1.69166481732213,3.03852047645593,
10.1530272856068));
#258377=CARTESIAN_POINT('Ctrl Pts',(-3.47037329360166,0.225490006572311,
10.3118494261615));
#258378=CARTESIAN_POINT('Ctrl Pts',(-2.07064106455555,-2.79406193950383,
10.4706715667162));
#258379=CARTESIAN_POINT('Ctrl Pts',(1.22554704658151,-3.25459229038338,
10.629493707271));
#258380=CARTESIAN_POINT('Ctrl Pts',(3.39928281913928,-0.734311143529869,
10.7883158478257));
#258381=CARTESIAN_POINT('Ctrl Pts',(2.45968813206418,2.45850988059642,10.9471379883804));
#258382=CARTESIAN_POINT('Ctrl Pts',(-0.732682328664183,3.39963426639848,
11.1059601289351));
#258383=CARTESIAN_POINT('Ctrl Pts',(-3.25400470883227,1.22710630953676,
11.2647822694899));
#258384=CARTESIAN_POINT('Ctrl Pts',(-2.79505374464792,-2.06930208150895,
11.4236044100446));
#258385=CARTESIAN_POINT('Ctrl Pts',(0.223827187860361,-3.47048093640955,
11.5824265505993));
#258386=CARTESIAN_POINT('Ctrl Pts',(3.03770958428446,-1.69312049823808,
11.7412486911541));
#258387=CARTESIAN_POINT('Ctrl Pts',(3.06941871668279,1.63493280647403,11.9000708317088));
#258388=CARTESIAN_POINT('Ctrl Pts',(0.289912868611965,3.46558610751786,
12.0588929722635));
#258389=CARTESIAN_POINT('Ctrl Pts',(-2.75511797767527,2.12218318462333,
12.2177151128182));
#258390=CARTESIAN_POINT('Ctrl Pts',(-3.27679517080862,-1.16488194619576,
12.376537253373));
#258391=CARTESIAN_POINT('Ctrl Pts',(-0.797325722710365,-3.38505660689921,
12.5353593939277));
#258392=CARTESIAN_POINT('Ctrl Pts',(2.41239730852211,-2.50493029161351,
12.6941815344824));
#258393=CARTESIAN_POINT('Ctrl Pts',(3.41265722033696,0.669408124009311,
12.8530036750372));
#258394=CARTESIAN_POINT('Ctrl Pts',(1.28733734439784,3.23064995035462,13.0118258155919));
#258395=CARTESIAN_POINT('Ctrl Pts',(-2.01702728285485,2.83300855632784,
13.1706479561466));
#258396=CARTESIAN_POINT('Ctrl Pts',(-3.47403974444911,-0.159324806591705,
13.3294700967013));
#258397=CARTESIAN_POINT('Ctrl Pts',(-1.7492534767729,-3.0057359854128,13.4882922372561));
#258398=CARTESIAN_POINT('Ctrl Pts',(1.57763665239809,-3.0992578358404,13.6471143778108));
#258399=CARTESIAN_POINT('Ctrl Pts',(3.45960310046506,-0.354235694502853,
13.8059365183655));
#258400=CARTESIAN_POINT('Ctrl Pts',(2.17299303284069,2.71522334610484,13.9647586589203));
#258401=CARTESIAN_POINT('Ctrl Pts',(-1.10381489640987,3.29786737369376,
14.123580799475));
#258402=CARTESIAN_POINT('Ctrl Pts',(-3.36966236087009,0.860065179937116,
14.2824029400297));
#258403=CARTESIAN_POINT('Ctrl Pts',(-2.54930811016128,-2.36545232449735,
14.4412250805845));
#258404=CARTESIAN_POINT('Ctrl Pts',(0.605902936125663,-3.42450261673412,
14.6000472211392));
#258405=CARTESIAN_POINT('Ctrl Pts',(3.20618043701593,-1.34712417589535,
14.7588693616939));
#258406=CARTESIAN_POINT('Ctrl Pts',(2.86998582166464,1.96405649700715,14.9176915022486));
#258407=CARTESIAN_POINT('Ctrl Pts',(-0.0947674493627475,3.47639981455846,
15.0765136428034));
#258408=CARTESIAN_POINT('Ctrl Pts',(-2.97272523956357,1.80478286502611,
15.2353357833581));
#258409=CARTESIAN_POINT('Ctrl Pts',(-3.12802753778546,-1.51979612541224,
15.3941579239129));
#258410=CARTESIAN_POINT('Ctrl Pts',(-0.418436289233176,-3.45242633702748,
15.5529800644676));
#258411=CARTESIAN_POINT('Ctrl Pts',(2.67439181059374,-2.22305307675472,
15.7118022050223));
#258412=CARTESIAN_POINT('Ctrl Pts',(3.31780162809799,1.04236696836076,15.870624345577));
#258413=CARTESIAN_POINT('Ctrl Pts',(0.922507866308364,3.35310539370922,
16.0294464861318));
#258414=CARTESIAN_POINT('Ctrl Pts',(-2.31769112662919,2.59280627338641,
16.1882686266865));
#258415=CARTESIAN_POINT('Ctrl Pts',(-3.43516636929164,-0.542188675003985,
16.3470907672412));
#258416=CARTESIAN_POINT('Ctrl Pts',(-1.40644617227113,-3.18060461760772,
16.5059129077959));
#258417=CARTESIAN_POINT('Ctrl Pts',(1.91040799810916,-2.90597277104503,
16.6647350483507));
#258418=CARTESIAN_POINT('Ctrl Pts',(3.47756033952126,0.0301773722343488,
16.8235571889054));
#258419=CARTESIAN_POINT('Ctrl Pts',(1.85968948862187,2.93868877516475,16.9823793294602));
#258420=CARTESIAN_POINT('Ctrl Pts',(-1.46143115770309,3.15571782304568,
17.1412014700149));
#258421=CARTESIAN_POINT('Ctrl Pts',(-3.44405834328818,0.48249263808589,
17.3000236105696));
#258422=CARTESIAN_POINT('Ctrl Pts',(-2.27234594795998,-2.63263772394267,
17.4588457511243));
#258423=CARTESIAN_POINT('Ctrl Pts',(0.980559183838789,-3.33659055221275,
17.6176678916791));
#258424=CARTESIAN_POINT('Ctrl Pts',(3.33539176443223,-0.984633196725734,
17.7764900322338));
#258425=CARTESIAN_POINT('Ctrl Pts',(2.63540911147839,2.26913203031142,17.9353121727885));
#258426=CARTESIAN_POINT('Ctrl Pts',(-0.478286064479774,3.4446412945574,
18.0941343133433));
#258427=CARTESIAN_POINT('Ctrl Pts',(-3.15393372518352,1.46528955420501,
18.252956453898));
#258428=CARTESIAN_POINT('Ctrl Pts',(-2.94095238931831,-1.85611307158376,
18.4117785944527));
#258429=CARTESIAN_POINT('Ctrl Pts',(-0.0344319160965253,-3.4774965294809,
18.5706007350074));
#258430=CARTESIAN_POINT('Ctrl Pts',(2.90365509789218,-1.91400096962023,
18.7294228755622));
#258431=CARTESIAN_POINT('Ctrl Pts',(3.1822871338934,1.40265080344969,18.8882450161169));
#258432=CARTESIAN_POINT('Ctrl Pts',(0.546443743866525,3.43433223077365,
19.0470671566716));
#258433=CARTESIAN_POINT('Ctrl Pts',(-2.59009217426645,2.32117885480077,
19.2058892972263));
#258434=CARTESIAN_POINT('Ctrl Pts',(-3.35400480467998,-0.919032408370063,
19.3647114377811));
#258435=CARTESIAN_POINT('Ctrl Pts',(-1.04684590468812,-3.31534029745207,
19.5235335783358));
#258436=CARTESIAN_POINT('Ctrl Pts',(2.22061130085995,-2.6794074717208,19.6823557188906));
#258437=CARTESIAN_POINT('Ctrl Pts',(3.45130747732673,0.418958489924277,
19.8411778594453));
#258438=CARTESIAN_POINT('Ctrl Pts',(2.16862035685408,2.21588336549518,19.9470592864818));
#258439=CARTESIAN_POINT('Ctrl Pts',(1.28892185405323,2.64462557919718,20.));
#258440=CARTESIAN_POINT('Ctrl Pts',(1.59774743137964,-2.24059110187414,
-0.219489327336925));
#258441=CARTESIAN_POINT('Ctrl Pts',(2.34304939518577,-1.70912228666845,
-0.166548613818682));
#258442=CARTESIAN_POINT('Ctrl Pts',(3.24870073271828,0.146819127666371,
-0.0606671867821956));
#258443=CARTESIAN_POINT('Ctrl Pts',(1.63455302484706,2.81500015907737,0.0981549537725337));
#258444=CARTESIAN_POINT('Ctrl Pts',(-1.4780676050523,2.89675798081618,0.256977094327264));
#258445=CARTESIAN_POINT('Ctrl Pts',(-3.23621085669046,0.329553710507722,
0.415799234881993));
#258446=CARTESIAN_POINT('Ctrl Pts',(-2.0307692965032,-2.54161607316561,
0.574621375436723));
#258447=CARTESIAN_POINT('Ctrl Pts',(1.03481554392453,-3.08385866892691,
0.733443515991452));
#258448=CARTESIAN_POINT('Ctrl Pts',(3.15252752867372,-0.802244922327108,
0.892265656546182));
#258449=CARTESIAN_POINT('Ctrl Pts',(2.38296321088507,2.21443356743241,1.05108779710091));
#258450=CARTESIAN_POINT('Ctrl Pts',(-0.569135632277061,3.20279955553706,
1.20990993765564));
#258451=CARTESIAN_POINT('Ctrl Pts',(-2.99995988470017,1.25787377587964,
1.36873207821037));
#258452=CARTESIAN_POINT('Ctrl Pts',(-2.68319309869152,-1.83915562932077,
1.5275542187651));
#258453=CARTESIAN_POINT('Ctrl Pts',(0.0910571148016564,-3.25171870740438,
1.68637635931983));
#258454=CARTESIAN_POINT('Ctrl Pts',(2.78190784645029,-1.68611419019846,
1.84519849987456));
#258455=CARTESIAN_POINT('Ctrl Pts',(2.92486981808652,1.42377257646074,2.00402064042929));
#258456=CARTESIAN_POINT('Ctrl Pts',(0.389005446950427,3.22965317451556,
2.16284278098402));
#258457=CARTESIAN_POINT('Ctrl Pts',(-2.50314037784715,2.07756520891067,
2.32166492153875));
#258458=CARTESIAN_POINT('Ctrl Pts',(-3.1027136128813,-0.977321221175992,
2.48048706209348));
#258459=CARTESIAN_POINT('Ctrl Pts',(-0.860577696469583,-3.13709956444123,
2.63930920264821));
#258460=CARTESIAN_POINT('Ctrl Pts',(2.16974288779722,-2.42367573443284,
2.79813134320294));
#258461=CARTESIAN_POINT('Ctrl Pts',(3.21284237276366,0.509541014406022,
2.95695348375767));
#258462=CARTESIAN_POINT('Ctrl Pts',(1.31336820440729,2.97607997358482,3.1157756243124));
#258463=CARTESIAN_POINT('Ctrl Pts',(-1.78899181684877,2.71689094730438,
3.27459776486713));
#258464=CARTESIAN_POINT('Ctrl Pts',(-3.25285248395709,-0.0306404309935377,
3.43341990542185));
#258465=CARTESIAN_POINT('Ctrl Pts',(-1.73749510303901,-2.75010888381658,
3.59224204597659));
#258466=CARTESIAN_POINT('Ctrl Pts',(1.36919689531271,-2.95081141059244,
3.75106418653131));
#258467=CARTESIAN_POINT('Ctrl Pts',(3.22187073026558,-0.448928850113442,
3.90988632708604));
#258468=CARTESIAN_POINT('Ctrl Pts',(2.12370204457293,2.46411804497485,4.06870846764078));
#258469=CARTESIAN_POINT('Ctrl Pts',(-0.91951994026425,3.12033190462097,
4.2275306081955));
#258470=CARTESIAN_POINT('Ctrl Pts',(-3.12057327061221,0.918700483069451,
4.38635274875024));
#258471=CARTESIAN_POINT('Ctrl Pts',(-2.46356025816037,-2.12434906951483,
4.54517488930496));
#258472=CARTESIAN_POINT('Ctrl Pts',(0.449774925433255,-3.22175272661351,
4.70399702985969));
#258473=CARTESIAN_POINT('Ctrl Pts',(2.951170870723,-1.36842194029234,4.86281917041443));
#258474=CARTESIAN_POINT('Ctrl Pts',(2.74965250959216,1.73821724515814,5.02164131096915));
#258475=CARTESIAN_POINT('Ctrl Pts',(0.0297862006794342,3.25286041771775,
5.18046345152389));
#258476=CARTESIAN_POINT('Ctrl Pts',(-2.71736065262779,1.78827827768449,
5.33928559207861));
#258477=CARTESIAN_POINT('Ctrl Pts',(-2.9757349795647,-1.31414970466982,
5.49810773263333));
#258478=CARTESIAN_POINT('Ctrl Pts',(-0.50869725796305,-3.21297606817014,
5.65692987318808));
#258479=CARTESIAN_POINT('Ctrl Pts',(2.42424540659647,-2.16910634213409,
5.81575201374279));
#258480=CARTESIAN_POINT('Ctrl Pts',(3.13687353201647,0.86140150860402,5.97457415429754));
#258481=CARTESIAN_POINT('Ctrl Pts',(0.976506253742583,3.10297013380615,
6.13339629485226));
#258482=CARTESIAN_POINT('Ctrl Pts',(-2.07822222527677,2.5025947529028,6.29221843540699));
#258483=CARTESIAN_POINT('Ctrl Pts',(-3.2295513991808,-0.389853658364687,
6.45104057596172));
#258484=CARTESIAN_POINT('Ctrl Pts',(-1.42300349224656,-2.92524343874919,
6.60986271651644));
#258485=CARTESIAN_POINT('Ctrl Pts',(1.68684289036347,-2.78146529335191,
6.76868485707118));
#258486=CARTESIAN_POINT('Ctrl Pts',(3.25174593327414,-0.0902025516606631,
6.92750699762591));
#258487=CARTESIAN_POINT('Ctrl Pts',(1.83844439607489,2.68367477862573,7.08632913818064));
#258488=CARTESIAN_POINT('Ctrl Pts',(-1.25864905876497,2.99963175435938,
7.24515127873536));
#258489=CARTESIAN_POINT('Ctrl Pts',(-3.20297274976581,0.56829013641684,
7.4039734192901));
#258490=CARTESIAN_POINT('Ctrl Pts',(-2.21376217669363,-2.38353626780289,
7.56279555984482));
#258491=CARTESIAN_POINT('Ctrl Pts',(0.802985845242104,-3.1523327627698,
7.72161770039957));
#258492=CARTESIAN_POINT('Ctrl Pts',(3.0842962988265,-1.03397507510392,7.88043984095428));
#258493=CARTESIAN_POINT('Ctrl Pts',(2.54076571252921,2.03137827814687,8.03926198150902));
#258494=CARTESIAN_POINT('Ctrl Pts',(-0.329797869984274,3.23623569596605,
8.19808412206374));
#258495=CARTESIAN_POINT('Ctrl Pts',(-2.89830663423934,1.47709402842718,
8.35690626261848));
#258496=CARTESIAN_POINT('Ctrl Pts',(-2.81231831607218,-1.63488648045544,
8.5157284031732));
#258497=CARTESIAN_POINT('Ctrl Pts',(-0.15058777771873,-3.24950941467982,
8.67455054372794));
#258498=CARTESIAN_POINT('Ctrl Pts',(2.64906288678028,-1.8879761483595,8.83337268428267));
#258499=CARTESIAN_POINT('Ctrl Pts',(3.02249348848844,1.20271410856281,8.99219482483739));
#258500=CARTESIAN_POINT('Ctrl Pts',(0.627686923000373,3.19186422668404,
9.15101696539211));
#258501=CARTESIAN_POINT('Ctrl Pts',(-2.34200467573275,2.25765413953,9.30983910594686));
#258502=CARTESIAN_POINT('Ctrl Pts',(-3.16670426247216,-0.744293106868311,
9.46866124650158));
#258503=CARTESIAN_POINT('Ctrl Pts',(-1.09108711725453,-3.06455820917996,
9.62748338705631));
#258504=CARTESIAN_POINT('Ctrl Pts',(1.98383339193611,-2.57805996592987,
9.78630552761104));
#258505=CARTESIAN_POINT('Ctrl Pts',(3.24180331049736,0.269628282899643,
9.94512766816577));
#258506=CARTESIAN_POINT('Ctrl Pts',(1.53067488458323,2.87036975189557,10.1039498087205));
#258507=CARTESIAN_POINT('Ctrl Pts',(-1.5823659433047,2.8422009317359,10.2627719492752));
#258508=CARTESIAN_POINT('Ctrl Pts',(-3.24615163365646,0.210921042574126,
10.42159408983));
#258509=CARTESIAN_POINT('Ctrl Pts',(-1.9368564433157,-2.61353692012903,
10.5804162303847));
#258510=CARTESIAN_POINT('Ctrl Pts',(1.14636415474908,-3.04431229337554,
10.7392383709394));
#258511=CARTESIAN_POINT('Ctrl Pts',(3.17965433198608,-0.686867122501313,
10.8980605114941));
#258512=CARTESIAN_POINT('Ctrl Pts',(2.30076708546213,2.29966496110741,11.0568826520489));
#258513=CARTESIAN_POINT('Ctrl Pts',(-0.685343545759056,3.17998307215264,
11.2157047926036));
#258514=CARTESIAN_POINT('Ctrl Pts',(-3.04376267561093,1.1478226733467,11.3745269331583));
#258515=CARTESIAN_POINT('Ctrl Pts',(-2.61446464450226,-1.93560397228843,
11.5333490737131));
#258516=CARTESIAN_POINT('Ctrl Pts',(0.209365658982355,-3.24625232163643,
11.6921712142678));
#258517=CARTESIAN_POINT('Ctrl Pts',(2.84144243150425,-1.58372757232369,
11.8509933548225));
#258518=CARTESIAN_POINT('Ctrl Pts',(2.87110282916994,1.52929940143304,12.0098154953773));
#258519=CARTESIAN_POINT('Ctrl Pts',(0.271181527877081,3.24167374882626,
12.168637635932));
#258520=CARTESIAN_POINT('Ctrl Pts',(-2.57710913711678,1.98506841450872,
12.3274597764867));
#258521=CARTESIAN_POINT('Ctrl Pts',(-3.06508064031307,-1.08961864120845,
12.4862819170414));
#258522=CARTESIAN_POINT('Ctrl Pts',(-0.745810314442101,-3.16634727876821,
12.6451040575962));
#258523=CARTESIAN_POINT('Ctrl Pts',(2.25653173349553,-2.34308613811331,
12.8039261981509));
#258524=CARTESIAN_POINT('Ctrl Pts',(3.19216460987954,0.626157502808743,
12.9627483387057));
#258525=CARTESIAN_POINT('Ctrl Pts',(1.20416216644146,3.02191687374124,13.1215704792603));
#258526=CARTESIAN_POINT('Ctrl Pts',(-1.8867066610502,2.64996718659681,13.2803926198151));
#258527=CARTESIAN_POINT('Ctrl Pts',(-3.24958119422566,-0.149030792207068,
13.4392147603698));
#258528=CARTESIAN_POINT('Ctrl Pts',(-1.63623378550507,-2.81153465460818,
13.5980369009245));
#258529=CARTESIAN_POINT('Ctrl Pts',(1.47570516576429,-2.89901403560382,
13.7568590414793));
#258530=CARTESIAN_POINT('Ctrl Pts',(3.23607730530981,-0.331348440391097,
13.915681182034));
#258531=CARTESIAN_POINT('Ctrl Pts',(2.03259542611312,2.53979210736519,14.0745033225887));
#258532=CARTESIAN_POINT('Ctrl Pts',(-1.03249714831588,3.08479136306052,
14.2333254631435));
#258533=CARTESIAN_POINT('Ctrl Pts',(-3.1519476587076,0.804496160125281,
14.3921476036982));
#258534=CARTESIAN_POINT('Ctrl Pts',(-2.38459669504463,-2.21261987627114,
14.5509697442529));
#258535=CARTESIAN_POINT('Ctrl Pts',(0.56675540051207,-3.20324467234338,
14.7097918848077));
#258536=CARTESIAN_POINT('Ctrl Pts',(2.99902834159238,-1.26008615625968,
14.8686140253624));
#258537=CARTESIAN_POINT('Ctrl Pts',(2.68455534185449,1.8371583305197,15.0274361659171));
#258538=CARTESIAN_POINT('Ctrl Pts',(-0.0886445014816008,3.25178877963302,
15.1862583064719));
#258539=CARTESIAN_POINT('Ctrl Pts',(-2.78065674105224,1.68817540651928,
15.3450804470265));
#258540=CARTESIAN_POINT('Ctrl Pts',(-2.92592492013056,-1.42160172925132,
15.5039025875813));
#258541=CARTESIAN_POINT('Ctrl Pts',(-0.391401019129468,-3.22936423429805,
15.662724728136));
#258542=CARTESIAN_POINT('Ctrl Pts',(2.50159870726369,-2.07942107845204,
15.8215468686908));
#258543=CARTESIAN_POINT('Ctrl Pts',(3.10343766045434,0.975019385797018,
15.9803690092455));
#258544=CARTESIAN_POINT('Ctrl Pts',(0.862904409389887,3.13646044120949,
16.1391911498002));
#258545=CARTESIAN_POINT('Ctrl Pts',(-2.16794454097767,2.42528443139698,
16.298013290355));
#258546=CARTESIAN_POINT('Ctrl Pts',(-3.21321943726258,-0.507157733249974,
16.4568354309097));
#258547=CARTESIAN_POINT('Ctrl Pts',(-1.31557534406608,-2.97510498207739,
16.6156575714644));
#258548=CARTESIAN_POINT('Ctrl Pts',(1.78697607414341,-2.71821716570983,
16.7744797120191));
#258549=CARTESIAN_POINT('Ctrl Pts',(3.25287432279659,0.0282276048973285,
16.9333018525739));
#258550=CARTESIAN_POINT('Ctrl Pts',(1.73953449985156,2.74881938087089,17.0921239931286));
#258551=CARTESIAN_POINT('Ctrl Pts',(-1.36700773625735,2.95182612934618,
17.2509461336833));
#258552=CARTESIAN_POINT('Ctrl Pts',(-3.2215368986632,0.451318671751355,
17.4097682742381));
#258553=CARTESIAN_POINT('Ctrl Pts',(-2.12552912529691,-2.46254236227507,
17.5685904147928));
#258554=CARTESIAN_POINT('Ctrl Pts',(0.917205017219261,-3.12101262762637,
17.7274125553475));
#258555=CARTESIAN_POINT('Ctrl Pts',(3.11989129381503,-0.921015807145746,
17.8862346959023));
#258556=CARTESIAN_POINT('Ctrl Pts',(2.46513468979012,2.1225228596469,18.045056836457));
#258557=CARTESIAN_POINT('Ctrl Pts',(-0.447383885885906,3.22208218530956,
18.2038789770117));
#258558=CARTESIAN_POINT('Ctrl Pts',(-2.95015730247948,1.37061684082573,
18.3627011175664));
#258559=CARTESIAN_POINT('Ctrl Pts',(-2.75093674236513,-1.73618915598547,
18.5215232581212));
#258560=CARTESIAN_POINT('Ctrl Pts',(-0.032207261648967,-3.2528146355384,
18.6803453986759));
#258561=CARTESIAN_POINT('Ctrl Pts',(2.71604923798135,-1.79033690289397,
18.8391675392306));
#258562=CARTESIAN_POINT('Ctrl Pts',(2.97667879057788,1.31202519494447,18.9979896797854));
#258563=CARTESIAN_POINT('Ctrl Pts',(0.511137881081572,3.21243919263648,
19.1568118203401));
#258564=CARTESIAN_POINT('Ctrl Pts',(-2.42274569087925,2.17120692618642,
19.3156339608948));
#258565=CARTESIAN_POINT('Ctrl Pts',(-3.13730174101935,-0.859653501631685,
19.4744561014495));
#258566=CARTESIAN_POINT('Ctrl Pts',(-0.97920893696225,-3.10113535697825,
19.6332782420043));
#258567=CARTESIAN_POINT('Ctrl Pts',(2.07713706628989,-2.50629030530919,
19.792100382559));
#258568=CARTESIAN_POINT('Ctrl Pts',(3.22831766439385,0.391889480307326,
19.9509225231137));
#258569=CARTESIAN_POINT('Ctrl Pts',(2.02850526978224,2.0727146039754,20.0568039501502));
#258570=CARTESIAN_POINT('Ctrl Pts',(1.20564430054383,2.47375567929494,20.1097446636685));
#258571=CARTESIAN_POINT('Ctrl Pts',(1.48738611075532,-2.08582659521589,
-0.109744663668464));
#258572=CARTESIAN_POINT('Ctrl Pts',(2.18120777963242,-1.59106796283684,
-0.0568039501502205));
#258573=CARTESIAN_POINT('Ctrl Pts',(3.02430299867442,0.136677879741996,
0.049077476886266));
#258574=CARTESIAN_POINT('Ctrl Pts',(1.52164942887829,2.62055945523898,0.207899617440994));
#258575=CARTESIAN_POINT('Ctrl Pts',(-1.37597293748352,2.69667001321051,
0.366721757995726));
#258576=CARTESIAN_POINT('Ctrl Pts',(-3.01267583673131,0.306790423899341,
0.525543898550453));
#258577=CARTESIAN_POINT('Ctrl Pts',(-1.89049782615453,-2.36605884750802,
0.684366039105185));
#258578=CARTESIAN_POINT('Ctrl Pts',(0.963337657127712,-2.87084708234112,
0.843188179659912));
#258579=CARTESIAN_POINT('Ctrl Pts',(2.9347727731123,-0.746831402421932,
1.00201032021465));
#258580=CARTESIAN_POINT('Ctrl Pts',(2.21836462553458,2.06147584198914,1.16083246076937));
#258581=CARTESIAN_POINT('Ctrl Pts',(-0.529823686747478,2.98157235673077,
1.3196546013241));
#258582=CARTESIAN_POINT('Ctrl Pts',(-2.79274344473406,1.17098857214945,
1.47847674187883));
#258583=CARTESIAN_POINT('Ctrl Pts',(-2.49785671319912,-1.71211950327285,
1.63729888243356));
#258584=CARTESIAN_POINT('Ctrl Pts',(0.0847675203110875,-3.02711251258291,
1.79612102298829));
#258585=CARTESIAN_POINT('Ctrl Pts',(2.58975293024786,-1.56964910623143,
1.95494316354302));
#258586=CARTESIAN_POINT('Ctrl Pts',(2.72284007956926,1.32542823321795,2.11376530409775));
#258587=CARTESIAN_POINT('Ctrl Pts',(0.362135646372212,3.00657111379819,
2.27258744465248));
#258588=CARTESIAN_POINT('Ctrl Pts',(-2.33024078659653,1.93406140121526,
2.43140958520721));
#258589=CARTESIAN_POINT('Ctrl Pts',(-2.88839965742654,-0.909814643775332,
2.59023172576194));
#258590=CARTESIAN_POINT('Ctrl Pts',(-0.801134952756186,-2.92041046573759,
2.74905386631667));
#258591=CARTESIAN_POINT('Ctrl Pts',(2.01987208480945,-2.25626501008188,
2.9078760068714));
#258592=CARTESIAN_POINT('Ctrl Pts',(2.99092148573722,0.47434545210521,3.06669814742613));
#258593=CARTESIAN_POINT('Ctrl Pts',(1.22264983011503,2.77051299239757,3.22552028798086));
#258594=CARTESIAN_POINT('Ctrl Pts',(-1.66542065934546,2.52922694794631,
3.38434242853559));
#258595=CARTESIAN_POINT('Ctrl Pts',(-3.02816797570811,-0.0285240023499908,
3.54316456909032));
#258596=CARTESIAN_POINT('Ctrl Pts',(-1.61748098166808,-2.56015041959512,
3.70198670964505));
#258597=CARTESIAN_POINT('Ctrl Pts',(1.27462226192968,-2.74698980663272,
3.86080885019978));
#258598=CARTESIAN_POINT('Ctrl Pts',(2.99932622686687,-0.417919956096872,
4.01963099075451));
#258599=CARTESIAN_POINT('Ctrl Pts',(1.97701142398513,2.29391384606539,4.17845313130924));
#258600=CARTESIAN_POINT('Ctrl Pts',(-0.856005874802533,2.90480099966259,
4.33727527186396));
#258601=CARTESIAN_POINT('Ctrl Pts',(-2.90502569376376,0.855243020032118,
4.4960974124187));
#258602=CARTESIAN_POINT('Ctrl Pts',(-2.29339458729873,-1.97761375692776,
4.65491955297342));
#258603=CARTESIAN_POINT('Ctrl Pts',(0.418707590396682,-2.99921637408935,
4.81374169352815));
#258604=CARTESIAN_POINT('Ctrl Pts',(2.74732443774844,-1.27390083543187,
4.97256383408288));
#258605=CARTESIAN_POINT('Ctrl Pts',(2.55972556853956,1.61815324321388,5.13138597463761));
#258606=CARTESIAN_POINT('Ctrl Pts',(0.0277287763463851,3.02817536145956,
5.29020811519234));
#258607=CARTESIAN_POINT('Ctrl Pts',(-2.52966420928092,1.66475640652201,
5.44903025574707));
#258608=CARTESIAN_POINT('Ctrl Pts',(-2.77019182817363,-1.22337734975502,
5.6078523963018));
#258609=CARTESIAN_POINT('Ctrl Pts',(-0.4735599765103,-2.9910459463915,5.76667453685653));
#258610=CARTESIAN_POINT('Ctrl Pts',(2.25679533324014,-2.01927950730963,
5.92549667741126));
#258611=CARTESIAN_POINT('Ctrl Pts',(2.92020004606639,0.801901861657186,
6.084318817966));
#258612=CARTESIAN_POINT('Ctrl Pts',(0.909055968644706,2.88863845966353,
6.24314095852072));
#258613=CARTESIAN_POINT('Ctrl Pts',(-1.93467303544375,2.32973284964229,
6.40196309907545));
#258614=CARTESIAN_POINT('Ctrl Pts',(-3.00647636839827,-0.362925269219867,
6.56078523963017));
#258615=CARTESIAN_POINT('Ctrl Pts',(-1.32471227201173,-2.72318789310565,
6.71960738018491));
#258616=CARTESIAN_POINT('Ctrl Pts',(1.57032747283876,-2.58934094565073,
6.87842952073963));
#258617=CARTESIAN_POINT('Ctrl Pts',(3.02713785787826,-0.0839719844699643,
7.03725166129438));
#258618=CARTESIAN_POINT('Ctrl Pts',(1.71145739709093,2.4983051220214,7.19607380184909));
#258619=CARTESIAN_POINT('Ctrl Pts',(-1.17171030386558,2.79243797936335,
7.35489594240384));
#258620=CARTESIAN_POINT('Ctrl Pts',(-2.98173358790239,0.529036591882203,
7.51371808295854));
#258621=CARTESIAN_POINT('Ctrl Pts',(-2.06085082627003,-2.21889809965165,
7.67254022351329));
#258622=CARTESIAN_POINT('Ctrl Pts',(0.747521147516374,-2.93459146028735,
7.83136236406802));
#258623=CARTESIAN_POINT('Ctrl Pts',(2.87125448379991,-0.962555242068991,
7.99018450462274));
#258624=CARTESIAN_POINT('Ctrl Pts',(2.36526722389161,1.89106474356635,8.14900664517748));
#258625=CARTESIAN_POINT('Ctrl Pts',(-0.307017718531236,3.01269896028187,
8.3078287857322));
#258626=CARTESIAN_POINT('Ctrl Pts',(-2.69811169638694,1.37506660878503,
8.46665092628694));
#258627=CARTESIAN_POINT('Ctrl Pts',(-2.61806285536416,-1.52195985168403,
8.62547306684166));
#258628=CARTESIAN_POINT('Ctrl Pts',(-0.140186217564388,-3.02505582248999,
8.78429520739639));
#258629=CARTESIAN_POINT('Ctrl Pts',(2.46608397981406,-1.75756783916868,
8.94311734795112));
#258630=CARTESIAN_POINT('Ctrl Pts',(2.81372058332409,1.11963895241009,9.10193948850585));
#258631=CARTESIAN_POINT('Ctrl Pts',(0.584330660051387,2.9713923646162,9.26076162906059));
#258632=CARTESIAN_POINT('Ctrl Pts',(-2.1802352221596,2.10171103647249,9.41958376961531));
#258633=CARTESIAN_POINT('Ctrl Pts',(-2.94797027638068,-0.692882496785455,
9.57840591017004));
#258634=CARTESIAN_POINT('Ctrl Pts',(-1.01572238011805,-2.8528797646068,
9.73722805072478));
#258635=CARTESIAN_POINT('Ctrl Pts',(1.84680392862249,-2.39998544870592,
9.89605019127949));
#258636=CARTESIAN_POINT('Ctrl Pts',(3.01788200258335,0.25100422956428,10.0548723318342));
#258637=CARTESIAN_POINT('Ctrl Pts',(1.42494647069792,2.67210450028084,10.213694472389));
#258638=CARTESIAN_POINT('Ctrl Pts',(-1.47306706928727,2.64588138701586,
10.3725166129437));
#258639=CARTESIAN_POINT('Ctrl Pts',(-3.02192997371126,0.196352078575943,
10.5313387534984));
#258640=CARTESIAN_POINT('Ctrl Pts',(-1.80307182207585,-2.43301190075423,
10.6901608940532));
#258641=CARTESIAN_POINT('Ctrl Pts',(1.06718126291666,-2.83403229636771,
10.8489830346079));
#258642=CARTESIAN_POINT('Ctrl Pts',(2.96002584483288,-0.639423101472757,
11.0078051751626));
#258643=CARTESIAN_POINT('Ctrl Pts',(2.14184603886008,2.1408200416184,11.1666273157173));
#258644=CARTESIAN_POINT('Ctrl Pts',(-0.638004762853933,2.96033187790681,
11.3254494562721));
#258645=CARTESIAN_POINT('Ctrl Pts',(-2.83352064238958,1.06853903715664,
11.4842715968268));
#258646=CARTESIAN_POINT('Ctrl Pts',(-2.43387554435661,-1.8019058630679,
11.6430937373815));
#258647=CARTESIAN_POINT('Ctrl Pts',(0.194904130104354,-3.02202370686332,
11.8019158779362));
#258648=CARTESIAN_POINT('Ctrl Pts',(2.64517527872404,-1.4743346464093,11.960738018491));
#258649=CARTESIAN_POINT('Ctrl Pts',(2.67278694165709,1.42366599639206,12.1195601590457));
#258650=CARTESIAN_POINT('Ctrl Pts',(0.252450187142197,3.01776139013466,
12.2783822996004));
#258651=CARTESIAN_POINT('Ctrl Pts',(-2.39910029655829,1.84795364439411,
12.4372044401552));
#258652=CARTESIAN_POINT('Ctrl Pts',(-2.85336610981753,-1.01435533622114,
12.5960265807099));
#258653=CARTESIAN_POINT('Ctrl Pts',(-0.694294906173836,-2.9476379506372,
12.7548487212646));
#258654=CARTESIAN_POINT('Ctrl Pts',(2.10066615846894,-2.18124198461312,
12.9136708618194));
#258655=CARTESIAN_POINT('Ctrl Pts',(2.97167199942212,0.582906881608178,
13.0724930023741));
#258656=CARTESIAN_POINT('Ctrl Pts',(1.12098698848508,2.81318379712787,13.2313151429288));
#258657=CARTESIAN_POINT('Ctrl Pts',(-1.75638603924554,2.46692581686579,
13.3901372834835));
#258658=CARTESIAN_POINT('Ctrl Pts',(-3.02512264400222,-0.138736777822433,
13.5489594240383));
#258659=CARTESIAN_POINT('Ctrl Pts',(-1.52321409423724,-2.61733332380355,
13.707781564593));
#258660=CARTESIAN_POINT('Ctrl Pts',(1.37377367913049,-2.69877023536724,
13.8666037051478));
#258661=CARTESIAN_POINT('Ctrl Pts',(3.01255151015457,-0.30846118627934,
14.0254258457024));
#258662=CARTESIAN_POINT('Ctrl Pts',(1.89219781938555,2.36436086862553,14.1842479862572));
#258663=CARTESIAN_POINT('Ctrl Pts',(-0.961179400221878,2.87171535242729,
14.3430701268119));
#258664=CARTESIAN_POINT('Ctrl Pts',(-2.93423295654511,0.748927140313446,
14.5018922673667));
#258665=CARTESIAN_POINT('Ctrl Pts',(-2.21988527992798,-2.05978742804493,
14.6607144079214));
#258666=CARTESIAN_POINT('Ctrl Pts',(0.527607864898483,-2.98198672795264,
14.8195365484761));
#258667=CARTESIAN_POINT('Ctrl Pts',(2.79187624616883,-1.17304813662401,
14.9783586890308));
#258668=CARTESIAN_POINT('Ctrl Pts',(2.49912486204435,1.71026016403225,15.1371808295856));
#258669=CARTESIAN_POINT('Ctrl Pts',(-0.082521553600458,3.02717774470757,
15.2960029701403));
#258670=CARTESIAN_POINT('Ctrl Pts',(-2.5885882425409,1.57156794801246,15.454825110695));
#258671=CARTESIAN_POINT('Ctrl Pts',(-2.72382230247565,-1.32340733309041,
15.6136472512498));
#258672=CARTESIAN_POINT('Ctrl Pts',(-0.364365749025758,-3.00630213156863,
15.7724693918045));
#258673=CARTESIAN_POINT('Ctrl Pts',(2.32880560393364,-1.93578908014936,
15.9312915323592));
#258674=CARTESIAN_POINT('Ctrl Pts',(2.88907369281068,0.90767180323327,16.090113672914));
#258675=CARTESIAN_POINT('Ctrl Pts',(0.803300952471413,2.91981548870976,
16.2489358134687));
#258676=CARTESIAN_POINT('Ctrl Pts',(-2.01819795532617,2.25776258940755,
16.4077579540234));
#258677=CARTESIAN_POINT('Ctrl Pts',(-2.9912725052335,-0.472126791495962,
16.5665800945781));
#258678=CARTESIAN_POINT('Ctrl Pts',(-1.22470451586104,-2.76960534654705,
16.7254022351329));
#258679=CARTESIAN_POINT('Ctrl Pts',(1.66354415017768,-2.53046156037463,
16.8842243756876));
#258680=CARTESIAN_POINT('Ctrl Pts',(3.0281883060719,0.0262778375603132,
17.0430465162423));
#258681=CARTESIAN_POINT('Ctrl Pts',(1.61937951108125,2.55894998657703,17.2018686567971));
#258682=CARTESIAN_POINT('Ctrl Pts',(-1.27258431481161,2.74793443564667,
17.3606907973518));
#258683=CARTESIAN_POINT('Ctrl Pts',(-2.99901545403822,0.420144705416821,
17.5195129379065));
#258684=CARTESIAN_POINT('Ctrl Pts',(-1.97871230263384,-2.29244700060747,
17.6783350784613));
#258685=CARTESIAN_POINT('Ctrl Pts',(0.853850850599735,-2.90543470304,17.837157219016));
#258686=CARTESIAN_POINT('Ctrl Pts',(2.90439082319782,-0.857398417565761,
17.9959793595707));
#258687=CARTESIAN_POINT('Ctrl Pts',(2.29486026810186,1.97591368898239,18.1548015001254));
#258688=CARTESIAN_POINT('Ctrl Pts',(-0.416481707292041,2.99952307606173,
18.3136236406802));
#258689=CARTESIAN_POINT('Ctrl Pts',(-2.74638087977544,1.27594412744645,
18.4724457812349));
#258690=CARTESIAN_POINT('Ctrl Pts',(-2.56092109541194,-1.61626524038718,
18.6312679217896));
#258691=CARTESIAN_POINT('Ctrl Pts',(-0.0299826072014076,-3.0281327415959,
18.7900900623443));
#258692=CARTESIAN_POINT('Ctrl Pts',(2.52844337807053,-1.6666728361677,18.9489122028991));
#258693=CARTESIAN_POINT('Ctrl Pts',(2.77107044726236,1.22139958643925,19.1077343434538));
#258694=CARTESIAN_POINT('Ctrl Pts',(0.475832018296617,2.99054615449931,
19.2665564840086));
#258695=CARTESIAN_POINT('Ctrl Pts',(-2.25539920749206,2.02123499757207,
19.4253786245633));
#258696=CARTESIAN_POINT('Ctrl Pts',(-2.92059867735871,-0.80027459489331,
19.584200765118));
#258697=CARTESIAN_POINT('Ctrl Pts',(-0.911571969236381,-2.88693041650442,
19.7430229056727));
#258698=CARTESIAN_POINT('Ctrl Pts',(1.93366283171984,-2.33317313889758,
19.9018450462275));
#258699=CARTESIAN_POINT('Ctrl Pts',(3.00532785146098,0.364820470690377,
20.0606671867822));
#258700=CARTESIAN_POINT('Ctrl Pts',(1.88839018271039,1.92954584245562,20.1665486138187));
#258701=CARTESIAN_POINT('Ctrl Pts',(1.12236674703443,2.3028857793927,20.2194893273369));
#258702=CARTESIAN_POINT('Ctrl Pts',(1.37702479013101,-1.93106208855765,
-2.4980018054066E-15));
#258703=CARTESIAN_POINT('Ctrl Pts',(2.01936616407906,-1.47301363900524,
0.0529407135182407));
#258704=CARTESIAN_POINT('Ctrl Pts',(2.79990526463056,0.126536631817626,
0.158822140554727));
#258705=CARTESIAN_POINT('Ctrl Pts',(1.40874583290953,2.42611875140058,0.317644281109456));
#258706=CARTESIAN_POINT('Ctrl Pts',(-1.27387826991474,2.49658204560485,
0.476466421664188));
#258707=CARTESIAN_POINT('Ctrl Pts',(-2.78914081677217,0.284027137290959,
0.635288562218914));
#258708=CARTESIAN_POINT('Ctrl Pts',(-1.75022635580586,-2.19050162185044,
0.794110702773647));
#258709=CARTESIAN_POINT('Ctrl Pts',(0.891859770330893,-2.65783549575534,
0.952932843328373));
#258710=CARTESIAN_POINT('Ctrl Pts',(2.71701801755088,-0.691417882516756,
1.11175498388311));
#258711=CARTESIAN_POINT('Ctrl Pts',(2.05376604018409,1.90851811654588,1.27057712443783));
#258712=CARTESIAN_POINT('Ctrl Pts',(-0.490511741217893,2.76034515792448,
1.42939926499256));
#258713=CARTESIAN_POINT('Ctrl Pts',(-2.58552700476795,1.08410336841926,
1.58822140554729));
#258714=CARTESIAN_POINT('Ctrl Pts',(-2.31252032770672,-1.58508337722494,
1.74704354610202));
#258715=CARTESIAN_POINT('Ctrl Pts',(0.078477925820518,-2.80250631776144,
1.90586568665675));
#258716=CARTESIAN_POINT('Ctrl Pts',(2.39759801404543,-1.4531840222644,2.06468782721148));
#258717=CARTESIAN_POINT('Ctrl Pts',(2.520810341052,1.22708388997517,2.22350996776621));
#258718=CARTESIAN_POINT('Ctrl Pts',(0.335265845793994,2.78348905308081,
2.38233210832094));
#258719=CARTESIAN_POINT('Ctrl Pts',(-2.15734119534592,1.79055759351985,
2.54115424887567));
#258720=CARTESIAN_POINT('Ctrl Pts',(-2.67408570197179,-0.842308066374673,
2.6999763894304));
#258721=CARTESIAN_POINT('Ctrl Pts',(-0.741692209042783,-2.70372136703395,
2.85879852998513));
#258722=CARTESIAN_POINT('Ctrl Pts',(1.87000128182168,-2.08885428573093,
3.01762067053986));
#258723=CARTESIAN_POINT('Ctrl Pts',(2.76900059871079,0.439149889804403,
3.17644281109459));
#258724=CARTESIAN_POINT('Ctrl Pts',(1.13193145582276,2.56494601121031,3.33526495164932));
#258725=CARTESIAN_POINT('Ctrl Pts',(-1.54184950184215,2.34156294858825,
3.49408709220405));
#258726=CARTESIAN_POINT('Ctrl Pts',(-2.80348346745913,-0.0264075737064492,
3.65290923275878));
#258727=CARTESIAN_POINT('Ctrl Pts',(-1.49746686029714,-2.37019195537365,
3.81173137331351));
#258728=CARTESIAN_POINT('Ctrl Pts',(1.18004762854664,-2.54316820267302,
3.97055351386824));
#258729=CARTESIAN_POINT('Ctrl Pts',(2.77678172346816,-0.3869110620803,4.12937565442297));
#258730=CARTESIAN_POINT('Ctrl Pts',(1.83032080339732,2.12370964715592,4.2881977949777));
#258731=CARTESIAN_POINT('Ctrl Pts',(-0.792491809340816,2.68927009470421,
4.44701993553242));
#258732=CARTESIAN_POINT('Ctrl Pts',(-2.68947811691531,0.791785556994785,
4.60584207608716));
#258733=CARTESIAN_POINT('Ctrl Pts',(-2.12322891643708,-1.83087844434069,
4.76466421664189));
#258734=CARTESIAN_POINT('Ctrl Pts',(0.387640255360107,-2.77668002156518,
4.92348635719661));
#258735=CARTESIAN_POINT('Ctrl Pts',(2.54347800477387,-1.17937973057141,
5.08230849775135));
#258736=CARTESIAN_POINT('Ctrl Pts',(2.36979862748696,1.49808924126962,5.24113063830607));
#258737=CARTESIAN_POINT('Ctrl Pts',(0.0256713520133373,2.80349030520137,
5.3999527788608));
#258738=CARTESIAN_POINT('Ctrl Pts',(-2.34196776593405,1.54123453535952,
5.55877491941554));
#258739=CARTESIAN_POINT('Ctrl Pts',(-2.56464867678256,-1.13260499484022,
5.71759705997026));
#258740=CARTESIAN_POINT('Ctrl Pts',(-0.438422695057549,-2.76911582461286,
5.876419200525));
#258741=CARTESIAN_POINT('Ctrl Pts',(2.08934525988381,-1.86945267248516,
6.03524134107972));
#258742=CARTESIAN_POINT('Ctrl Pts',(2.7035265601163,0.742402214710351,6.19406348163445));
#258743=CARTESIAN_POINT('Ctrl Pts',(0.841605683546825,2.67430678552092,
6.35288562218919));
#258744=CARTESIAN_POINT('Ctrl Pts',(-1.79112384561072,2.15687094638179,
6.5117077627439));
#258745=CARTESIAN_POINT('Ctrl Pts',(-2.78340133761574,-0.335996880075048,
6.67052990329864));
#258746=CARTESIAN_POINT('Ctrl Pts',(-1.2264210517769,-2.5211323474621,6.82935204385337));
#258747=CARTESIAN_POINT('Ctrl Pts',(1.45381205531404,-2.39721659794956,
6.9881741844081));
#258748=CARTESIAN_POINT('Ctrl Pts',(2.80252978248238,-0.0777414172792658,
7.14699632496283));
#258749=CARTESIAN_POINT('Ctrl Pts',(1.58447039810697,2.31293546541706,7.30581846551756));
#258750=CARTESIAN_POINT('Ctrl Pts',(-1.08477154896619,2.58524420436732,
7.46464060607229));
#258751=CARTESIAN_POINT('Ctrl Pts',(-2.76049442603897,0.489783047347568,
7.62346274662702));
#258752=CARTESIAN_POINT('Ctrl Pts',(-1.90793947584643,-2.05425993150043,
7.78228488718174));
#258753=CARTESIAN_POINT('Ctrl Pts',(0.692056449790645,-2.71685015780489,
7.94110702773648));
#258754=CARTESIAN_POINT('Ctrl Pts',(2.65821266877332,-0.891135409034062,
8.0999291682912));
#258755=CARTESIAN_POINT('Ctrl Pts',(2.18976873525401,1.75075120898583,8.25875130884594));
#258756=CARTESIAN_POINT('Ctrl Pts',(-0.284237567078199,2.78916222459769,
8.41757344940066));
#258757=CARTESIAN_POINT('Ctrl Pts',(-2.49791675853455,1.27303918914287,
8.57639558995541));
#258758=CARTESIAN_POINT('Ctrl Pts',(-2.42380739465615,-1.40903322291262,
8.73521773051011));
#258759=CARTESIAN_POINT('Ctrl Pts',(-0.129784657410042,-2.80060223030017,
8.89403987106487));
#258760=CARTESIAN_POINT('Ctrl Pts',(2.28310507284784,-1.62715952997786,
9.05286201161958));
#258761=CARTESIAN_POINT('Ctrl Pts',(2.60494767815974,1.03656379625737,9.21168415217432));
#258762=CARTESIAN_POINT('Ctrl Pts',(0.540974397102402,2.75092050254836,
9.37050629272904));
#258763=CARTESIAN_POINT('Ctrl Pts',(-2.01846576858645,1.94576793341498,
9.52932843328377));
#258764=CARTESIAN_POINT('Ctrl Pts',(-2.7292362902892,-0.6414718867026,9.68815057383851));
#258765=CARTESIAN_POINT('Ctrl Pts',(-0.940357642981567,-2.64120132003364,
9.84697271439322));
#258766=CARTESIAN_POINT('Ctrl Pts',(1.70977446530886,-2.22191093148198,
10.005794854948));
#258767=CARTESIAN_POINT('Ctrl Pts',(2.79396069466933,0.232380176228921,
10.1646169955027));
#258768=CARTESIAN_POINT('Ctrl Pts',(1.3192180568126,2.47383924866609,10.3234391360574));
#258769=CARTESIAN_POINT('Ctrl Pts',(-1.36376819526984,2.44956184229582,
10.4822612766122));
#258770=CARTESIAN_POINT('Ctrl Pts',(-2.79770831376606,0.181783114577756,
10.6410834171669));
#258771=CARTESIAN_POINT('Ctrl Pts',(-1.66928720083601,-2.25248688137943,
10.7999055577216));
#258772=CARTESIAN_POINT('Ctrl Pts',(0.987998371084236,-2.62375229935987,
10.9587276982763));
#258773=CARTESIAN_POINT('Ctrl Pts',(2.74039735767968,-0.591979080444202,
11.1175498388311));
#258774=CARTESIAN_POINT('Ctrl Pts',(1.98292499225804,1.98197512212938,11.2763719793858));
#258775=CARTESIAN_POINT('Ctrl Pts',(-0.590665979948808,2.74068068366097,
11.4351941199405));
#258776=CARTESIAN_POINT('Ctrl Pts',(-2.62327860916824,0.989255400966587,
11.5940162604952));
#258777=CARTESIAN_POINT('Ctrl Pts',(-2.25328644421095,-1.66820775384737,
11.75283840105));
#258778=CARTESIAN_POINT('Ctrl Pts',(0.180442601226353,-2.79779509209019,
11.9116605416047));
#258779=CARTESIAN_POINT('Ctrl Pts',(2.44890812594382,-1.36494172049492,
12.0704826821594));
#258780=CARTESIAN_POINT('Ctrl Pts',(2.47447105414424,1.31803259135108,12.2293048227142));
#258781=CARTESIAN_POINT('Ctrl Pts',(0.233718846407313,2.79384903144306,
12.3881269632689));
#258782=CARTESIAN_POINT('Ctrl Pts',(-2.2210914559998,1.7108388742795,12.5469491038237));
#258783=CARTESIAN_POINT('Ctrl Pts',(-2.64165157932199,-0.939092031233823,
12.7057712443783));
#258784=CARTESIAN_POINT('Ctrl Pts',(-0.642779497905573,-2.7289286225062,
12.8645933849331));
#258785=CARTESIAN_POINT('Ctrl Pts',(1.94480058344235,-2.01939783111293,
13.0234155254878));
#258786=CARTESIAN_POINT('Ctrl Pts',(2.7511793889647,0.539656260407611,13.1822376660426));
#258787=CARTESIAN_POINT('Ctrl Pts',(1.03781181052871,2.60445072051449,13.3410598065973));
#258788=CARTESIAN_POINT('Ctrl Pts',(-1.62606541744088,2.28388444713476,
13.499881947152));
#258789=CARTESIAN_POINT('Ctrl Pts',(-2.80066409377878,-0.128442763437796,
13.6587040877067));
#258790=CARTESIAN_POINT('Ctrl Pts',(-1.41019440296941,-2.42313199299893,
13.8175262282615));
#258791=CARTESIAN_POINT('Ctrl Pts',(1.27184219249669,-2.49852643513066,
13.9763483688162));
#258792=CARTESIAN_POINT('Ctrl Pts',(2.78902571499932,-0.285573932167581,
14.1351705093709));
#258793=CARTESIAN_POINT('Ctrl Pts',(1.75180021265799,2.18892962988587,14.2939926499257));
#258794=CARTESIAN_POINT('Ctrl Pts',(-0.889861652127881,2.65863934179406,
14.4528147904804));
#258795=CARTESIAN_POINT('Ctrl Pts',(-2.71651825438262,0.693358120501612,
14.6116369310351));
#258796=CARTESIAN_POINT('Ctrl Pts',(-2.05517386481133,-1.90695497981872,
14.7704590715899));
#258797=CARTESIAN_POINT('Ctrl Pts',(0.488460329284891,-2.7607287835619,
14.9292812121446));
#258798=CARTESIAN_POINT('Ctrl Pts',(2.58472415074527,-1.08601011698834,
15.0881033526993));
#258799=CARTESIAN_POINT('Ctrl Pts',(2.31369438223421,1.5833619975448,15.246925493254));
#258800=CARTESIAN_POINT('Ctrl Pts',(-0.0763986057193116,2.80256670978213,
15.4057476338088));
#258801=CARTESIAN_POINT('Ctrl Pts',(-2.39651974402956,1.45496048950563,
15.5645697743635));
#258802=CARTESIAN_POINT('Ctrl Pts',(-2.52171968482074,-1.2252129369295,
15.7233919149182));
#258803=CARTESIAN_POINT('Ctrl Pts',(-0.33733047892205,-2.7832400288392,
15.882214055473));
#258804=CARTESIAN_POINT('Ctrl Pts',(2.15601250060359,-1.79215708184668,
16.0410361960277));
#258805=CARTESIAN_POINT('Ctrl Pts',(2.67470972516702,0.840324220669528,
16.1998583365824));
#258806=CARTESIAN_POINT('Ctrl Pts',(0.743697495552939,2.70317053621002,
16.3586804771371));
#258807=CARTESIAN_POINT('Ctrl Pts',(-1.86845136967466,2.09024074741813,
16.5175026176919));
#258808=CARTESIAN_POINT('Ctrl Pts',(-2.76932557320444,-0.437095849741951,
16.6763247582466));
#258809=CARTESIAN_POINT('Ctrl Pts',(-1.13383368765599,-2.56410571101671,
16.8351468988013));
#258810=CARTESIAN_POINT('Ctrl Pts',(1.54011222621193,-2.34270595503943,
16.9939690393561));
#258811=CARTESIAN_POINT('Ctrl Pts',(2.80350228934723,0.0243280702232952,
17.1527911799108));
#258812=CARTESIAN_POINT('Ctrl Pts',(1.49922452231095,2.36908059228316,17.3116133204655));
#258813=CARTESIAN_POINT('Ctrl Pts',(-1.17816089336587,2.54404274194716,
17.4704354610202));
#258814=CARTESIAN_POINT('Ctrl Pts',(-2.77649400941324,0.388970739082288,
17.629257601575));
#258815=CARTESIAN_POINT('Ctrl Pts',(-1.83189547997077,-2.12235163893987,
17.7880797421297));
#258816=CARTESIAN_POINT('Ctrl Pts',(0.790496683980206,-2.68985677845362,
17.9469018826844));
#258817=CARTESIAN_POINT('Ctrl Pts',(2.68889035258062,-0.793781027985773,
18.1057240232392));
#258818=CARTESIAN_POINT('Ctrl Pts',(2.1245858464136,1.82930451831788,18.2645461637939));
#258819=CARTESIAN_POINT('Ctrl Pts',(-0.385579528698175,2.7769639668139,
18.4233683043486));
#258820=CARTESIAN_POINT('Ctrl Pts',(-2.5426044570714,1.18127141406717,18.5821904449034));
#258821=CARTESIAN_POINT('Ctrl Pts',(-2.37090544845875,-1.49634132478888,
18.7410125854581));
#258822=CARTESIAN_POINT('Ctrl Pts',(-0.0277579527538448,-2.80345084765341,
18.8998347260128));
#258823=CARTESIAN_POINT('Ctrl Pts',(2.3408375181597,-1.54300876944143,19.0586568665676));
#258824=CARTESIAN_POINT('Ctrl Pts',(2.56546210394684,1.13077397793403,19.2174790071223));
#258825=CARTESIAN_POINT('Ctrl Pts',(0.440526155511663,2.76865311636215,
19.376301147677));
#258826=CARTESIAN_POINT('Ctrl Pts',(-2.08805272410487,1.87126306895772,
19.5351232882317));
#258827=CARTESIAN_POINT('Ctrl Pts',(-2.70389561369807,-0.740895688154933,
19.6939454287865));
#258828=CARTESIAN_POINT('Ctrl Pts',(-0.843935001510512,-2.67272547603058,
19.8527675693412));
#258829=CARTESIAN_POINT('Ctrl Pts',(1.79018859714979,-2.16005597248598,
20.0115897098959));
#258830=CARTESIAN_POINT('Ctrl Pts',(2.7823380385281,0.337751461073428,20.1704118504506));
#258831=CARTESIAN_POINT('Ctrl Pts',(1.74827509563854,1.78637708093585,20.2762932774871));
#258832=CARTESIAN_POINT('Ctrl Pts',(1.03908919352503,2.13201587949046,20.3292339910054));
#258833=CARTESIAN_POINT('',(1.28892185405323,2.64462557919718,20.));
#258834=CARTESIAN_POINT('Ctrl Pts',(1.38000112159638,-1.93372602389037,
20.));
#258835=CARTESIAN_POINT('Ctrl Pts',(1.43104039670144,-1.90596629917353,
20.));
#258836=CARTESIAN_POINT('Ctrl Pts',(1.48086808386216,-1.87627442504008,
20.));
#258837=CARTESIAN_POINT('Ctrl Pts',(1.52936177959298,-1.84468159128334,
20.));
#258838=CARTESIAN_POINT('Ctrl Pts',(1.59716821331816,-1.80050683091434,
20.));
#258839=CARTESIAN_POINT('Ctrl Pts',(1.66236782235411,-1.75261800820872,
20.));
#258840=CARTESIAN_POINT('Ctrl Pts',(1.72488638260891,-1.70138403719481,
20.));
#258841=CARTESIAN_POINT('Ctrl Pts',(1.78902316386727,-1.64882393378674,
20.));
#258842=CARTESIAN_POINT('Ctrl Pts',(1.8503388588045,-1.5927428737396,20.));
#258843=CARTESIAN_POINT('Ctrl Pts',(1.90873407605101,-1.53348793892088,
20.));
#258844=CARTESIAN_POINT('Ctrl Pts',(1.96836316935041,-1.47298096243615,
20.));
#258845=CARTESIAN_POINT('Ctrl Pts',(2.02494770374105,-1.40916401657361,
20.));
#258846=CARTESIAN_POINT('Ctrl Pts',(2.07835290128116,-1.34236124876648,
20.));
#258847=CARTESIAN_POINT('Ctrl Pts',(2.08686002520482,-1.33171997319116,
20.));
#258848=CARTESIAN_POINT('Ctrl Pts',(2.09528652032987,-1.32100257727076,
20.));
#258849=CARTESIAN_POINT('Ctrl Pts',(2.10362268727388,-1.31022238979363,
20.));
#258850=CARTESIAN_POINT('Ctrl Pts',(2.15664189201375,-1.2416588676349,20.));
#258851=CARTESIAN_POINT('Ctrl Pts',(2.20610243814027,-1.17044390820985,
20.));
#258852=CARTESIAN_POINT('Ctrl Pts',(2.25191648819796,-1.09697647600033,
20.));
#258853=CARTESIAN_POINT('Ctrl Pts',(2.29866887655797,-1.0220043240481,20.));
#258854=CARTESIAN_POINT('Ctrl Pts',(2.34162449612302,-0.944685869277743,
20.));
#258855=CARTESIAN_POINT('Ctrl Pts',(2.38066172624132,-0.86539794489534,
20.));
#258856=CARTESIAN_POINT('Ctrl Pts',(2.42000062340461,-0.785497309165861,
20.));
#258857=CARTESIAN_POINT('Ctrl Pts',(2.45536096486505,-0.703595853686508,
20.));
#258858=CARTESIAN_POINT('Ctrl Pts',(2.48658040767009,-0.62004268886668,
20.));
#258859=CARTESIAN_POINT('Ctrl Pts',(2.50067454461614,-0.582322292810884,
20.));
#258860=CARTESIAN_POINT('Ctrl Pts',(2.51392415514951,-0.544264842490704,
20.));
#258861=CARTESIAN_POINT('Ctrl Pts',(2.52631126586128,-0.505900729858203,
20.));
#258862=CARTESIAN_POINT('Ctrl Pts',(2.53056444695775,-0.492728205414998,
20.));
#258863=CARTESIAN_POINT('Ctrl Pts',(2.53471592773745,-0.479519520243206,
20.));
#258864=CARTESIAN_POINT('Ctrl Pts',(2.53876492381411,-0.46627588320346,
20.));
#258865=CARTESIAN_POINT('Ctrl Pts',(2.54272170769679,-0.453333857922437,
20.));
#258866=CARTESIAN_POINT('Ctrl Pts',(2.5465779933553,-0.44036701015714,20.));
#258867=CARTESIAN_POINT('Ctrl Pts',(2.55033280274283,-0.427378822049379,
20.));
#258868=CARTESIAN_POINT('Ctrl Pts',(2.57581353743285,-0.339238908375791,
20.));
#258869=CARTESIAN_POINT('Ctrl Pts',(2.59663392622878,-0.250087233771202,
20.));
#258870=CARTESIAN_POINT('Ctrl Pts',(2.61267173384564,-0.160322906932646,
20.));
#258871=CARTESIAN_POINT('Ctrl Pts',(2.62865972446749,-0.0708374080441688,
20.));
#258872=CARTESIAN_POINT('Ctrl Pts',(2.63989534171169,0.0192578513483404,
20.));
#258873=CARTESIAN_POINT('Ctrl Pts',(2.64621597035763,0.109597181710584,
20.));
#258874=CARTESIAN_POINT('Ctrl Pts',(2.65109085997397,0.179272887751659,
20.));
#258875=CARTESIAN_POINT('Ctrl Pts',(2.65304130476616,0.24909449849761,20.));
#258876=CARTESIAN_POINT('Ctrl Pts',(2.65197262376409,0.31890119631434,20.));
#258877=CARTESIAN_POINT('Ctrl Pts',(2.65108318146032,0.376999946086523,
20.));
#258878=CARTESIAN_POINT('Ctrl Pts',(2.64810211482615,0.435088533644068,
20.));
#258879=CARTESIAN_POINT('Ctrl Pts',(2.64308540245169,0.493094560823236,
20.));
#258880=CARTESIAN_POINT('Ctrl Pts',(2.64180721514896,0.507873675488013,
20.));
#258881=CARTESIAN_POINT('Ctrl Pts',(2.64039683402233,0.522647431607784,
20.));
#258882=CARTESIAN_POINT('Ctrl Pts',(2.63885508706822,0.537414630746964,
20.));
#258883=CARTESIAN_POINT('Ctrl Pts',(2.63731701688765,0.552146612922076,
20.));
#258884=CARTESIAN_POINT('Ctrl Pts',(2.63564900582864,0.566864075411001,
20.));
#258885=CARTESIAN_POINT('Ctrl Pts',(2.63385310696625,0.581559801841969,
20.));
#258886=CARTESIAN_POINT('Ctrl Pts',(2.62304356262524,0.67001361725719,20.));
#258887=CARTESIAN_POINT('Ctrl Pts',(2.6075979139829,0.757747286034274,20.));
#258888=CARTESIAN_POINT('Ctrl Pts',(2.58779888199941,0.844496593095176,
20.));
#258889=CARTESIAN_POINT('Ctrl Pts',(2.5668320373806,0.936362662277352,20.));
#258890=CARTESIAN_POINT('Ctrl Pts',(2.54098334417491,1.02712551913946,20.));
#258891=CARTESIAN_POINT('Ctrl Pts',(2.5105286039796,1.11648109850773,20.));
#258892=CARTESIAN_POINT('Ctrl Pts',(2.4838807063087,1.19466723045496,20.));
#258893=CARTESIAN_POINT('Ctrl Pts',(2.45370523303439,1.27177643242526,20.));
#258894=CARTESIAN_POINT('Ctrl Pts',(2.42015135515334,1.3476035881054,20.));
#258895=CARTESIAN_POINT('Ctrl Pts',(2.40261366909957,1.38723634993944,20.));
#258896=CARTESIAN_POINT('Ctrl Pts',(2.38415251762534,1.42651880651212,20.));
#258897=CARTESIAN_POINT('Ctrl Pts',(2.36478585672699,1.46542086170342,20.));
#258898=CARTESIAN_POINT('Ctrl Pts',(2.35510885575605,1.48485917519657,20.));
#258899=CARTESIAN_POINT('Ctrl Pts',(2.34520573857011,1.50420250113221,20.));
#258900=CARTESIAN_POINT('Ctrl Pts',(2.33507854188857,1.52344700440923,20.));
#258901=CARTESIAN_POINT('Ctrl Pts',(2.32609493115886,1.54051837485496,20.));
#258902=CARTESIAN_POINT('Ctrl Pts',(2.31693343742811,1.55751456940709,20.));
#258903=CARTESIAN_POINT('Ctrl Pts',(2.30760786718556,1.57441093843168,20.));
#258904=CARTESIAN_POINT('Ctrl Pts',(2.2610478988748,1.65876979112269,20.));
#258905=CARTESIAN_POINT('Ctrl Pts',(2.21034456355009,1.74075363192982,20.));
#258906=CARTESIAN_POINT('Ctrl Pts',(2.1557571209275,1.82005591564008,20.));
#258907=CARTESIAN_POINT('Ctrl Pts',(2.09879739664546,1.90280454789056,20.));
#258908=CARTESIAN_POINT('Ctrl Pts',(2.03760859153995,1.98263458419847,20.));
#258909=CARTESIAN_POINT('Ctrl Pts',(1.97242793240484,2.05918273337975,20.));
#258910=CARTESIAN_POINT('Ctrl Pts',(1.9514213230739,2.08385288992916,20.));
#258911=CARTESIAN_POINT('Ctrl Pts',(1.92999966961265,2.10818198519152,20.));
#258912=CARTESIAN_POINT('Ctrl Pts',(1.90816974030175,2.13215724040594,20.));
#258913=CARTESIAN_POINT('Ctrl Pts',(1.89233578867659,2.14954726608397,20.));
#258914=CARTESIAN_POINT('Ctrl Pts',(1.87628380519926,2.16675431787413,20.));
#258915=CARTESIAN_POINT('Ctrl Pts',(1.86003660437627,2.18375258633449,20.));
#258916=CARTESIAN_POINT('Ctrl Pts',(1.79159664630606,2.25535635324592,20.));
#258917=CARTESIAN_POINT('Ctrl Pts',(1.71963685016589,2.32332525945659,20.));
#258918=CARTESIAN_POINT('Ctrl Pts',(1.64439743292523,2.38733140490762,20.));
#258919=CARTESIAN_POINT('Ctrl Pts',(1.57010648122843,2.45053069105827,20.));
#258920=CARTESIAN_POINT('Ctrl Pts',(1.49261756777843,2.50986732158365,20.));
#258921=CARTESIAN_POINT('Ctrl Pts',(1.41211902868467,2.56499971753534,20.));
#258922=CARTESIAN_POINT('Ctrl Pts',(1.37180215812419,2.5926122145607,20.));
#258923=CARTESIAN_POINT('Ctrl Pts',(1.33072972222921,2.61916963457235,20.));
#258924=CARTESIAN_POINT('Ctrl Pts',(1.28892185405323,2.64462557919718,20.));
#258925=CARTESIAN_POINT('Ctrl Pts',(1.29201717055307,2.64849452802569,1.73472347597681E-18));
#258926=CARTESIAN_POINT('Ctrl Pts',(1.35304057255792,2.61171371626496,-4.41564112292885E-17));
#258927=CARTESIAN_POINT('Ctrl Pts',(1.41253786891839,2.57261997258187,-1.97337342542082E-16));
#258928=CARTESIAN_POINT('Ctrl Pts',(1.47035891216485,2.53120529245361,-2.74086309204336E-16));
#258929=CARTESIAN_POINT('Ctrl Pts',(1.54979852115497,2.47430618079598,-3.7714836491708E-16));
#258930=CARTESIAN_POINT('Ctrl Pts',(1.6260758814995,2.41302695688629,1.41787018262576E-18));
#258931=CARTESIAN_POINT('Ctrl Pts',(1.6990147092737,2.34774686778585,2.04697370165263E-16));
#258932=CARTESIAN_POINT('Ctrl Pts',(1.73774680310026,2.3130817297078,3.12643177722203E-16));
#258933=CARTESIAN_POINT('Ctrl Pts',(1.77553678566096,2.27728785079842,-9.65553741364963E-17));
#258934=CARTESIAN_POINT('Ctrl Pts',(1.81235319455274,2.24041903484712,-9.0205620750794E-17));
#258935=CARTESIAN_POINT('Ctrl Pts',(1.83051349989456,2.22223287885251,-8.70734994005395E-17));
#258936=CARTESIAN_POINT('Ctrl Pts',(1.84843686678461,2.20378515234822,-5.57779331647957E-16));
#258937=CARTESIAN_POINT('Ctrl Pts',(1.8661191808394,2.18508218765713,-5.62050406216485E-16));
#258938=CARTESIAN_POINT('Ctrl Pts',(1.8813003216564,2.16902476780864,-5.6571733489244E-16));
#258939=CARTESIAN_POINT('Ctrl Pts',(1.89630589148148,2.15277668641829,-8.7084074591344E-16));
#258940=CARTESIAN_POINT('Ctrl Pts',(1.91111646711286,2.13636094210903,-8.53483950180589E-16));
#258941=CARTESIAN_POINT('Ctrl Pts',(1.97625654995093,2.06416098373011,-7.77145046144621E-16));
#258942=CARTESIAN_POINT('Ctrl Pts',(2.03769603328323,1.98865039987372,-5.52894930421052E-17));
#258943=CARTESIAN_POINT('Ctrl Pts',(2.09526132380736,1.910204650615,-2.35922392732846E-16));
#258944=CARTESIAN_POINT('Ctrl Pts',(2.14247204912315,1.84586934218999,-3.84063922683431E-16));
#258945=CARTESIAN_POINT('Ctrl Pts',(2.18707626360589,1.77955897818102,-1.9456188113995E-16));
#258946=CARTESIAN_POINT('Ctrl Pts',(2.22895387699605,1.71147104687654,-1.2490009027033E-16));
#258947=CARTESIAN_POINT('Ctrl Pts',(2.24792551730372,1.68062545570191,-9.33415000695447E-17));
#258948=CARTESIAN_POINT('Ctrl Pts',(2.26633725889061,1.64941497047097,-2.71651496365891E-16));
#258949=CARTESIAN_POINT('Ctrl Pts',(2.28417633551315,1.61785769665074,-3.19189119579733E-16));
#258950=CARTESIAN_POINT('Ctrl Pts',(2.29466973440569,1.59929490502404,-3.47151959436352E-16));
#258951=CARTESIAN_POINT('Ctrl Pts',(2.3049649666982,1.58061211955791,-4.10929051741138E-16));
#258952=CARTESIAN_POINT('Ctrl Pts',(2.31505926524131,1.56181301987131,-4.16333634234434E-16));
#258953=CARTESIAN_POINT('Ctrl Pts',(2.32233104844966,1.54827042680759,-4.20227015439185E-16));
#258954=CARTESIAN_POINT('Ctrl Pts',(2.3294983759238,1.53466764779613,-6.49847629289258E-17));
#258955=CARTESIAN_POINT('Ctrl Pts',(2.33655394576526,1.52101860731817,-8.32667268468867E-17));
#258956=CARTESIAN_POINT('Ctrl Pts',(2.38021790436486,1.43655042802932,-1.96406123602879E-16));
#258957=CARTESIAN_POINT('Ctrl Pts',(2.41967121036231,1.3501913449407,6.88706256054415E-17));
#258958=CARTESIAN_POINT('Ctrl Pts',(2.45474928345663,1.26228765150751,4.16333634234434E-17));
#258959=CARTESIAN_POINT('Ctrl Pts',(2.49092308776736,1.1716381167998,1.35452928648742E-17));
#258960=CARTESIAN_POINT('Ctrl Pts',(2.52244468369081,1.07934497178013,-2.21712706299005E-16));
#258961=CARTESIAN_POINT('Ctrl Pts',(2.54907591826243,0.985777684531876,
-6.93889390390723E-17));
#258962=CARTESIAN_POINT('Ctrl Pts',(2.57381682909422,0.898851939337636,
7.21226658098787E-17));
#258963=CARTESIAN_POINT('Ctrl Pts',(2.59433663472327,0.810825740820981,
-9.80095638385124E-17));
#258964=CARTESIAN_POINT('Ctrl Pts',(2.61039511711921,0.721999381027909,
-2.77555756156289E-17));
#258965=CARTESIAN_POINT('Ctrl Pts',(2.6195878391639,0.671150489103632,1.24615115499021E-17));
#258966=CARTESIAN_POINT('Ctrl Pts',(2.62731768360901,0.620039518677072,
-3.00496852254879E-16));
#258967=CARTESIAN_POINT('Ctrl Pts',(2.63353210695095,0.568724824688507,
-3.60822483003176E-16));
#258968=CARTESIAN_POINT('Ctrl Pts',(2.63589786401921,0.549189930889105,
-3.8378773327462E-16));
#258969=CARTESIAN_POINT('Ctrl Pts',(2.63804436688365,0.529620027364891,
-4.11084434172389E-16));
#258970=CARTESIAN_POINT('Ctrl Pts',(2.63996573358163,0.510050166638142,
-4.16333634234434E-16));
#258971=CARTESIAN_POINT('Ctrl Pts',(2.64867955611758,0.421296523929082,
-4.40139916421116E-16));
#258972=CARTESIAN_POINT('Ctrl Pts',(2.65278205939108,0.332438665006606,
4.43189382769785E-16));
#258973=CARTESIAN_POINT('Ctrl Pts',(2.6520903038075,0.243767416134848,3.05311331771918E-16));
#258974=CARTESIAN_POINT('Ctrl Pts',(2.65177499678039,0.203350441505137,
2.4246555300958E-16));
#258975=CARTESIAN_POINT('Ctrl Pts',(2.65046293738114,0.162972281097136,
-4.01413413377188E-16));
#258976=CARTESIAN_POINT('Ctrl Pts',(2.6481332116628,0.122661008583792,-4.16333634234434E-16));
#258977=CARTESIAN_POINT('Ctrl Pts',(2.64291502376441,0.0323706397470573,
-4.48739692579806E-16));
#258978=CARTESIAN_POINT('Ctrl Pts',(2.63259442660143,-0.0575857021650941,
-6.13287208414012E-16));
#258979=CARTESIAN_POINT('Ctrl Pts',(2.61736772417562,-0.146875162641521,
-7.21644966006352E-16));
#258980=CARTESIAN_POINT('Ctrl Pts',(2.60171400810126,-0.238668633325112,
-8.33041480128173E-16));
#258981=CARTESIAN_POINT('Ctrl Pts',(2.5808746796005,-0.329758351676144,
-1.90458112270157E-16));
#258982=CARTESIAN_POINT('Ctrl Pts',(2.55501621449523,-0.419750916628513,
-2.4980018054066E-16));
#258983=CARTESIAN_POINT('Ctrl Pts',(2.55103891410019,-0.433592707418413,
-2.58927606728312E-16));
#258984=CARTESIAN_POINT('Ctrl Pts',(2.54694279346922,-0.447408464297446,
3.75767635899293E-16));
#258985=CARTESIAN_POINT('Ctrl Pts',(2.5427283753618,-0.461196666179357,
3.88578058618805E-16));
#258986=CARTESIAN_POINT('Ctrl Pts',(2.53849453512576,-0.475048410933263,
4.0144751811904E-16));
#258987=CARTESIAN_POINT('Ctrl Pts',(2.53414344842462,-0.488865206644749,
8.48754092844161E-17));
#258988=CARTESIAN_POINT('Ctrl Pts',(2.52967811492983,-0.502639383000654,
8.32667268468867E-17));
#258989=CARTESIAN_POINT('Ctrl Pts',(2.50231167638331,-0.58705640385971,
7.340768516079E-17));
#258990=CARTESIAN_POINT('Ctrl Pts',(2.47063498600197,-0.669950084265983,
4.22436203556581E-17));
#258991=CARTESIAN_POINT('Ctrl Pts',(2.43486046177467,-0.751017022735213,
-2.77555756156289E-17));
#258992=CARTESIAN_POINT('Ctrl Pts',(2.399141311881,-0.831958480075241,-9.76464218907314E-17));
#258993=CARTESIAN_POINT('Ctrl Pts',(2.3593363425435,-0.911079627280405,
2.35473293751788E-18));
#258994=CARTESIAN_POINT('Ctrl Pts',(2.31561489444494,-0.98804847264715,
5.55111512312578E-17));
#258995=CARTESIAN_POINT('Ctrl Pts',(2.27259325787788,-1.06378534405382,
1.0781674055859E-16));
#258996=CARTESIAN_POINT('Ctrl Pts',(2.22577883862421,-1.13743887886136,
-1.12290620317281E-16));
#258997=CARTESIAN_POINT('Ctrl Pts',(2.17530221885831,-1.20865349993215,
-1.66533453693773E-16));
#258998=CARTESIAN_POINT('Ctrl Pts',(2.15809729115553,-1.23292696381674,
-1.85022093205784E-16));
#258999=CARTESIAN_POINT('Ctrl Pts',(2.14046667353494,-1.25691669716042,
-1.35829105932757E-16));
#259000=CARTESIAN_POINT('Ctrl Pts',(2.12241491153992,-1.28060735992797,
-1.66533453693773E-16));
#259001=CARTESIAN_POINT('Ctrl Pts',(2.11071608335196,-1.29596059765916,
-1.8643205911404E-16));
#259002=CARTESIAN_POINT('Ctrl Pts',(2.09884037016556,-1.31118821315322,
-3.70177197692537E-16));
#259003=CARTESIAN_POINT('Ctrl Pts',(2.08678895088832,-1.32628587161512,
-3.88578058618805E-16));
#259004=CARTESIAN_POINT('Ctrl Pts',(2.07852306914528,-1.33664112161282,
-4.01198924003022E-16));
#259005=CARTESIAN_POINT('Ctrl Pts',(2.07018042347752,-1.34692783442558,
-1.72843886385882E-16));
#259006=CARTESIAN_POINT('Ctrl Pts',(2.06176261244685,-1.35714381216209,
-1.66533453693773E-16));
#259007=CARTESIAN_POINT('Ctrl Pts',(2.00753927090544,-1.42295004705715,
-1.25884792671121E-16));
#259008=CARTESIAN_POINT('Ctrl Pts',(1.95018700439859,-1.48584042548277,
6.40190105150689E-17));
#259009=CARTESIAN_POINT('Ctrl Pts',(1.88986384968284,-1.54551861016893,
5.55111512312578E-17));
#259010=CARTESIAN_POINT('Ctrl Pts',(1.83049021222098,-1.60425742975877,
4.71372099963581E-17));
#259011=CARTESIAN_POINT('Ctrl Pts',(1.76823783877865,-1.65988489840281,
6.01633408062021E-17));
#259012=CARTESIAN_POINT('Ctrl Pts',(1.70323154838963,-1.71207601348042,
5.55111512312578E-17));
#259013=CARTESIAN_POINT('Ctrl Pts',(1.64025200525105,-1.76263992912321,
5.10040062723506E-17));
#259014=CARTESIAN_POINT('Ctrl Pts',(1.57468702241033,-1.80997871266923,
3.69270603532203E-16));
#259015=CARTESIAN_POINT('Ctrl Pts',(1.50663444364591,-1.85375106403961,
4.44089209850063E-16));
#259016=CARTESIAN_POINT('Ctrl Pts',(1.46438318762361,-1.88092765099674,
4.90541234860173E-16));
#259017=CARTESIAN_POINT('Ctrl Pts',(1.42117276288613,-1.90672856661623,
5.10338476158255E-17));
#259018=CARTESIAN_POINT('Ctrl Pts',(1.37702479013104,-1.93106208855763,
5.55111512312578E-17));
#259019=CARTESIAN_POINT('Ctrl Pts',(1.28892185405323,2.64462557919718,20.));
#259020=CARTESIAN_POINT('Ctrl Pts',(2.16862035685408,2.21588336549518,19.9470592864818));
#259021=CARTESIAN_POINT('Ctrl Pts',(2.80996391709042,1.31742092770971,19.8941185729635));
#259022=CARTESIAN_POINT('Ctrl Pts',(2.92551966779744,0.35179538187613,19.8411778594453));
#259023=CARTESIAN_POINT('Ctrl Pts',(3.04107541850447,-0.613830163957432,
19.788237145927));
#259024=CARTESIAN_POINT('Ctrl Pts',(2.63084335968222,-1.6466188178391,19.7352964324088));
#259025=CARTESIAN_POINT('Ctrl Pts',(1.88115112934642,-2.26900194906848,
19.6823557188906));
#259026=CARTESIAN_POINT('Ctrl Pts',(1.13145889901062,-2.89138508029788,
19.6294150053723));
#259027=CARTESIAN_POINT('Ctrl Pts',(0.0423064971612432,-3.10336268887498,
19.576474291854));
#259028=CARTESIAN_POINT('Ctrl Pts',(-0.886796187095413,-2.80996684498319,
19.5235335783358));
#259029=CARTESIAN_POINT('Ctrl Pts',(-1.81589887135208,-2.5165710010914,
19.4705928648176));
#259030=CARTESIAN_POINT('Ctrl Pts',(-2.58495183801603,-1.71780170473074,
19.4176521512993));
#259031=CARTESIAN_POINT('Ctrl Pts',(-2.84215954961242,-0.778381846021926,
19.3647114377811));
#259032=CARTESIAN_POINT('Ctrl Pts',(-2.91104423067048,-0.526788933254545,
19.3505329975506));
#259033=CARTESIAN_POINT('Ctrl Pts',(-2.94321623800843,-0.265107701502241,
19.3363545573201));
#259034=CARTESIAN_POINT('Ctrl Pts',(-2.94091171156293,-0.00284992947760021,
19.3221761170896));
#259035=CARTESIAN_POINT('Origin',(0.,0.,0.));
#259036=CARTESIAN_POINT('Origin',(0.,0.,20.));
#259037=CARTESIAN_POINT('Origin',(-1.44337567297407,-2.5,-6.));
#259038=CARTESIAN_POINT('',(-1.44337567297407,-2.5,-6.));
#259039=CARTESIAN_POINT('',(1.44337567297406,-2.5,-6.));
#259040=CARTESIAN_POINT('',(-0.721687836487033,-2.5,-6.));
#259041=CARTESIAN_POINT('',(-1.44337567297407,-2.5,-3.));
#259042=CARTESIAN_POINT('',(-1.44337567297407,-2.5,-6.));
#259043=CARTESIAN_POINT('',(1.44337567297406,-2.5,-3.));
#259044=CARTESIAN_POINT('',(-1.44337567297407,-2.5,-3.));
#259045=CARTESIAN_POINT('',(1.44337567297406,-2.5,-6.));
#259046=CARTESIAN_POINT('Origin',(-2.88675134594813,3.53525079574969E-16,
-6.));
#259047=CARTESIAN_POINT('',(-2.88675134594813,3.53525079574969E-16,-6.));
#259048=CARTESIAN_POINT('',(-2.52590742770461,-0.625,-6.));
#259049=CARTESIAN_POINT('',(-2.88675134594813,5.55111512312578E-16,-3.));
#259050=CARTESIAN_POINT('',(-2.88675134594813,3.53525079574969E-16,-6.));
#259051=CARTESIAN_POINT('',(-2.88675134594813,3.53525079574969E-16,-3.));
#259052=CARTESIAN_POINT('Origin',(-1.44337567297406,2.5,-6.));
#259053=CARTESIAN_POINT('',(-1.44337567297406,2.5,-6.));
#259054=CARTESIAN_POINT('',(-1.80421959121758,1.875,-6.));
#259055=CARTESIAN_POINT('',(-1.44337567297406,2.5,-3.));
#259056=CARTESIAN_POINT('',(-1.44337567297406,2.5,-6.));
#259057=CARTESIAN_POINT('',(-1.44337567297406,2.5,-3.));
#259058=CARTESIAN_POINT('Origin',(1.44337567297406,2.5,-6.));
#259059=CARTESIAN_POINT('',(1.44337567297406,2.5,-6.));
#259060=CARTESIAN_POINT('',(0.721687836487033,2.5,-6.));
#259061=CARTESIAN_POINT('',(1.44337567297406,2.5,-3.));
#259062=CARTESIAN_POINT('',(1.44337567297406,2.5,-6.));
#259063=CARTESIAN_POINT('',(1.44337567297406,2.5,-3.));
#259064=CARTESIAN_POINT('Origin',(2.88675134594813,0.,-6.));
#259065=CARTESIAN_POINT('',(2.88675134594813,0.,-6.));
#259066=CARTESIAN_POINT('',(2.52590742770461,0.625,-6.));
#259067=CARTESIAN_POINT('',(2.88675134594813,0.,-3.));
#259068=CARTESIAN_POINT('',(2.88675134594813,0.,-6.));
#259069=CARTESIAN_POINT('',(2.88675134594813,0.,-3.));
#259070=CARTESIAN_POINT('Origin',(1.44337567297406,-2.5,-6.));
#259071=CARTESIAN_POINT('',(1.80421959121758,-1.875,-6.));
#259072=CARTESIAN_POINT('',(1.44337567297406,-2.5,-3.));
#259073=CARTESIAN_POINT('Origin',(0.,0.,-3.));
#259074=CARTESIAN_POINT('Origin',(0.,0.,0.));
#259075=CARTESIAN_POINT('',(-5.,-6.12323399573677E-16,0.));
#259076=CARTESIAN_POINT('Origin',(0.,0.,0.));
#259077=CARTESIAN_POINT('Origin',(0.,0.,-6.));
#259078=CARTESIAN_POINT('',(-5.,-6.12323399573677E-16,-6.));
#259079=CARTESIAN_POINT('',(-5.,-6.12323399573677E-16,-6.));
#259080=CARTESIAN_POINT('Origin',(0.,0.,-6.));
#259081=CARTESIAN_POINT('Origin',(0.,0.,-6.));
#259082=CARTESIAN_POINT('Origin',(0.,0.,20.));
#259201=UNCERTAINTY_MEASURE_WITH_UNIT(LENGTH_MEASURE(0.01),#259225,
'DISTANCE_ACCURACY_VALUE',
'Maximum model space distance between geometric entities at asserted c
onnectivities');
#259202=UNCERTAINTY_MEASURE_WITH_UNIT(LENGTH_MEASURE(0.01),#259225,
'DISTANCE_ACCURACY_VALUE',
'Maximum model space distance between geometric entities at asserted c
onnectivities');
#259223=(
GEOMETRIC_REPRESENTATION_CONTEXT(3)
GLOBAL_UNCERTAINTY_ASSIGNED_CONTEXT((#259201))
GLOBAL_UNIT_ASSIGNED_CONTEXT((#259225,#259227,#259228))
REPRESENTATION_CONTEXT('','3D')
);
#259224=(
GEOMETRIC_REPRESENTATION_CONTEXT(3)
GLOBAL_UNCERTAINTY_ASSIGNED_CONTEXT((#259202))
GLOBAL_UNIT_ASSIGNED_CONTEXT((#259225,#259227,#259228))
REPRESENTATION_CONTEXT('','3D')
);
#259225=(
LENGTH_UNIT()
NAMED_UNIT(*)
SI_UNIT(.MILLI.,.METRE.)
);
#259227=(
NAMED_UNIT(*)
PLANE_ANGLE_UNIT()
SI_UNIT($,.RADIAN.)
);
#259228=(
NAMED_UNIT(*)
SI_UNIT($,.STERADIAN.)
SOLID_ANGLE_UNIT()
);
#259249=SHAPE_DEFINITION_REPRESENTATION(#259270,#259389);
#259270=PRODUCT_DEFINITION_SHAPE('',$,#259411);
#259389=SHAPE_REPRESENTATION('',(#27176),#259223);
#259390=PRODUCT_DEFINITION_CONTEXT('part definition',#259455,'design');
#259411=PRODUCT_DEFINITION('Socket head cap screw M6x20',
'Socket head cap screw M6x20',#259432,#259390);
#259432=PRODUCT_DEFINITION_FORMATION('',$,#259477);
#259455=APPLICATION_CONTEXT(
'Core Data for Automotive Mechanical Design Process');
#259456=PRODUCT_CONTEXT('part definition',#259455,'mechanical');
#259477=PRODUCT('Socket head cap screw M6x20',
'Socket head cap screw M6x20',$,(#259456));
#259492=PRESENTATION_STYLE_ASSIGNMENT((#259507));
#259507=SURFACE_STYLE_USAGE(.BOTH.,#259522);
#259522=SURFACE_SIDE_STYLE('',(#259537));
#259537=SURFACE_STYLE_FILL_AREA(#259552);
#259552=FILL_AREA_STYLE('Fastener dark gray',(#259567));
#259567=FILL_AREA_STYLE_COLOUR('Fastener dark gray',#259582);
#259582=COLOUR_RGB('Fastener dark gray',0.250980392156863,0.282352941176471,
0.32156862745098);
ENDSEC;
END-ISO-10303-21;
